ISO-10303-21;
HEADER;
/* Generated by software containing ST-Developer
 * from STEP Tools, Inc. (www.steptools.com) 
 */
/* OPTION: using custom renumber hook */

FILE_DESCRIPTION(
/* description */ ('STEP AP242 Edition 2', 'CAx-IF Rec.Pracs.---Representation and Presentation of Product Manufa
cturing Information (PMI)---4.0---2014-10-13', 'CAx-IF Rec.Pracs.---3D Tessellated Geometry---0.4---2014-09-14', '2;1', 'CAx-IF Rec.Pracs.---User Defined Attributes---1.5---2016-08-15'),
/* implementation_level */ '2;1');

FILE_NAME(
/* name */ '75632s_.prt.step',
/* time_stamp */ '2026-10-08T12:15:07Z',
/* author */ (''),
/* organization */ (''),
/* preprocessor_version */ 'ST-DEVELOPER v20',
/* originating_system */ 'ONSHAPE BY PTC INC, 1.221',
/* authorisation */ '  ');

FILE_SCHEMA (('AP242_MANAGED_MODEL_BASED_3D_ENGINEERING_MIM_LF { 1 0 10303 442 3 1 4 }'));
ENDSEC;

DATA;
#41=B_SPLINE_SURFACE_WITH_KNOTS('',3,3,((#20582,#20583,#20584,#20585,#20586,
#20587,#20588,#20589,#20590,#20591,#20592,#20593,#20594,#20595,#20596,#20597,
#20598,#20599,#20600,#20601,#20602,#20603,#20604,#20605,#20606,#20607,#20608,
#20609,#20610,#20611,#20612,#20613,#20614,#20615),(#20616,#20617,#20618,
#20619,#20620,#20621,#20622,#20623,#20624,#20625,#20626,#20627,#20628,#20629,
#20630,#20631,#20632,#20633,#20634,#20635,#20636,#20637,#20638,#20639,#20640,
#20641,#20642,#20643,#20644,#20645,#20646,#20647,#20648,#20649),(#20650,
#20651,#20652,#20653,#20654,#20655,#20656,#20657,#20658,#20659,#20660,#20661,
#20662,#20663,#20664,#20665,#20666,#20667,#20668,#20669,#20670,#20671,#20672,
#20673,#20674,#20675,#20676,#20677,#20678,#20679,#20680,#20681,#20682,#20683),
(#20684,#20685,#20686,#20687,#20688,#20689,#20690,#20691,#20692,#20693,
#20694,#20695,#20696,#20697,#20698,#20699,#20700,#20701,#20702,#20703,#20704,
#20705,#20706,#20707,#20708,#20709,#20710,#20711,#20712,#20713,#20714,#20715,
#20716,#20717),(#20718,#20719,#20720,#20721,#20722,#20723,#20724,#20725,
#20726,#20727,#20728,#20729,#20730,#20731,#20732,#20733,#20734,#20735,#20736,
#20737,#20738,#20739,#20740,#20741,#20742,#20743,#20744,#20745,#20746,#20747,
#20748,#20749,#20750,#20751),(#20752,#20753,#20754,#20755,#20756,#20757,
#20758,#20759,#20760,#20761,#20762,#20763,#20764,#20765,#20766,#20767,#20768,
#20769,#20770,#20771,#20772,#20773,#20774,#20775,#20776,#20777,#20778,#20779,
#20780,#20781,#20782,#20783,#20784,#20785),(#20786,#20787,#20788,#20789,
#20790,#20791,#20792,#20793,#20794,#20795,#20796,#20797,#20798,#20799,#20800,
#20801,#20802,#20803,#20804,#20805,#20806,#20807,#20808,#20809,#20810,#20811,
#20812,#20813,#20814,#20815,#20816,#20817,#20818,#20819),(#20820,#20821,
#20822,#20823,#20824,#20825,#20826,#20827,#20828,#20829,#20830,#20831,#20832,
#20833,#20834,#20835,#20836,#20837,#20838,#20839,#20840,#20841,#20842,#20843,
#20844,#20845,#20846,#20847,#20848,#20849,#20850,#20851,#20852,#20853),
(#20854,#20855,#20856,#20857,#20858,#20859,#20860,#20861,#20862,#20863,
#20864,#20865,#20866,#20867,#20868,#20869,#20870,#20871,#20872,#20873,#20874,
#20875,#20876,#20877,#20878,#20879,#20880,#20881,#20882,#20883,#20884,#20885,
#20886,#20887),(#20888,#20889,#20890,#20891,#20892,#20893,#20894,#20895,
#20896,#20897,#20898,#20899,#20900,#20901,#20902,#20903,#20904,#20905,#20906,
#20907,#20908,#20909,#20910,#20911,#20912,#20913,#20914,#20915,#20916,#20917,
#20918,#20919,#20920,#20921),(#20922,#20923,#20924,#20925,#20926,#20927,
#20928,#20929,#20930,#20931,#20932,#20933,#20934,#20935,#20936,#20937,#20938,
#20939,#20940,#20941,#20942,#20943,#20944,#20945,#20946,#20947,#20948,#20949,
#20950,#20951,#20952,#20953,#20954,#20955),(#20956,#20957,#20958,#20959,
#20960,#20961,#20962,#20963,#20964,#20965,#20966,#20967,#20968,#20969,#20970,
#20971,#20972,#20973,#20974,#20975,#20976,#20977,#20978,#20979,#20980,#20981,
#20982,#20983,#20984,#20985,#20986,#20987,#20988,#20989),(#20990,#20991,
#20992,#20993,#20994,#20995,#20996,#20997,#20998,#20999,#21000,#21001,#21002,
#21003,#21004,#21005,#21006,#21007,#21008,#21009,#21010,#21011,#21012,#21013,
#21014,#21015,#21016,#21017,#21018,#21019,#21020,#21021,#21022,#21023),
(#21024,#21025,#21026,#21027,#21028,#21029,#21030,#21031,#21032,#21033,
#21034,#21035,#21036,#21037,#21038,#21039,#21040,#21041,#21042,#21043,#21044,
#21045,#21046,#21047,#21048,#21049,#21050,#21051,#21052,#21053,#21054,#21055,
#21056,#21057)),.UNSPECIFIED.,.F.,.F.,.F.,(4,2,2,2,2,2,4),(4,2,2,2,2,2,
2,2,2,2,2,2,2,2,2,2,4),(0.496999950768087,0.5,0.625,0.75,0.875,1.,1.00300004881078),
(-0.00600030525376163,0.0450000000000826,0.110000000000075,0.175000000000067,
0.24000000000006,0.305000000000052,0.370000000000045,0.435000000000037,
0.500000000000029,0.565000000000022,0.630000000000014,0.695,0.76,0.824999999999991,
0.889999999999984,0.954999999999976,1.00600015524748),.UNSPECIFIED.);
#42=B_SPLINE_SURFACE_WITH_KNOTS('',3,3,((#21089,#21090,#21091,#21092,#21093,
#21094,#21095,#21096,#21097,#21098,#21099,#21100,#21101,#21102,#21103,#21104,
#21105,#21106,#21107,#21108,#21109,#21110,#21111,#21112,#21113,#21114,#21115,
#21116,#21117,#21118,#21119,#21120,#21121,#21122),(#21123,#21124,#21125,
#21126,#21127,#21128,#21129,#21130,#21131,#21132,#21133,#21134,#21135,#21136,
#21137,#21138,#21139,#21140,#21141,#21142,#21143,#21144,#21145,#21146,#21147,
#21148,#21149,#21150,#21151,#21152,#21153,#21154,#21155,#21156),(#21157,
#21158,#21159,#21160,#21161,#21162,#21163,#21164,#21165,#21166,#21167,#21168,
#21169,#21170,#21171,#21172,#21173,#21174,#21175,#21176,#21177,#21178,#21179,
#21180,#21181,#21182,#21183,#21184,#21185,#21186,#21187,#21188,#21189,#21190),
(#21191,#21192,#21193,#21194,#21195,#21196,#21197,#21198,#21199,#21200,
#21201,#21202,#21203,#21204,#21205,#21206,#21207,#21208,#21209,#21210,#21211,
#21212,#21213,#21214,#21215,#21216,#21217,#21218,#21219,#21220,#21221,#21222,
#21223,#21224),(#21225,#21226,#21227,#21228,#21229,#21230,#21231,#21232,
#21233,#21234,#21235,#21236,#21237,#21238,#21239,#21240,#21241,#21242,#21243,
#21244,#21245,#21246,#21247,#21248,#21249,#21250,#21251,#21252,#21253,#21254,
#21255,#21256,#21257,#21258),(#21259,#21260,#21261,#21262,#21263,#21264,
#21265,#21266,#21267,#21268,#21269,#21270,#21271,#21272,#21273,#21274,#21275,
#21276,#21277,#21278,#21279,#21280,#21281,#21282,#21283,#21284,#21285,#21286,
#21287,#21288,#21289,#21290,#21291,#21292),(#21293,#21294,#21295,#21296,
#21297,#21298,#21299,#21300,#21301,#21302,#21303,#21304,#21305,#21306,#21307,
#21308,#21309,#21310,#21311,#21312,#21313,#21314,#21315,#21316,#21317,#21318,
#21319,#21320,#21321,#21322,#21323,#21324,#21325,#21326),(#21327,#21328,
#21329,#21330,#21331,#21332,#21333,#21334,#21335,#21336,#21337,#21338,#21339,
#21340,#21341,#21342,#21343,#21344,#21345,#21346,#21347,#21348,#21349,#21350,
#21351,#21352,#21353,#21354,#21355,#21356,#21357,#21358,#21359,#21360),
(#21361,#21362,#21363,#21364,#21365,#21366,#21367,#21368,#21369,#21370,
#21371,#21372,#21373,#21374,#21375,#21376,#21377,#21378,#21379,#21380,#21381,
#21382,#21383,#21384,#21385,#21386,#21387,#21388,#21389,#21390,#21391,#21392,
#21393,#21394),(#21395,#21396,#21397,#21398,#21399,#21400,#21401,#21402,
#21403,#21404,#21405,#21406,#21407,#21408,#21409,#21410,#21411,#21412,#21413,
#21414,#21415,#21416,#21417,#21418,#21419,#21420,#21421,#21422,#21423,#21424,
#21425,#21426,#21427,#21428),(#21429,#21430,#21431,#21432,#21433,#21434,
#21435,#21436,#21437,#21438,#21439,#21440,#21441,#21442,#21443,#21444,#21445,
#21446,#21447,#21448,#21449,#21450,#21451,#21452,#21453,#21454,#21455,#21456,
#21457,#21458,#21459,#21460,#21461,#21462),(#21463,#21464,#21465,#21466,
#21467,#21468,#21469,#21470,#21471,#21472,#21473,#21474,#21475,#21476,#21477,
#21478,#21479,#21480,#21481,#21482,#21483,#21484,#21485,#21486,#21487,#21488,
#21489,#21490,#21491,#21492,#21493,#21494,#21495,#21496),(#21497,#21498,
#21499,#21500,#21501,#21502,#21503,#21504,#21505,#21506,#21507,#21508,#21509,
#21510,#21511,#21512,#21513,#21514,#21515,#21516,#21517,#21518,#21519,#21520,
#21521,#21522,#21523,#21524,#21525,#21526,#21527,#21528,#21529,#21530),
(#21531,#21532,#21533,#21534,#21535,#21536,#21537,#21538,#21539,#21540,
#21541,#21542,#21543,#21544,#21545,#21546,#21547,#21548,#21549,#21550,#21551,
#21552,#21553,#21554,#21555,#21556,#21557,#21558,#21559,#21560,#21561,#21562,
#21563,#21564)),.UNSPECIFIED.,.F.,.F.,.F.,(4,2,2,2,2,2,4),(4,2,2,2,2,2,
2,2,2,2,2,2,2,2,2,2,4),(-0.00024497105823581,0.,0.125,0.25,0.375,0.5,0.500244971058236),
(-1.90758107793014E-7,0.0450000000000825,0.110000000000075,0.175000000000067,
0.240000000000059,0.305000000000052,0.370000000000044,0.435000000000037,
0.500000000000029,0.565000000000021,0.630000000000014,0.695,0.76,0.824999999999991,
0.889999999999983,0.954999999999975,1.00000029951007),.UNSPECIFIED.);
#43=B_SPLINE_SURFACE_WITH_KNOTS('',3,3,((#21676,#21677,#21678,#21679,#21680,
#21681,#21682,#21683,#21684,#21685,#21686,#21687,#21688,#21689,#21690,#21691,
#21692,#21693,#21694,#21695,#21696,#21697,#21698,#21699,#21700,#21701,#21702,
#21703,#21704,#21705,#21706,#21707,#21708,#21709),(#21710,#21711,#21712,
#21713,#21714,#21715,#21716,#21717,#21718,#21719,#21720,#21721,#21722,#21723,
#21724,#21725,#21726,#21727,#21728,#21729,#21730,#21731,#21732,#21733,#21734,
#21735,#21736,#21737,#21738,#21739,#21740,#21741,#21742,#21743),(#21744,
#21745,#21746,#21747,#21748,#21749,#21750,#21751,#21752,#21753,#21754,#21755,
#21756,#21757,#21758,#21759,#21760,#21761,#21762,#21763,#21764,#21765,#21766,
#21767,#21768,#21769,#21770,#21771,#21772,#21773,#21774,#21775,#21776,#21777),
(#21778,#21779,#21780,#21781,#21782,#21783,#21784,#21785,#21786,#21787,
#21788,#21789,#21790,#21791,#21792,#21793,#21794,#21795,#21796,#21797,#21798,
#21799,#21800,#21801,#21802,#21803,#21804,#21805,#21806,#21807,#21808,#21809,
#21810,#21811),(#21812,#21813,#21814,#21815,#21816,#21817,#21818,#21819,
#21820,#21821,#21822,#21823,#21824,#21825,#21826,#21827,#21828,#21829,#21830,
#21831,#21832,#21833,#21834,#21835,#21836,#21837,#21838,#21839,#21840,#21841,
#21842,#21843,#21844,#21845),(#21846,#21847,#21848,#21849,#21850,#21851,
#21852,#21853,#21854,#21855,#21856,#21857,#21858,#21859,#21860,#21861,#21862,
#21863,#21864,#21865,#21866,#21867,#21868,#21869,#21870,#21871,#21872,#21873,
#21874,#21875,#21876,#21877,#21878,#21879),(#21880,#21881,#21882,#21883,
#21884,#21885,#21886,#21887,#21888,#21889,#21890,#21891,#21892,#21893,#21894,
#21895,#21896,#21897,#21898,#21899,#21900,#21901,#21902,#21903,#21904,#21905,
#21906,#21907,#21908,#21909,#21910,#21911,#21912,#21913),(#21914,#21915,
#21916,#21917,#21918,#21919,#21920,#21921,#21922,#21923,#21924,#21925,#21926,
#21927,#21928,#21929,#21930,#21931,#21932,#21933,#21934,#21935,#21936,#21937,
#21938,#21939,#21940,#21941,#21942,#21943,#21944,#21945,#21946,#21947),
(#21948,#21949,#21950,#21951,#21952,#21953,#21954,#21955,#21956,#21957,
#21958,#21959,#21960,#21961,#21962,#21963,#21964,#21965,#21966,#21967,#21968,
#21969,#21970,#21971,#21972,#21973,#21974,#21975,#21976,#21977,#21978,#21979,
#21980,#21981),(#21982,#21983,#21984,#21985,#21986,#21987,#21988,#21989,
#21990,#21991,#21992,#21993,#21994,#21995,#21996,#21997,#21998,#21999,#22000,
#22001,#22002,#22003,#22004,#22005,#22006,#22007,#22008,#22009,#22010,#22011,
#22012,#22013,#22014,#22015),(#22016,#22017,#22018,#22019,#22020,#22021,
#22022,#22023,#22024,#22025,#22026,#22027,#22028,#22029,#22030,#22031,#22032,
#22033,#22034,#22035,#22036,#22037,#22038,#22039,#22040,#22041,#22042,#22043,
#22044,#22045,#22046,#22047,#22048,#22049),(#22050,#22051,#22052,#22053,
#22054,#22055,#22056,#22057,#22058,#22059,#22060,#22061,#22062,#22063,#22064,
#22065,#22066,#22067,#22068,#22069,#22070,#22071,#22072,#22073,#22074,#22075,
#22076,#22077,#22078,#22079,#22080,#22081,#22082,#22083),(#22084,#22085,
#22086,#22087,#22088,#22089,#22090,#22091,#22092,#22093,#22094,#22095,#22096,
#22097,#22098,#22099,#22100,#22101,#22102,#22103,#22104,#22105,#22106,#22107,
#22108,#22109,#22110,#22111,#22112,#22113,#22114,#22115,#22116,#22117),
(#22118,#22119,#22120,#22121,#22122,#22123,#22124,#22125,#22126,#22127,
#22128,#22129,#22130,#22131,#22132,#22133,#22134,#22135,#22136,#22137,#22138,
#22139,#22140,#22141,#22142,#22143,#22144,#22145,#22146,#22147,#22148,#22149,
#22150,#22151),(#22152,#22153,#22154,#22155,#22156,#22157,#22158,#22159,
#22160,#22161,#22162,#22163,#22164,#22165,#22166,#22167,#22168,#22169,#22170,
#22171,#22172,#22173,#22174,#22175,#22176,#22177,#22178,#22179,#22180,#22181,
#22182,#22183,#22184,#22185),(#22186,#22187,#22188,#22189,#22190,#22191,
#22192,#22193,#22194,#22195,#22196,#22197,#22198,#22199,#22200,#22201,#22202,
#22203,#22204,#22205,#22206,#22207,#22208,#22209,#22210,#22211,#22212,#22213,
#22214,#22215,#22216,#22217,#22218,#22219)),.UNSPECIFIED.,.F.,.F.,.F.,(4,
2,2,2,2,2,2,4),(4,2,2,2,2,2,2,2,2,2,2,2,2,2,2,2,4),(0.499748503678476,0.5,
0.6,0.7,0.8,0.9,1.,1.00025149632152),(-1.92698650980853E-7,0.0450000000000825,
0.110000000000075,0.175000000000067,0.240000000000059,0.305000000000052,
0.370000000000044,0.435000000000037,0.500000000000029,0.565000000000021,
0.630000000000013,0.695,0.76,0.82499999999999,0.889999999999983,0.954999999999975,
1.00000029951007),.UNSPECIFIED.);
#44=B_SPLINE_SURFACE_WITH_KNOTS('',3,3,((#22251,#22252,#22253,#22254,#22255,
#22256,#22257,#22258,#22259,#22260,#22261,#22262,#22263,#22264,#22265,#22266,
#22267,#22268,#22269,#22270,#22271,#22272,#22273,#22274,#22275,#22276,#22277,
#22278,#22279,#22280,#22281,#22282,#22283,#22284),(#22285,#22286,#22287,
#22288,#22289,#22290,#22291,#22292,#22293,#22294,#22295,#22296,#22297,#22298,
#22299,#22300,#22301,#22302,#22303,#22304,#22305,#22306,#22307,#22308,#22309,
#22310,#22311,#22312,#22313,#22314,#22315,#22316,#22317,#22318),(#22319,
#22320,#22321,#22322,#22323,#22324,#22325,#22326,#22327,#22328,#22329,#22330,
#22331,#22332,#22333,#22334,#22335,#22336,#22337,#22338,#22339,#22340,#22341,
#22342,#22343,#22344,#22345,#22346,#22347,#22348,#22349,#22350,#22351,#22352),
(#22353,#22354,#22355,#22356,#22357,#22358,#22359,#22360,#22361,#22362,
#22363,#22364,#22365,#22366,#22367,#22368,#22369,#22370,#22371,#22372,#22373,
#22374,#22375,#22376,#22377,#22378,#22379,#22380,#22381,#22382,#22383,#22384,
#22385,#22386),(#22387,#22388,#22389,#22390,#22391,#22392,#22393,#22394,
#22395,#22396,#22397,#22398,#22399,#22400,#22401,#22402,#22403,#22404,#22405,
#22406,#22407,#22408,#22409,#22410,#22411,#22412,#22413,#22414,#22415,#22416,
#22417,#22418,#22419,#22420),(#22421,#22422,#22423,#22424,#22425,#22426,
#22427,#22428,#22429,#22430,#22431,#22432,#22433,#22434,#22435,#22436,#22437,
#22438,#22439,#22440,#22441,#22442,#22443,#22444,#22445,#22446,#22447,#22448,
#22449,#22450,#22451,#22452,#22453,#22454),(#22455,#22456,#22457,#22458,
#22459,#22460,#22461,#22462,#22463,#22464,#22465,#22466,#22467,#22468,#22469,
#22470,#22471,#22472,#22473,#22474,#22475,#22476,#22477,#22478,#22479,#22480,
#22481,#22482,#22483,#22484,#22485,#22486,#22487,#22488),(#22489,#22490,
#22491,#22492,#22493,#22494,#22495,#22496,#22497,#22498,#22499,#22500,#22501,
#22502,#22503,#22504,#22505,#22506,#22507,#22508,#22509,#22510,#22511,#22512,
#22513,#22514,#22515,#22516,#22517,#22518,#22519,#22520,#22521,#22522),
(#22523,#22524,#22525,#22526,#22527,#22528,#22529,#22530,#22531,#22532,
#22533,#22534,#22535,#22536,#22537,#22538,#22539,#22540,#22541,#22542,#22543,
#22544,#22545,#22546,#22547,#22548,#22549,#22550,#22551,#22552,#22553,#22554,
#22555,#22556),(#22557,#22558,#22559,#22560,#22561,#22562,#22563,#22564,
#22565,#22566,#22567,#22568,#22569,#22570,#22571,#22572,#22573,#22574,#22575,
#22576,#22577,#22578,#22579,#22580,#22581,#22582,#22583,#22584,#22585,#22586,
#22587,#22588,#22589,#22590),(#22591,#22592,#22593,#22594,#22595,#22596,
#22597,#22598,#22599,#22600,#22601,#22602,#22603,#22604,#22605,#22606,#22607,
#22608,#22609,#22610,#22611,#22612,#22613,#22614,#22615,#22616,#22617,#22618,
#22619,#22620,#22621,#22622,#22623,#22624),(#22625,#22626,#22627,#22628,
#22629,#22630,#22631,#22632,#22633,#22634,#22635,#22636,#22637,#22638,#22639,
#22640,#22641,#22642,#22643,#22644,#22645,#22646,#22647,#22648,#22649,#22650,
#22651,#22652,#22653,#22654,#22655,#22656,#22657,#22658),(#22659,#22660,
#22661,#22662,#22663,#22664,#22665,#22666,#22667,#22668,#22669,#22670,#22671,
#22672,#22673,#22674,#22675,#22676,#22677,#22678,#22679,#22680,#22681,#22682,
#22683,#22684,#22685,#22686,#22687,#22688,#22689,#22690,#22691,#22692),
(#22693,#22694,#22695,#22696,#22697,#22698,#22699,#22700,#22701,#22702,
#22703,#22704,#22705,#22706,#22707,#22708,#22709,#22710,#22711,#22712,#22713,
#22714,#22715,#22716,#22717,#22718,#22719,#22720,#22721,#22722,#22723,#22724,
#22725,#22726)),.UNSPECIFIED.,.F.,.F.,.F.,(4,2,2,2,2,2,4),(4,2,2,2,2,2,
2,2,2,2,2,2,2,2,2,2,4),(0.487638113642685,0.5,0.625,0.75,0.875,1.,1.01236188635731),
(9.7389676693069,10.1395200046188,10.5400723399307,10.9406246752426,11.3411770105545,
11.7417293458665,12.1422816811784,12.5428340164903,12.9433863518022,13.3439386871141,
13.744491022426,14.1450433577379,14.5455956930498,14.9461480283618,15.3467003636736,
15.7472526989856,16.1478050342975),.UNSPECIFIED.);
#45=B_SPLINE_SURFACE_WITH_KNOTS('',3,3,((#22758,#22759,#22760,#22761,#22762,
#22763,#22764,#22765,#22766,#22767,#22768,#22769,#22770,#22771,#22772,#22773,
#22774,#22775,#22776,#22777,#22778,#22779,#22780,#22781,#22782,#22783,#22784,
#22785,#22786,#22787,#22788,#22789,#22790,#22791),(#22792,#22793,#22794,
#22795,#22796,#22797,#22798,#22799,#22800,#22801,#22802,#22803,#22804,#22805,
#22806,#22807,#22808,#22809,#22810,#22811,#22812,#22813,#22814,#22815,#22816,
#22817,#22818,#22819,#22820,#22821,#22822,#22823,#22824,#22825),(#22826,
#22827,#22828,#22829,#22830,#22831,#22832,#22833,#22834,#22835,#22836,#22837,
#22838,#22839,#22840,#22841,#22842,#22843,#22844,#22845,#22846,#22847,#22848,
#22849,#22850,#22851,#22852,#22853,#22854,#22855,#22856,#22857,#22858,#22859),
(#22860,#22861,#22862,#22863,#22864,#22865,#22866,#22867,#22868,#22869,
#22870,#22871,#22872,#22873,#22874,#22875,#22876,#22877,#22878,#22879,#22880,
#22881,#22882,#22883,#22884,#22885,#22886,#22887,#22888,#22889,#22890,#22891,
#22892,#22893),(#22894,#22895,#22896,#22897,#22898,#22899,#22900,#22901,
#22902,#22903,#22904,#22905,#22906,#22907,#22908,#22909,#22910,#22911,#22912,
#22913,#22914,#22915,#22916,#22917,#22918,#22919,#22920,#22921,#22922,#22923,
#22924,#22925,#22926,#22927),(#22928,#22929,#22930,#22931,#22932,#22933,
#22934,#22935,#22936,#22937,#22938,#22939,#22940,#22941,#22942,#22943,#22944,
#22945,#22946,#22947,#22948,#22949,#22950,#22951,#22952,#22953,#22954,#22955,
#22956,#22957,#22958,#22959,#22960,#22961),(#22962,#22963,#22964,#22965,
#22966,#22967,#22968,#22969,#22970,#22971,#22972,#22973,#22974,#22975,#22976,
#22977,#22978,#22979,#22980,#22981,#22982,#22983,#22984,#22985,#22986,#22987,
#22988,#22989,#22990,#22991,#22992,#22993,#22994,#22995),(#22996,#22997,
#22998,#22999,#23000,#23001,#23002,#23003,#23004,#23005,#23006,#23007,#23008,
#23009,#23010,#23011,#23012,#23013,#23014,#23015,#23016,#23017,#23018,#23019,
#23020,#23021,#23022,#23023,#23024,#23025,#23026,#23027,#23028,#23029),
(#23030,#23031,#23032,#23033,#23034,#23035,#23036,#23037,#23038,#23039,
#23040,#23041,#23042,#23043,#23044,#23045,#23046,#23047,#23048,#23049,#23050,
#23051,#23052,#23053,#23054,#23055,#23056,#23057,#23058,#23059,#23060,#23061,
#23062,#23063),(#23064,#23065,#23066,#23067,#23068,#23069,#23070,#23071,
#23072,#23073,#23074,#23075,#23076,#23077,#23078,#23079,#23080,#23081,#23082,
#23083,#23084,#23085,#23086,#23087,#23088,#23089,#23090,#23091,#23092,#23093,
#23094,#23095,#23096,#23097),(#23098,#23099,#23100,#23101,#23102,#23103,
#23104,#23105,#23106,#23107,#23108,#23109,#23110,#23111,#23112,#23113,#23114,
#23115,#23116,#23117,#23118,#23119,#23120,#23121,#23122,#23123,#23124,#23125,
#23126,#23127,#23128,#23129,#23130,#23131),(#23132,#23133,#23134,#23135,
#23136,#23137,#23138,#23139,#23140,#23141,#23142,#23143,#23144,#23145,#23146,
#23147,#23148,#23149,#23150,#23151,#23152,#23153,#23154,#23155,#23156,#23157,
#23158,#23159,#23160,#23161,#23162,#23163,#23164,#23165),(#23166,#23167,
#23168,#23169,#23170,#23171,#23172,#23173,#23174,#23175,#23176,#23177,#23178,
#23179,#23180,#23181,#23182,#23183,#23184,#23185,#23186,#23187,#23188,#23189,
#23190,#23191,#23192,#23193,#23194,#23195,#23196,#23197,#23198,#23199),
(#23200,#23201,#23202,#23203,#23204,#23205,#23206,#23207,#23208,#23209,
#23210,#23211,#23212,#23213,#23214,#23215,#23216,#23217,#23218,#23219,#23220,
#23221,#23222,#23223,#23224,#23225,#23226,#23227,#23228,#23229,#23230,#23231,
#23232,#23233)),.UNSPECIFIED.,.F.,.F.,.F.,(4,2,2,2,2,2,4),(4,2,2,2,2,2,
2,2,2,2,2,2,2,2,2,2,4),(-0.0123618863573116,0.,0.125,0.25,0.375,0.5,0.512361886357312),
(9.7389676693069,10.1395200046188,10.5400723399307,10.9406246752426,11.3411770105545,
11.7417293458665,12.1422816811784,12.5428340164903,12.9433863518022,13.3439386871141,
13.744491022426,14.1450433577379,14.5455956930498,14.9461480283618,15.3467003636736,
15.7472526989856,16.1478050342975),.UNSPECIFIED.);
#46=B_SPLINE_SURFACE_WITH_KNOTS('',3,3,((#23241,#23242,#23243,#23244,#23245,
#23246,#23247,#23248,#23249,#23250,#23251,#23252,#23253,#23254,#23255,#23256,
#23257,#23258,#23259,#23260,#23261,#23262,#23263,#23264,#23265,#23266,#23267,
#23268,#23269,#23270,#23271,#23272,#23273,#23274),(#23275,#23276,#23277,
#23278,#23279,#23280,#23281,#23282,#23283,#23284,#23285,#23286,#23287,#23288,
#23289,#23290,#23291,#23292,#23293,#23294,#23295,#23296,#23297,#23298,#23299,
#23300,#23301,#23302,#23303,#23304,#23305,#23306,#23307,#23308),(#23309,
#23310,#23311,#23312,#23313,#23314,#23315,#23316,#23317,#23318,#23319,#23320,
#23321,#23322,#23323,#23324,#23325,#23326,#23327,#23328,#23329,#23330,#23331,
#23332,#23333,#23334,#23335,#23336,#23337,#23338,#23339,#23340,#23341,#23342),
(#23343,#23344,#23345,#23346,#23347,#23348,#23349,#23350,#23351,#23352,
#23353,#23354,#23355,#23356,#23357,#23358,#23359,#23360,#23361,#23362,#23363,
#23364,#23365,#23366,#23367,#23368,#23369,#23370,#23371,#23372,#23373,#23374,
#23375,#23376),(#23377,#23378,#23379,#23380,#23381,#23382,#23383,#23384,
#23385,#23386,#23387,#23388,#23389,#23390,#23391,#23392,#23393,#23394,#23395,
#23396,#23397,#23398,#23399,#23400,#23401,#23402,#23403,#23404,#23405,#23406,
#23407,#23408,#23409,#23410),(#23411,#23412,#23413,#23414,#23415,#23416,
#23417,#23418,#23419,#23420,#23421,#23422,#23423,#23424,#23425,#23426,#23427,
#23428,#23429,#23430,#23431,#23432,#23433,#23434,#23435,#23436,#23437,#23438,
#23439,#23440,#23441,#23442,#23443,#23444),(#23445,#23446,#23447,#23448,
#23449,#23450,#23451,#23452,#23453,#23454,#23455,#23456,#23457,#23458,#23459,
#23460,#23461,#23462,#23463,#23464,#23465,#23466,#23467,#23468,#23469,#23470,
#23471,#23472,#23473,#23474,#23475,#23476,#23477,#23478),(#23479,#23480,
#23481,#23482,#23483,#23484,#23485,#23486,#23487,#23488,#23489,#23490,#23491,
#23492,#23493,#23494,#23495,#23496,#23497,#23498,#23499,#23500,#23501,#23502,
#23503,#23504,#23505,#23506,#23507,#23508,#23509,#23510,#23511,#23512),
(#23513,#23514,#23515,#23516,#23517,#23518,#23519,#23520,#23521,#23522,
#23523,#23524,#23525,#23526,#23527,#23528,#23529,#23530,#23531,#23532,#23533,
#23534,#23535,#23536,#23537,#23538,#23539,#23540,#23541,#23542,#23543,#23544,
#23545,#23546),(#23547,#23548,#23549,#23550,#23551,#23552,#23553,#23554,
#23555,#23556,#23557,#23558,#23559,#23560,#23561,#23562,#23563,#23564,#23565,
#23566,#23567,#23568,#23569,#23570,#23571,#23572,#23573,#23574,#23575,#23576,
#23577,#23578,#23579,#23580),(#23581,#23582,#23583,#23584,#23585,#23586,
#23587,#23588,#23589,#23590,#23591,#23592,#23593,#23594,#23595,#23596,#23597,
#23598,#23599,#23600,#23601,#23602,#23603,#23604,#23605,#23606,#23607,#23608,
#23609,#23610,#23611,#23612,#23613,#23614),(#23615,#23616,#23617,#23618,
#23619,#23620,#23621,#23622,#23623,#23624,#23625,#23626,#23627,#23628,#23629,
#23630,#23631,#23632,#23633,#23634,#23635,#23636,#23637,#23638,#23639,#23640,
#23641,#23642,#23643,#23644,#23645,#23646,#23647,#23648),(#23649,#23650,
#23651,#23652,#23653,#23654,#23655,#23656,#23657,#23658,#23659,#23660,#23661,
#23662,#23663,#23664,#23665,#23666,#23667,#23668,#23669,#23670,#23671,#23672,
#23673,#23674,#23675,#23676,#23677,#23678,#23679,#23680,#23681,#23682),
(#23683,#23684,#23685,#23686,#23687,#23688,#23689,#23690,#23691,#23692,
#23693,#23694,#23695,#23696,#23697,#23698,#23699,#23700,#23701,#23702,#23703,
#23704,#23705,#23706,#23707,#23708,#23709,#23710,#23711,#23712,#23713,#23714,
#23715,#23716),(#23717,#23718,#23719,#23720,#23721,#23722,#23723,#23724,
#23725,#23726,#23727,#23728,#23729,#23730,#23731,#23732,#23733,#23734,#23735,
#23736,#23737,#23738,#23739,#23740,#23741,#23742,#23743,#23744,#23745,#23746,
#23747,#23748,#23749,#23750),(#23751,#23752,#23753,#23754,#23755,#23756,
#23757,#23758,#23759,#23760,#23761,#23762,#23763,#23764,#23765,#23766,#23767,
#23768,#23769,#23770,#23771,#23772,#23773,#23774,#23775,#23776,#23777,#23778,
#23779,#23780,#23781,#23782,#23783,#23784)),.UNSPECIFIED.,.F.,.F.,.F.,(4,
2,2,2,2,2,2,4),(4,2,2,2,2,2,2,2,2,2,2,2,2,2,2,2,4),(-0.00300004903652835,
0.,0.1,0.2,0.3,0.4,0.5,0.50300004884616),(-0.00600030454937093,0.0450000000000826,
0.110000000000075,0.175000000000067,0.240000000000059,0.305000000000052,
0.370000000000045,0.435000000000037,0.500000000000029,0.565000000000022,
0.630000000000014,0.695,0.76,0.824999999999991,0.889999999999984,0.954999999999976,
1.00600015484898),.UNSPECIFIED.);
#47=B_SPLINE_SURFACE_WITH_KNOTS('',3,3,((#23792,#23793,#23794,#23795,#23796,
#23797,#23798,#23799,#23800,#23801,#23802,#23803,#23804,#23805,#23806,#23807,
#23808,#23809,#23810,#23811,#23812,#23813,#23814,#23815,#23816,#23817,#23818,
#23819,#23820,#23821,#23822,#23823,#23824,#23825),(#23826,#23827,#23828,
#23829,#23830,#23831,#23832,#23833,#23834,#23835,#23836,#23837,#23838,#23839,
#23840,#23841,#23842,#23843,#23844,#23845,#23846,#23847,#23848,#23849,#23850,
#23851,#23852,#23853,#23854,#23855,#23856,#23857,#23858,#23859),(#23860,
#23861,#23862,#23863,#23864,#23865,#23866,#23867,#23868,#23869,#23870,#23871,
#23872,#23873,#23874,#23875,#23876,#23877,#23878,#23879,#23880,#23881,#23882,
#23883,#23884,#23885,#23886,#23887,#23888,#23889,#23890,#23891,#23892,#23893),
(#23894,#23895,#23896,#23897,#23898,#23899,#23900,#23901,#23902,#23903,
#23904,#23905,#23906,#23907,#23908,#23909,#23910,#23911,#23912,#23913,#23914,
#23915,#23916,#23917,#23918,#23919,#23920,#23921,#23922,#23923,#23924,#23925,
#23926,#23927),(#23928,#23929,#23930,#23931,#23932,#23933,#23934,#23935,
#23936,#23937,#23938,#23939,#23940,#23941,#23942,#23943,#23944,#23945,#23946,
#23947,#23948,#23949,#23950,#23951,#23952,#23953,#23954,#23955,#23956,#23957,
#23958,#23959,#23960,#23961),(#23962,#23963,#23964,#23965,#23966,#23967,
#23968,#23969,#23970,#23971,#23972,#23973,#23974,#23975,#23976,#23977,#23978,
#23979,#23980,#23981,#23982,#23983,#23984,#23985,#23986,#23987,#23988,#23989,
#23990,#23991,#23992,#23993,#23994,#23995),(#23996,#23997,#23998,#23999,
#24000,#24001,#24002,#24003,#24004,#24005,#24006,#24007,#24008,#24009,#24010,
#24011,#24012,#24013,#24014,#24015,#24016,#24017,#24018,#24019,#24020,#24021,
#24022,#24023,#24024,#24025,#24026,#24027,#24028,#24029),(#24030,#24031,
#24032,#24033,#24034,#24035,#24036,#24037,#24038,#24039,#24040,#24041,#24042,
#24043,#24044,#24045,#24046,#24047,#24048,#24049,#24050,#24051,#24052,#24053,
#24054,#24055,#24056,#24057,#24058,#24059,#24060,#24061,#24062,#24063),
(#24064,#24065,#24066,#24067,#24068,#24069,#24070,#24071,#24072,#24073,
#24074,#24075,#24076,#24077,#24078,#24079,#24080,#24081,#24082,#24083,#24084,
#24085,#24086,#24087,#24088,#24089,#24090,#24091,#24092,#24093,#24094,#24095,
#24096,#24097),(#24098,#24099,#24100,#24101,#24102,#24103,#24104,#24105,
#24106,#24107,#24108,#24109,#24110,#24111,#24112,#24113,#24114,#24115,#24116,
#24117,#24118,#24119,#24120,#24121,#24122,#24123,#24124,#24125,#24126,#24127,
#24128,#24129,#24130,#24131),(#24132,#24133,#24134,#24135,#24136,#24137,
#24138,#24139,#24140,#24141,#24142,#24143,#24144,#24145,#24146,#24147,#24148,
#24149,#24150,#24151,#24152,#24153,#24154,#24155,#24156,#24157,#24158,#24159,
#24160,#24161,#24162,#24163,#24164,#24165),(#24166,#24167,#24168,#24169,
#24170,#24171,#24172,#24173,#24174,#24175,#24176,#24177,#24178,#24179,#24180,
#24181,#24182,#24183,#24184,#24185,#24186,#24187,#24188,#24189,#24190,#24191,
#24192,#24193,#24194,#24195,#24196,#24197,#24198,#24199),(#24200,#24201,
#24202,#24203,#24204,#24205,#24206,#24207,#24208,#24209,#24210,#24211,#24212,
#24213,#24214,#24215,#24216,#24217,#24218,#24219,#24220,#24221,#24222,#24223,
#24224,#24225,#24226,#24227,#24228,#24229,#24230,#24231,#24232,#24233),
(#24234,#24235,#24236,#24237,#24238,#24239,#24240,#24241,#24242,#24243,
#24244,#24245,#24246,#24247,#24248,#24249,#24250,#24251,#24252,#24253,#24254,
#24255,#24256,#24257,#24258,#24259,#24260,#24261,#24262,#24263,#24264,#24265,
#24266,#24267),(#24268,#24269,#24270,#24271,#24272,#24273,#24274,#24275,
#24276,#24277,#24278,#24279,#24280,#24281,#24282,#24283,#24284,#24285,#24286,
#24287,#24288,#24289,#24290,#24291,#24292,#24293,#24294,#24295,#24296,#24297,
#24298,#24299,#24300,#24301),(#24302,#24303,#24304,#24305,#24306,#24307,
#24308,#24309,#24310,#24311,#24312,#24313,#24314,#24315,#24316,#24317,#24318,
#24319,#24320,#24321,#24322,#24323,#24324,#24325,#24326,#24327,#24328,#24329,
#24330,#24331,#24332,#24333,#24334,#24335)),.UNSPECIFIED.,.F.,.F.,.F.,(4,
2,2,2,2,2,2,4),(4,2,2,2,2,2,2,2,2,2,2,2,2,2,2,2,4),(0.48765503023554,0.5,
0.6,0.7,0.8,0.9,1.,1.01234496976446),(9.7389676693069,10.1395200046188,
10.5400723399307,10.9406246752427,11.3411770105546,11.7417293458665,12.1422816811784,
12.5428340164903,12.9433863518023,13.3439386871142,13.7444910224261,14.145043357738,
14.5455956930499,14.9461480283619,15.3467003636738,15.7472526989857,16.1478050342977),
 .UNSPECIFIED.);
#48=B_SPLINE_SURFACE_WITH_KNOTS('',3,3,((#24367,#24368,#24369,#24370,#24371,
#24372,#24373,#24374,#24375,#24376,#24377,#24378,#24379,#24380,#24381,#24382,
#24383,#24384,#24385,#24386,#24387,#24388,#24389,#24390,#24391,#24392,#24393,
#24394,#24395,#24396,#24397,#24398,#24399,#24400),(#24401,#24402,#24403,
#24404,#24405,#24406,#24407,#24408,#24409,#24410,#24411,#24412,#24413,#24414,
#24415,#24416,#24417,#24418,#24419,#24420,#24421,#24422,#24423,#24424,#24425,
#24426,#24427,#24428,#24429,#24430,#24431,#24432,#24433,#24434),(#24435,
#24436,#24437,#24438,#24439,#24440,#24441,#24442,#24443,#24444,#24445,#24446,
#24447,#24448,#24449,#24450,#24451,#24452,#24453,#24454,#24455,#24456,#24457,
#24458,#24459,#24460,#24461,#24462,#24463,#24464,#24465,#24466,#24467,#24468),
(#24469,#24470,#24471,#24472,#24473,#24474,#24475,#24476,#24477,#24478,
#24479,#24480,#24481,#24482,#24483,#24484,#24485,#24486,#24487,#24488,#24489,
#24490,#24491,#24492,#24493,#24494,#24495,#24496,#24497,#24498,#24499,#24500,
#24501,#24502),(#24503,#24504,#24505,#24506,#24507,#24508,#24509,#24510,
#24511,#24512,#24513,#24514,#24515,#24516,#24517,#24518,#24519,#24520,#24521,
#24522,#24523,#24524,#24525,#24526,#24527,#24528,#24529,#24530,#24531,#24532,
#24533,#24534,#24535,#24536),(#24537,#24538,#24539,#24540,#24541,#24542,
#24543,#24544,#24545,#24546,#24547,#24548,#24549,#24550,#24551,#24552,#24553,
#24554,#24555,#24556,#24557,#24558,#24559,#24560,#24561,#24562,#24563,#24564,
#24565,#24566,#24567,#24568,#24569,#24570),(#24571,#24572,#24573,#24574,
#24575,#24576,#24577,#24578,#24579,#24580,#24581,#24582,#24583,#24584,#24585,
#24586,#24587,#24588,#24589,#24590,#24591,#24592,#24593,#24594,#24595,#24596,
#24597,#24598,#24599,#24600,#24601,#24602,#24603,#24604),(#24605,#24606,
#24607,#24608,#24609,#24610,#24611,#24612,#24613,#24614,#24615,#24616,#24617,
#24618,#24619,#24620,#24621,#24622,#24623,#24624,#24625,#24626,#24627,#24628,
#24629,#24630,#24631,#24632,#24633,#24634,#24635,#24636,#24637,#24638),
(#24639,#24640,#24641,#24642,#24643,#24644,#24645,#24646,#24647,#24648,
#24649,#24650,#24651,#24652,#24653,#24654,#24655,#24656,#24657,#24658,#24659,
#24660,#24661,#24662,#24663,#24664,#24665,#24666,#24667,#24668,#24669,#24670,
#24671,#24672),(#24673,#24674,#24675,#24676,#24677,#24678,#24679,#24680,
#24681,#24682,#24683,#24684,#24685,#24686,#24687,#24688,#24689,#24690,#24691,
#24692,#24693,#24694,#24695,#24696,#24697,#24698,#24699,#24700,#24701,#24702,
#24703,#24704,#24705,#24706),(#24707,#24708,#24709,#24710,#24711,#24712,
#24713,#24714,#24715,#24716,#24717,#24718,#24719,#24720,#24721,#24722,#24723,
#24724,#24725,#24726,#24727,#24728,#24729,#24730,#24731,#24732,#24733,#24734,
#24735,#24736,#24737,#24738,#24739,#24740),(#24741,#24742,#24743,#24744,
#24745,#24746,#24747,#24748,#24749,#24750,#24751,#24752,#24753,#24754,#24755,
#24756,#24757,#24758,#24759,#24760,#24761,#24762,#24763,#24764,#24765,#24766,
#24767,#24768,#24769,#24770,#24771,#24772,#24773,#24774),(#24775,#24776,
#24777,#24778,#24779,#24780,#24781,#24782,#24783,#24784,#24785,#24786,#24787,
#24788,#24789,#24790,#24791,#24792,#24793,#24794,#24795,#24796,#24797,#24798,
#24799,#24800,#24801,#24802,#24803,#24804,#24805,#24806,#24807,#24808),
(#24809,#24810,#24811,#24812,#24813,#24814,#24815,#24816,#24817,#24818,
#24819,#24820,#24821,#24822,#24823,#24824,#24825,#24826,#24827,#24828,#24829,
#24830,#24831,#24832,#24833,#24834,#24835,#24836,#24837,#24838,#24839,#24840,
#24841,#24842)),.UNSPECIFIED.,.F.,.F.,.F.,(4,2,2,2,2,2,4),(4,2,2,2,2,2,
2,2,2,2,2,2,2,2,2,2,4),(0.496998870686259,0.5,0.625,0.75,0.875,1.,1.0030011270394),
(-0.00600170187786821,0.045,0.11,0.175,0.24,0.305,0.37,0.435,0.5,0.565,
0.63,0.695,0.76,0.825,0.89,0.955,1.00600177391382),.UNSPECIFIED.);
#49=B_SPLINE_SURFACE_WITH_KNOTS('',3,3,((#24890,#24891,#24892,#24893,#24894,
#24895,#24896,#24897,#24898,#24899,#24900,#24901,#24902,#24903,#24904,#24905,
#24906,#24907,#24908,#24909,#24910,#24911,#24912,#24913,#24914,#24915,#24916,
#24917,#24918,#24919,#24920,#24921,#24922,#24923),(#24924,#24925,#24926,
#24927,#24928,#24929,#24930,#24931,#24932,#24933,#24934,#24935,#24936,#24937,
#24938,#24939,#24940,#24941,#24942,#24943,#24944,#24945,#24946,#24947,#24948,
#24949,#24950,#24951,#24952,#24953,#24954,#24955,#24956,#24957),(#24958,
#24959,#24960,#24961,#24962,#24963,#24964,#24965,#24966,#24967,#24968,#24969,
#24970,#24971,#24972,#24973,#24974,#24975,#24976,#24977,#24978,#24979,#24980,
#24981,#24982,#24983,#24984,#24985,#24986,#24987,#24988,#24989,#24990,#24991),
(#24992,#24993,#24994,#24995,#24996,#24997,#24998,#24999,#25000,#25001,
#25002,#25003,#25004,#25005,#25006,#25007,#25008,#25009,#25010,#25011,#25012,
#25013,#25014,#25015,#25016,#25017,#25018,#25019,#25020,#25021,#25022,#25023,
#25024,#25025),(#25026,#25027,#25028,#25029,#25030,#25031,#25032,#25033,
#25034,#25035,#25036,#25037,#25038,#25039,#25040,#25041,#25042,#25043,#25044,
#25045,#25046,#25047,#25048,#25049,#25050,#25051,#25052,#25053,#25054,#25055,
#25056,#25057,#25058,#25059),(#25060,#25061,#25062,#25063,#25064,#25065,
#25066,#25067,#25068,#25069,#25070,#25071,#25072,#25073,#25074,#25075,#25076,
#25077,#25078,#25079,#25080,#25081,#25082,#25083,#25084,#25085,#25086,#25087,
#25088,#25089,#25090,#25091,#25092,#25093),(#25094,#25095,#25096,#25097,
#25098,#25099,#25100,#25101,#25102,#25103,#25104,#25105,#25106,#25107,#25108,
#25109,#25110,#25111,#25112,#25113,#25114,#25115,#25116,#25117,#25118,#25119,
#25120,#25121,#25122,#25123,#25124,#25125,#25126,#25127),(#25128,#25129,
#25130,#25131,#25132,#25133,#25134,#25135,#25136,#25137,#25138,#25139,#25140,
#25141,#25142,#25143,#25144,#25145,#25146,#25147,#25148,#25149,#25150,#25151,
#25152,#25153,#25154,#25155,#25156,#25157,#25158,#25159,#25160,#25161),
(#25162,#25163,#25164,#25165,#25166,#25167,#25168,#25169,#25170,#25171,
#25172,#25173,#25174,#25175,#25176,#25177,#25178,#25179,#25180,#25181,#25182,
#25183,#25184,#25185,#25186,#25187,#25188,#25189,#25190,#25191,#25192,#25193,
#25194,#25195),(#25196,#25197,#25198,#25199,#25200,#25201,#25202,#25203,
#25204,#25205,#25206,#25207,#25208,#25209,#25210,#25211,#25212,#25213,#25214,
#25215,#25216,#25217,#25218,#25219,#25220,#25221,#25222,#25223,#25224,#25225,
#25226,#25227,#25228,#25229),(#25230,#25231,#25232,#25233,#25234,#25235,
#25236,#25237,#25238,#25239,#25240,#25241,#25242,#25243,#25244,#25245,#25246,
#25247,#25248,#25249,#25250,#25251,#25252,#25253,#25254,#25255,#25256,#25257,
#25258,#25259,#25260,#25261,#25262,#25263),(#25264,#25265,#25266,#25267,
#25268,#25269,#25270,#25271,#25272,#25273,#25274,#25275,#25276,#25277,#25278,
#25279,#25280,#25281,#25282,#25283,#25284,#25285,#25286,#25287,#25288,#25289,
#25290,#25291,#25292,#25293,#25294,#25295,#25296,#25297),(#25298,#25299,
#25300,#25301,#25302,#25303,#25304,#25305,#25306,#25307,#25308,#25309,#25310,
#25311,#25312,#25313,#25314,#25315,#25316,#25317,#25318,#25319,#25320,#25321,
#25322,#25323,#25324,#25325,#25326,#25327,#25328,#25329,#25330,#25331),
(#25332,#25333,#25334,#25335,#25336,#25337,#25338,#25339,#25340,#25341,
#25342,#25343,#25344,#25345,#25346,#25347,#25348,#25349,#25350,#25351,#25352,
#25353,#25354,#25355,#25356,#25357,#25358,#25359,#25360,#25361,#25362,#25363,
#25364,#25365)),.UNSPECIFIED.,.F.,.F.,.F.,(4,2,2,2,2,2,4),(4,2,2,2,2,2,
2,2,2,2,2,2,2,2,2,2,4),(-0.0030068551580675,0.,0.125,0.25,0.375,0.5,0.503006855154615),
(-0.00600170280327224,0.045,0.11,0.175,0.24,0.305,0.37,0.435,0.5,0.565,
0.63,0.695,0.76,0.825,0.89,0.955,1.00000190754036),.UNSPECIFIED.);
#50=B_SPLINE_SURFACE_WITH_KNOTS('',3,3,((#25373,#25374,#25375,#25376,#25377,
#25378,#25379,#25380,#25381,#25382,#25383,#25384,#25385,#25386,#25387,#25388,
#25389,#25390,#25391,#25392,#25393,#25394,#25395,#25396,#25397,#25398,#25399,
#25400,#25401,#25402,#25403,#25404,#25405,#25406),(#25407,#25408,#25409,
#25410,#25411,#25412,#25413,#25414,#25415,#25416,#25417,#25418,#25419,#25420,
#25421,#25422,#25423,#25424,#25425,#25426,#25427,#25428,#25429,#25430,#25431,
#25432,#25433,#25434,#25435,#25436,#25437,#25438,#25439,#25440),(#25441,
#25442,#25443,#25444,#25445,#25446,#25447,#25448,#25449,#25450,#25451,#25452,
#25453,#25454,#25455,#25456,#25457,#25458,#25459,#25460,#25461,#25462,#25463,
#25464,#25465,#25466,#25467,#25468,#25469,#25470,#25471,#25472,#25473,#25474),
(#25475,#25476,#25477,#25478,#25479,#25480,#25481,#25482,#25483,#25484,
#25485,#25486,#25487,#25488,#25489,#25490,#25491,#25492,#25493,#25494,#25495,
#25496,#25497,#25498,#25499,#25500,#25501,#25502,#25503,#25504,#25505,#25506,
#25507,#25508),(#25509,#25510,#25511,#25512,#25513,#25514,#25515,#25516,
#25517,#25518,#25519,#25520,#25521,#25522,#25523,#25524,#25525,#25526,#25527,
#25528,#25529,#25530,#25531,#25532,#25533,#25534,#25535,#25536,#25537,#25538,
#25539,#25540,#25541,#25542),(#25543,#25544,#25545,#25546,#25547,#25548,
#25549,#25550,#25551,#25552,#25553,#25554,#25555,#25556,#25557,#25558,#25559,
#25560,#25561,#25562,#25563,#25564,#25565,#25566,#25567,#25568,#25569,#25570,
#25571,#25572,#25573,#25574,#25575,#25576),(#25577,#25578,#25579,#25580,
#25581,#25582,#25583,#25584,#25585,#25586,#25587,#25588,#25589,#25590,#25591,
#25592,#25593,#25594,#25595,#25596,#25597,#25598,#25599,#25600,#25601,#25602,
#25603,#25604,#25605,#25606,#25607,#25608,#25609,#25610),(#25611,#25612,
#25613,#25614,#25615,#25616,#25617,#25618,#25619,#25620,#25621,#25622,#25623,
#25624,#25625,#25626,#25627,#25628,#25629,#25630,#25631,#25632,#25633,#25634,
#25635,#25636,#25637,#25638,#25639,#25640,#25641,#25642,#25643,#25644),
(#25645,#25646,#25647,#25648,#25649,#25650,#25651,#25652,#25653,#25654,
#25655,#25656,#25657,#25658,#25659,#25660,#25661,#25662,#25663,#25664,#25665,
#25666,#25667,#25668,#25669,#25670,#25671,#25672,#25673,#25674,#25675,#25676,
#25677,#25678),(#25679,#25680,#25681,#25682,#25683,#25684,#25685,#25686,
#25687,#25688,#25689,#25690,#25691,#25692,#25693,#25694,#25695,#25696,#25697,
#25698,#25699,#25700,#25701,#25702,#25703,#25704,#25705,#25706,#25707,#25708,
#25709,#25710,#25711,#25712),(#25713,#25714,#25715,#25716,#25717,#25718,
#25719,#25720,#25721,#25722,#25723,#25724,#25725,#25726,#25727,#25728,#25729,
#25730,#25731,#25732,#25733,#25734,#25735,#25736,#25737,#25738,#25739,#25740,
#25741,#25742,#25743,#25744,#25745,#25746),(#25747,#25748,#25749,#25750,
#25751,#25752,#25753,#25754,#25755,#25756,#25757,#25758,#25759,#25760,#25761,
#25762,#25763,#25764,#25765,#25766,#25767,#25768,#25769,#25770,#25771,#25772,
#25773,#25774,#25775,#25776,#25777,#25778,#25779,#25780),(#25781,#25782,
#25783,#25784,#25785,#25786,#25787,#25788,#25789,#25790,#25791,#25792,#25793,
#25794,#25795,#25796,#25797,#25798,#25799,#25800,#25801,#25802,#25803,#25804,
#25805,#25806,#25807,#25808,#25809,#25810,#25811,#25812,#25813,#25814),
(#25815,#25816,#25817,#25818,#25819,#25820,#25821,#25822,#25823,#25824,
#25825,#25826,#25827,#25828,#25829,#25830,#25831,#25832,#25833,#25834,#25835,
#25836,#25837,#25838,#25839,#25840,#25841,#25842,#25843,#25844,#25845,#25846,
#25847,#25848),(#25849,#25850,#25851,#25852,#25853,#25854,#25855,#25856,
#25857,#25858,#25859,#25860,#25861,#25862,#25863,#25864,#25865,#25866,#25867,
#25868,#25869,#25870,#25871,#25872,#25873,#25874,#25875,#25876,#25877,#25878,
#25879,#25880,#25881,#25882),(#25883,#25884,#25885,#25886,#25887,#25888,
#25889,#25890,#25891,#25892,#25893,#25894,#25895,#25896,#25897,#25898,#25899,
#25900,#25901,#25902,#25903,#25904,#25905,#25906,#25907,#25908,#25909,#25910,
#25911,#25912,#25913,#25914,#25915,#25916)),.UNSPECIFIED.,.F.,.F.,.F.,(4,
2,2,2,2,2,2,4),(4,2,2,2,2,2,2,2,2,2,2,2,2,2,2,2,4),(-0.0123449697644626,
0.,0.1,0.2,0.3,0.4,0.5,0.512344969764463),(9.7389676693069,10.1395200046188,
10.5400723399307,10.9406246752427,11.3411770105546,11.7417293458665,12.1422816811784,
12.5428340164903,12.9433863518023,13.3439386871142,13.7444910224261,14.145043357738,
14.5455956930499,14.9461480283619,15.3467003636738,15.7472526989857,16.1478050342977),
 .UNSPECIFIED.);
#51=B_SPLINE_SURFACE_WITH_KNOTS('',3,3,((#25924,#25925,#25926,#25927,#25928,
#25929,#25930,#25931,#25932,#25933,#25934,#25935,#25936,#25937,#25938,#25939,
#25940,#25941,#25942,#25943,#25944,#25945,#25946,#25947,#25948,#25949,#25950,
#25951,#25952,#25953,#25954,#25955,#25956,#25957),(#25958,#25959,#25960,
#25961,#25962,#25963,#25964,#25965,#25966,#25967,#25968,#25969,#25970,#25971,
#25972,#25973,#25974,#25975,#25976,#25977,#25978,#25979,#25980,#25981,#25982,
#25983,#25984,#25985,#25986,#25987,#25988,#25989,#25990,#25991),(#25992,
#25993,#25994,#25995,#25996,#25997,#25998,#25999,#26000,#26001,#26002,#26003,
#26004,#26005,#26006,#26007,#26008,#26009,#26010,#26011,#26012,#26013,#26014,
#26015,#26016,#26017,#26018,#26019,#26020,#26021,#26022,#26023,#26024,#26025),
(#26026,#26027,#26028,#26029,#26030,#26031,#26032,#26033,#26034,#26035,
#26036,#26037,#26038,#26039,#26040,#26041,#26042,#26043,#26044,#26045,#26046,
#26047,#26048,#26049,#26050,#26051,#26052,#26053,#26054,#26055,#26056,#26057,
#26058,#26059),(#26060,#26061,#26062,#26063,#26064,#26065,#26066,#26067,
#26068,#26069,#26070,#26071,#26072,#26073,#26074,#26075,#26076,#26077,#26078,
#26079,#26080,#26081,#26082,#26083,#26084,#26085,#26086,#26087,#26088,#26089,
#26090,#26091,#26092,#26093),(#26094,#26095,#26096,#26097,#26098,#26099,
#26100,#26101,#26102,#26103,#26104,#26105,#26106,#26107,#26108,#26109,#26110,
#26111,#26112,#26113,#26114,#26115,#26116,#26117,#26118,#26119,#26120,#26121,
#26122,#26123,#26124,#26125,#26126,#26127),(#26128,#26129,#26130,#26131,
#26132,#26133,#26134,#26135,#26136,#26137,#26138,#26139,#26140,#26141,#26142,
#26143,#26144,#26145,#26146,#26147,#26148,#26149,#26150,#26151,#26152,#26153,
#26154,#26155,#26156,#26157,#26158,#26159,#26160,#26161),(#26162,#26163,
#26164,#26165,#26166,#26167,#26168,#26169,#26170,#26171,#26172,#26173,#26174,
#26175,#26176,#26177,#26178,#26179,#26180,#26181,#26182,#26183,#26184,#26185,
#26186,#26187,#26188,#26189,#26190,#26191,#26192,#26193,#26194,#26195),
(#26196,#26197,#26198,#26199,#26200,#26201,#26202,#26203,#26204,#26205,
#26206,#26207,#26208,#26209,#26210,#26211,#26212,#26213,#26214,#26215,#26216,
#26217,#26218,#26219,#26220,#26221,#26222,#26223,#26224,#26225,#26226,#26227,
#26228,#26229),(#26230,#26231,#26232,#26233,#26234,#26235,#26236,#26237,
#26238,#26239,#26240,#26241,#26242,#26243,#26244,#26245,#26246,#26247,#26248,
#26249,#26250,#26251,#26252,#26253,#26254,#26255,#26256,#26257,#26258,#26259,
#26260,#26261,#26262,#26263),(#26264,#26265,#26266,#26267,#26268,#26269,
#26270,#26271,#26272,#26273,#26274,#26275,#26276,#26277,#26278,#26279,#26280,
#26281,#26282,#26283,#26284,#26285,#26286,#26287,#26288,#26289,#26290,#26291,
#26292,#26293,#26294,#26295,#26296,#26297),(#26298,#26299,#26300,#26301,
#26302,#26303,#26304,#26305,#26306,#26307,#26308,#26309,#26310,#26311,#26312,
#26313,#26314,#26315,#26316,#26317,#26318,#26319,#26320,#26321,#26322,#26323,
#26324,#26325,#26326,#26327,#26328,#26329,#26330,#26331),(#26332,#26333,
#26334,#26335,#26336,#26337,#26338,#26339,#26340,#26341,#26342,#26343,#26344,
#26345,#26346,#26347,#26348,#26349,#26350,#26351,#26352,#26353,#26354,#26355,
#26356,#26357,#26358,#26359,#26360,#26361,#26362,#26363,#26364,#26365),
(#26366,#26367,#26368,#26369,#26370,#26371,#26372,#26373,#26374,#26375,
#26376,#26377,#26378,#26379,#26380,#26381,#26382,#26383,#26384,#26385,#26386,
#26387,#26388,#26389,#26390,#26391,#26392,#26393,#26394,#26395,#26396,#26397,
#26398,#26399),(#26400,#26401,#26402,#26403,#26404,#26405,#26406,#26407,
#26408,#26409,#26410,#26411,#26412,#26413,#26414,#26415,#26416,#26417,#26418,
#26419,#26420,#26421,#26422,#26423,#26424,#26425,#26426,#26427,#26428,#26429,
#26430,#26431,#26432,#26433),(#26434,#26435,#26436,#26437,#26438,#26439,
#26440,#26441,#26442,#26443,#26444,#26445,#26446,#26447,#26448,#26449,#26450,
#26451,#26452,#26453,#26454,#26455,#26456,#26457,#26458,#26459,#26460,#26461,
#26462,#26463,#26464,#26465,#26466,#26467)),.UNSPECIFIED.,.F.,.F.,.F.,(4,
2,2,2,2,2,2,4),(4,2,2,2,2,2,2,2,2,2,2,2,2,2,2,2,4),(0.496997718705871,0.5000000000048,
0.6,0.7,0.8,0.9,0.999999999995041,1.00300228129556),(-0.00600176935748849,
0.0449995022183333,0.109999536098761,0.174999569979189,0.239999603859616,
0.304999637740044,0.369999671620471,0.434999705500899,0.499999739381326,
0.564999773261754,0.629999807142181,0.694999841022609,0.759999874903037,
0.824999908783464,0.889999942663892,0.954999976544319,1.0000018983327),
 .UNSPECIFIED.);
#52=B_SPLINE_SURFACE_WITH_KNOTS('',3,3,((#26506,#26507,#26508,#26509,#26510,
#26511,#26512,#26513,#26514,#26515,#26516,#26517,#26518,#26519,#26520,#26521,
#26522,#26523,#26524,#26525,#26526,#26527,#26528,#26529,#26530,#26531,#26532,
#26533,#26534,#26535,#26536,#26537,#26538,#26539),(#26540,#26541,#26542,
#26543,#26544,#26545,#26546,#26547,#26548,#26549,#26550,#26551,#26552,#26553,
#26554,#26555,#26556,#26557,#26558,#26559,#26560,#26561,#26562,#26563,#26564,
#26565,#26566,#26567,#26568,#26569,#26570,#26571,#26572,#26573),(#26574,
#26575,#26576,#26577,#26578,#26579,#26580,#26581,#26582,#26583,#26584,#26585,
#26586,#26587,#26588,#26589,#26590,#26591,#26592,#26593,#26594,#26595,#26596,
#26597,#26598,#26599,#26600,#26601,#26602,#26603,#26604,#26605,#26606,#26607),
(#26608,#26609,#26610,#26611,#26612,#26613,#26614,#26615,#26616,#26617,
#26618,#26619,#26620,#26621,#26622,#26623,#26624,#26625,#26626,#26627,#26628,
#26629,#26630,#26631,#26632,#26633,#26634,#26635,#26636,#26637,#26638,#26639,
#26640,#26641),(#26642,#26643,#26644,#26645,#26646,#26647,#26648,#26649,
#26650,#26651,#26652,#26653,#26654,#26655,#26656,#26657,#26658,#26659,#26660,
#26661,#26662,#26663,#26664,#26665,#26666,#26667,#26668,#26669,#26670,#26671,
#26672,#26673,#26674,#26675),(#26676,#26677,#26678,#26679,#26680,#26681,
#26682,#26683,#26684,#26685,#26686,#26687,#26688,#26689,#26690,#26691,#26692,
#26693,#26694,#26695,#26696,#26697,#26698,#26699,#26700,#26701,#26702,#26703,
#26704,#26705,#26706,#26707,#26708,#26709),(#26710,#26711,#26712,#26713,
#26714,#26715,#26716,#26717,#26718,#26719,#26720,#26721,#26722,#26723,#26724,
#26725,#26726,#26727,#26728,#26729,#26730,#26731,#26732,#26733,#26734,#26735,
#26736,#26737,#26738,#26739,#26740,#26741,#26742,#26743),(#26744,#26745,
#26746,#26747,#26748,#26749,#26750,#26751,#26752,#26753,#26754,#26755,#26756,
#26757,#26758,#26759,#26760,#26761,#26762,#26763,#26764,#26765,#26766,#26767,
#26768,#26769,#26770,#26771,#26772,#26773,#26774,#26775,#26776,#26777),
(#26778,#26779,#26780,#26781,#26782,#26783,#26784,#26785,#26786,#26787,
#26788,#26789,#26790,#26791,#26792,#26793,#26794,#26795,#26796,#26797,#26798,
#26799,#26800,#26801,#26802,#26803,#26804,#26805,#26806,#26807,#26808,#26809,
#26810,#26811),(#26812,#26813,#26814,#26815,#26816,#26817,#26818,#26819,
#26820,#26821,#26822,#26823,#26824,#26825,#26826,#26827,#26828,#26829,#26830,
#26831,#26832,#26833,#26834,#26835,#26836,#26837,#26838,#26839,#26840,#26841,
#26842,#26843,#26844,#26845),(#26846,#26847,#26848,#26849,#26850,#26851,
#26852,#26853,#26854,#26855,#26856,#26857,#26858,#26859,#26860,#26861,#26862,
#26863,#26864,#26865,#26866,#26867,#26868,#26869,#26870,#26871,#26872,#26873,
#26874,#26875,#26876,#26877,#26878,#26879),(#26880,#26881,#26882,#26883,
#26884,#26885,#26886,#26887,#26888,#26889,#26890,#26891,#26892,#26893,#26894,
#26895,#26896,#26897,#26898,#26899,#26900,#26901,#26902,#26903,#26904,#26905,
#26906,#26907,#26908,#26909,#26910,#26911,#26912,#26913),(#26914,#26915,
#26916,#26917,#26918,#26919,#26920,#26921,#26922,#26923,#26924,#26925,#26926,
#26927,#26928,#26929,#26930,#26931,#26932,#26933,#26934,#26935,#26936,#26937,
#26938,#26939,#26940,#26941,#26942,#26943,#26944,#26945,#26946,#26947),
(#26948,#26949,#26950,#26951,#26952,#26953,#26954,#26955,#26956,#26957,
#26958,#26959,#26960,#26961,#26962,#26963,#26964,#26965,#26966,#26967,#26968,
#26969,#26970,#26971,#26972,#26973,#26974,#26975,#26976,#26977,#26978,#26979,
#26980,#26981),(#26982,#26983,#26984,#26985,#26986,#26987,#26988,#26989,
#26990,#26991,#26992,#26993,#26994,#26995,#26996,#26997,#26998,#26999,#27000,
#27001,#27002,#27003,#27004,#27005,#27006,#27007,#27008,#27009,#27010,#27011,
#27012,#27013,#27014,#27015),(#27016,#27017,#27018,#27019,#27020,#27021,
#27022,#27023,#27024,#27025,#27026,#27027,#27028,#27029,#27030,#27031,#27032,
#27033,#27034,#27035,#27036,#27037,#27038,#27039,#27040,#27041,#27042,#27043,
#27044,#27045,#27046,#27047,#27048,#27049)),.UNSPECIFIED.,.F.,.F.,.F.,(4,
2,2,2,2,2,2,4),(4,2,2,2,2,2,2,2,2,2,2,2,2,2,2,2,4),(-0.00300112884876056,
0.,0.1,0.2,0.3,0.4,0.500000000011615,0.503001344659739),(-0.00600176891874219,
0.0449987955440709,0.109998877522747,0.174998959501422,0.239999041480098,
0.304999123458774,0.36999920543745,0.434999287416126,0.499999369394802,
0.564999451373477,0.629999533352153,0.694999615330829,0.759999697309505,
0.824999779288181,0.889999861266856,0.954999943245532,1.00600178762734),
 .UNSPECIFIED.);
#61=COLOUR_RGB('', 0.31764706, 0.68627451, 0.89019608);
#203=SHAPE_REPRESENTATION_RELATIONSHIP('','',#13777,#230);
#230=ADVANCED_BREP_SHAPE_REPRESENTATION('',(#13721),#45467);
#1066=B_SPLINE_CURVE_WITH_KNOTS('',3,(#20463,#20464,#20465,#20466,#20467,
#20468,#20469,#20470,#20471,#20472,#20473,#20474,#20475,#20476,#20477,#20478,
#20479,#20480,#20481,#20482,#20483,#20484,#20485,#20486,#20487,#20488,#20489,
#20490,#20491,#20492,#20493,#20494,#20495,#20496,#20497,#20498,#20499,#20500,
#20501,#20502,#20503,#20504,#20505,#20506,#20507,#20508,#20509,#20510,#20511,
#20512,#20513,#20514,#20515,#20516,#20517,#20518,#20519,#20520,#20521,#20522,
#20523,#20524,#20525,#20526,#20527,#20528,#20529,#20530,#20531,#20532,#20533,
#20534,#20535,#20536,#20537,#20538,#20539,#20540,#20541,#20542,#20543,#20544,
#20545,#20546,#20547,#20548,#20549,#20550,#20551,#20552,#20553,#20554,#20555,
#20556,#20557,#20558,#20559,#20560,#20561,#20562),.UNSPECIFIED.,.F.,.F.,
(4,1,1,1,1,1,1,1,1,1,1,1,1,1,1,1,1,1,1,1,1,1,1,1,1,1,1,1,1,1,1,1,1,1,1,
1,1,1,1,1,1,1,1,1,1,1,1,1,1,1,1,1,1,1,1,1,1,1,1,1,1,1,1,1,1,1,1,1,1,1,1,
1,1,1,1,1,1,1,1,1,1,1,1,1,1,1,1,1,1,1,1,1,1,1,1,1,1,4),(0.,0.015625,0.0234375,
0.03125,0.0390625,0.046875,0.0546875,0.0625,0.0703125,0.078125,0.0859375,
0.09375,0.1015625,0.109375,0.125,0.140625,0.1484375,0.15234375,0.15625,
0.16015625,0.1640625,0.171875,0.1796875,0.1875,0.203125,0.21875,0.234375,
0.2421875,0.25,0.2578125,0.265625,0.28125,0.296875,0.3125,0.328125,0.34375,
0.359375,0.3671875,0.37109375,0.375,0.37890625,0.3828125,0.390625,0.40625,
0.421875,0.4296875,0.4375,0.453125,0.46875,0.484375,0.5,0.515625,0.53125,
0.546875,0.5546875,0.5625,0.5703125,0.578125,0.59375,0.609375,0.6171875,
0.625,0.6328125,0.640625,0.65625,0.671875,0.6796875,0.6875,0.6953125,0.703125,
0.71875,0.734375,0.7421875,0.75,0.7578125,0.765625,0.7734375,0.78125,0.7890625,
0.796875,0.8046875,0.8125,0.8203125,0.828125,0.84375,0.859375,0.8671875,
0.875,0.8828125,0.890625,0.90625,0.921875,0.9375,0.953125,0.96875,0.9765625,
0.984375,1.),.UNSPECIFIED.);
#1067=B_SPLINE_CURVE_WITH_KNOTS('',3,(#20564,#20565,#20566,#20567,#20568,
#20569,#20570),.UNSPECIFIED.,.F.,.F.,(4,1,1,1,4),(5.29374964685745E-18,
0.000466110391549299,0.000932220783098593,0.00139833117464789,0.00186444156619718),
 .UNSPECIFIED.);
#1068=B_SPLINE_CURVE_WITH_KNOTS('',3,(#20575,#20576,#20577,#20578,#20579,
#20580,#20581),.UNSPECIFIED.,.F.,.F.,(4,1,1,1,4),(0.,0.00046618153144794,
0.00093236306289588,0.00139854459434382,0.00186472612579176),
 .UNSPECIFIED.);
#1069=B_SPLINE_CURVE_WITH_KNOTS('',3,(#21058,#21059,#21060,#21061,#21062,
#21063,#21064),.UNSPECIFIED.,.F.,.F.,(4,1,1,1,4),(0.,0.25,0.5,0.75,1.),
 .UNSPECIFIED.);
#1070=B_SPLINE_CURVE_WITH_KNOTS('',3,(#21067,#21068,#21069,#21070,#21071,
#21072,#21073,#21074,#21075,#21076,#21077),.UNSPECIFIED.,.F.,.F.,(4,1,1,
1,1,1,1,1,4),(0.,0.125,0.25,0.375,0.5,0.625,0.75,0.875,1.),
 .UNSPECIFIED.);
#1071=B_SPLINE_CURVE_WITH_KNOTS('',3,(#21078,#21079,#21080,#21081,#21082,
#21083,#21084,#21085,#21086,#21087,#21088),.UNSPECIFIED.,.F.,.F.,(4,1,1,
1,1,1,1,1,4),(0.,0.125,0.25,0.375,0.5,0.625,0.75,0.875,1.),
 .UNSPECIFIED.);
#1072=B_SPLINE_CURVE_WITH_KNOTS('',3,(#21565,#21566,#21567,#21568,#21569,
#21570,#21571),.UNSPECIFIED.,.F.,.F.,(4,1,1,1,4),(0.,0.25,0.5,0.75,1.),
 .UNSPECIFIED.);
#1073=B_SPLINE_CURVE_WITH_KNOTS('',3,(#21573,#21574,#21575,#21576,#21577,
#21578,#21579,#21580,#21581,#21582,#21583,#21584,#21585,#21586,#21587,#21588,
#21589,#21590,#21591,#21592,#21593,#21594,#21595,#21596,#21597,#21598,#21599,
#21600,#21601,#21602,#21603,#21604,#21605,#21606,#21607,#21608,#21609,#21610,
#21611,#21612,#21613,#21614,#21615,#21616,#21617,#21618,#21619,#21620,#21621,
#21622,#21623,#21624,#21625,#21626,#21627,#21628,#21629,#21630,#21631,#21632,
#21633,#21634,#21635,#21636,#21637,#21638,#21639,#21640,#21641,#21642,#21643,
#21644,#21645,#21646,#21647,#21648,#21649,#21650,#21651,#21652,#21653,#21654,
#21655,#21656,#21657,#21658,#21659,#21660,#21661,#21662,#21663,#21664,#21665,
#21666,#21667,#21668,#21669,#21670,#21671,#21672,#21673,#21674,#21675),
 .UNSPECIFIED.,.F.,.F.,(4,1,1,1,1,1,1,1,1,1,1,1,1,1,1,1,1,1,1,1,1,1,1,1,
1,1,1,1,1,1,1,1,1,1,1,1,1,1,1,1,1,1,1,1,1,1,1,1,1,1,1,1,1,1,1,1,1,1,1,1,
1,1,1,1,1,1,1,1,1,1,1,1,1,1,1,1,1,1,1,1,1,1,1,1,1,1,1,1,1,1,1,1,1,1,1,1,
1,1,1,1,4),(0.,0.015625,0.0234375,0.03125,0.0390625,0.046875,0.0546875,
0.0625,0.0703125,0.078125,0.0859375,0.09375,0.1015625,0.109375,0.125,0.140625,
0.1484375,0.15234375,0.15625,0.16015625,0.1640625,0.171875,0.1796875,0.1875,
0.203125,0.21875,0.234375,0.25,0.265625,0.28125,0.296875,0.3046875,0.3125,
0.3203125,0.328125,0.34375,0.359375,0.3671875,0.37109375,0.375,0.37890625,
0.3828125,0.390625,0.40625,0.421875,0.4296875,0.4375,0.4453125,0.453125,
0.4609375,0.46875,0.4765625,0.484375,0.5,0.515625,0.53125,0.546875,0.5546875,
0.5625,0.5703125,0.578125,0.59375,0.609375,0.6171875,0.625,0.6328125,0.640625,
0.65625,0.671875,0.6796875,0.6875,0.6953125,0.703125,0.71875,0.734375,0.7421875,
0.75,0.7578125,0.765625,0.7734375,0.78125,0.7890625,0.796875,0.8046875,
0.8125,0.8203125,0.828125,0.84375,0.859375,0.8671875,0.875,0.8828125,0.890625,
0.90625,0.921875,0.9375,0.953125,0.96875,0.9765625,0.984375,1.),
 .UNSPECIFIED.);
#1074=B_SPLINE_CURVE_WITH_KNOTS('',3,(#22220,#22221,#22222,#22223,#22224,
#22225,#22226),.UNSPECIFIED.,.F.,.F.,(4,1,1,1,4),(0.,0.25,0.5,0.75,1.),
 .UNSPECIFIED.);
#1075=B_SPLINE_CURVE_WITH_KNOTS('',3,(#22229,#22230,#22231,#22232,#22233,
#22234,#22235,#22236,#22237,#22238,#22239),.UNSPECIFIED.,.F.,.F.,(4,1,1,
1,1,1,1,1,4),(0.,0.125,0.25,0.375,0.5,0.625,0.75,0.875,1.),
 .UNSPECIFIED.);
#1076=B_SPLINE_CURVE_WITH_KNOTS('',3,(#22240,#22241,#22242,#22243,#22244,
#22245,#22246,#22247,#22248,#22249,#22250),.UNSPECIFIED.,.F.,.F.,(4,1,1,
1,1,1,1,1,4),(0.,0.125,0.25,0.375,0.5,0.625,0.75,0.875,1.),
 .UNSPECIFIED.);
#1077=B_SPLINE_CURVE_WITH_KNOTS('',3,(#22727,#22728,#22729,#22730,#22731,
#22732,#22733,#22734,#22735,#22736,#22737),.UNSPECIFIED.,.F.,.F.,(4,1,1,
1,1,1,1,1,4),(0.,0.125,0.25,0.375,0.5,0.625,0.75,0.875,1.),
 .UNSPECIFIED.);
#1078=B_SPLINE_CURVE_WITH_KNOTS('',3,(#22739,#22740,#22741,#22742,#22743,
#22744,#22745),.UNSPECIFIED.,.F.,.F.,(4,1,1,1,4),(0.,0.25,0.5,0.75,1.),
 .UNSPECIFIED.);
#1079=B_SPLINE_CURVE_WITH_KNOTS('',3,(#22747,#22748,#22749,#22750,#22751,
#22752,#22753,#22754,#22755,#22756,#22757),.UNSPECIFIED.,.F.,.F.,(4,1,1,
1,1,1,1,1,4),(0.,0.125,0.25,0.375,0.5,0.625,0.75,0.875,1.),
 .UNSPECIFIED.);
#1080=B_SPLINE_CURVE_WITH_KNOTS('',3,(#23234,#23235,#23236,#23237,#23238,
#23239,#23240),.UNSPECIFIED.,.F.,.F.,(4,1,1,1,4),(0.,0.25,0.5,0.75,1.),
 .UNSPECIFIED.);
#1081=B_SPLINE_CURVE_WITH_KNOTS('',3,(#23785,#23786,#23787,#23788,#23789,
#23790,#23791),.UNSPECIFIED.,.F.,.F.,(4,1,1,1,4),(0.,0.25,0.5,0.75,1.),
 .UNSPECIFIED.);
#1082=B_SPLINE_CURVE_WITH_KNOTS('',3,(#24336,#24337,#24338,#24339,#24340,
#24341,#24342,#24343,#24344,#24345,#24346),.UNSPECIFIED.,.F.,.F.,(4,1,1,
1,1,1,1,1,4),(0.,0.125,0.25,0.375,0.5,0.625,0.75,0.875,1.),
 .UNSPECIFIED.);
#1083=B_SPLINE_CURVE_WITH_KNOTS('',3,(#24348,#24349,#24350,#24351,#24352,
#24353,#24354),.UNSPECIFIED.,.F.,.F.,(4,1,1,1,4),(0.,0.25,0.5,0.75,1.),
 .UNSPECIFIED.);
#1084=B_SPLINE_CURVE_WITH_KNOTS('',3,(#24356,#24357,#24358,#24359,#24360,
#24361,#24362,#24363,#24364,#24365,#24366),.UNSPECIFIED.,.F.,.F.,(4,1,1,
1,1,1,1,1,4),(0.,0.125,0.25,0.375,0.5,0.625,0.75,0.875,1.),
 .UNSPECIFIED.);
#1085=B_SPLINE_CURVE_WITH_KNOTS('',3,(#24843,#24844,#24845,#24846,#24847,
#24848,#24849,#24850,#24851,#24852,#24853,#24854,#24855,#24856,#24857,#24858,
#24859,#24860,#24861),.UNSPECIFIED.,.F.,.F.,(4,1,1,1,1,1,1,1,1,1,1,1,1,
1,1,1,4),(0.,0.0625,0.125,0.1875,0.25,0.3125,0.375,0.4375,0.5,0.5625,0.625,
0.6875,0.75,0.8125,0.875,0.9375,1.),.UNSPECIFIED.);
#1086=B_SPLINE_CURVE_WITH_KNOTS('',3,(#24863,#24864,#24865,#24866,#24867,
#24868,#24869,#24870,#24871,#24872,#24873,#24874,#24875,#24876,#24877,#24878,
#24879,#24880,#24881),.UNSPECIFIED.,.F.,.F.,(4,1,1,1,1,1,1,1,1,1,1,1,1,
1,1,1,4),(0.,0.0625,0.125,0.1875,0.25,0.3125,0.375,0.4375,0.5,0.5625,0.625,
0.6875,0.75,0.8125,0.875,0.9375,1.),.UNSPECIFIED.);
#1087=B_SPLINE_CURVE_WITH_KNOTS('',3,(#24883,#24884,#24885,#24886,#24887,
#24888,#24889),.UNSPECIFIED.,.F.,.F.,(4,1,1,1,4),(0.,0.25,0.5,0.75,1.),
 .UNSPECIFIED.);
#1088=B_SPLINE_CURVE_WITH_KNOTS('',3,(#25366,#25367,#25368,#25369,#25370,
#25371,#25372),.UNSPECIFIED.,.F.,.F.,(4,1,1,1,4),(0.,0.25,0.5,0.75,1.),
 .UNSPECIFIED.);
#1089=B_SPLINE_CURVE_WITH_KNOTS('',3,(#25917,#25918,#25919,#25920,#25921,
#25922,#25923),.UNSPECIFIED.,.F.,.F.,(4,1,1,1,4),(0.,0.25,0.5,0.75,1.),
 .UNSPECIFIED.);
#1090=B_SPLINE_CURVE_WITH_KNOTS('',3,(#26468,#26469,#26470,#26471,#26472,
#26473,#26474,#26475,#26476,#26477,#26478,#26479,#26480,#26481,#26482,#26483,
#26484,#26485,#26486),.UNSPECIFIED.,.F.,.F.,(4,1,1,1,1,1,1,1,1,1,1,1,1,
1,1,1,4),(0.,0.0625,0.125,0.1875,0.25,0.3125,0.375,0.4375,0.5,0.5625,0.625,
0.6875,0.75,0.8125,0.875,0.9375,1.),.UNSPECIFIED.);
#1091=B_SPLINE_CURVE_WITH_KNOTS('',3,(#26487,#26488,#26489,#26490,#26491,
#26492,#26493,#26494,#26495,#26496,#26497,#26498,#26499,#26500,#26501,#26502,
#26503,#26504,#26505),.UNSPECIFIED.,.F.,.F.,(4,1,1,1,1,1,1,1,1,1,1,1,1,
1,1,1,4),(0.,0.0625,0.125,0.1875,0.25,0.3125,0.375,0.4375,0.5,0.5625,0.625,
0.6875,0.75,0.8125,0.875,0.9375,1.),.UNSPECIFIED.);
#1233=PLANE('',#13986);
#1234=PLANE('',#13987);
#1235=PLANE('',#13988);
#1236=PLANE('',#13989);
#2296=ORIENTED_EDGE('',*,*,#5795,.T.);
#2297=ORIENTED_EDGE('',*,*,#5796,.F.);
#2298=ORIENTED_EDGE('',*,*,#5795,.F.);
#2299=ORIENTED_EDGE('',*,*,#5797,.T.);
#2300=ORIENTED_EDGE('',*,*,#5798,.F.);
#2301=ORIENTED_EDGE('',*,*,#5799,.T.);
#2302=ORIENTED_EDGE('',*,*,#5800,.F.);
#2303=ORIENTED_EDGE('',*,*,#5801,.T.);
#2304=ORIENTED_EDGE('',*,*,#5796,.T.);
#2305=ORIENTED_EDGE('',*,*,#5802,.T.);
#2306=ORIENTED_EDGE('',*,*,#5803,.F.);
#2307=ORIENTED_EDGE('',*,*,#5802,.F.);
#2308=ORIENTED_EDGE('',*,*,#5797,.F.);
#2309=ORIENTED_EDGE('',*,*,#5801,.F.);
#2310=ORIENTED_EDGE('',*,*,#5798,.T.);
#2311=ORIENTED_EDGE('',*,*,#5804,.F.);
#2312=ORIENTED_EDGE('',*,*,#5805,.F.);
#2313=ORIENTED_EDGE('',*,*,#5806,.F.);
#2314=ORIENTED_EDGE('',*,*,#5799,.F.);
#2315=ORIENTED_EDGE('',*,*,#5807,.F.);
#2316=ORIENTED_EDGE('',*,*,#5800,.T.);
#2317=ORIENTED_EDGE('',*,*,#5808,.F.);
#2318=ORIENTED_EDGE('',*,*,#5809,.F.);
#2319=ORIENTED_EDGE('',*,*,#5810,.F.);
#2320=ORIENTED_EDGE('',*,*,#5803,.T.);
#2321=ORIENTED_EDGE('',*,*,#5810,.T.);
#2322=ORIENTED_EDGE('',*,*,#5811,.F.);
#2323=ORIENTED_EDGE('',*,*,#5808,.T.);
#2324=ORIENTED_EDGE('',*,*,#5812,.F.);
#2325=ORIENTED_EDGE('',*,*,#5807,.T.);
#2326=ORIENTED_EDGE('',*,*,#5804,.T.);
#2327=ORIENTED_EDGE('',*,*,#5806,.T.);
#2328=ORIENTED_EDGE('',*,*,#5805,.T.);
#2329=ORIENTED_EDGE('',*,*,#5813,.T.);
#2330=ORIENTED_EDGE('',*,*,#5814,.F.);
#2331=ORIENTED_EDGE('',*,*,#5815,.T.);
#2332=ORIENTED_EDGE('',*,*,#5816,.T.);
#2333=ORIENTED_EDGE('',*,*,#5809,.T.);
#2334=ORIENTED_EDGE('',*,*,#5817,.T.);
#2335=ORIENTED_EDGE('',*,*,#5818,.F.);
#2336=ORIENTED_EDGE('',*,*,#5816,.F.);
#2337=ORIENTED_EDGE('',*,*,#5819,.F.);
#2338=ORIENTED_EDGE('',*,*,#5817,.F.);
#2339=ORIENTED_EDGE('',*,*,#5811,.T.);
#2340=ORIENTED_EDGE('',*,*,#5812,.T.);
#2341=ORIENTED_EDGE('',*,*,#5815,.F.);
#2342=ORIENTED_EDGE('',*,*,#5820,.F.);
#2343=ORIENTED_EDGE('',*,*,#5813,.F.);
#2344=ORIENTED_EDGE('',*,*,#5821,.F.);
#2345=ORIENTED_EDGE('',*,*,#5818,.T.);
#2346=ORIENTED_EDGE('',*,*,#5822,.F.);
#2347=ORIENTED_EDGE('',*,*,#5814,.T.);
#2348=ORIENTED_EDGE('',*,*,#5821,.T.);
#2349=ORIENTED_EDGE('',*,*,#5820,.T.);
#2350=ORIENTED_EDGE('',*,*,#5822,.T.);
#2351=ORIENTED_EDGE('',*,*,#5819,.T.);
#5795=EDGE_CURVE('',#7603,#7604,#8815,.T.);
#5796=EDGE_CURVE('',#7603,#7604,#1066,.F.);
#5797=EDGE_CURVE('',#7603,#7604,#1067,.T.);
#5798=EDGE_CURVE('',#7605,#7606,#8816,.T.);
#5799=EDGE_CURVE('',#7605,#7606,#1068,.T.);
#5800=EDGE_CURVE('',#7607,#7608,#1069,.F.);
#5801=EDGE_CURVE('',#7607,#7603,#1070,.T.);
#5802=EDGE_CURVE('',#7604,#7608,#1071,.T.);
#5803=EDGE_CURVE('',#7608,#7607,#1072,.F.);
#5804=EDGE_CURVE('',#7605,#7606,#1073,.F.);
#5805=EDGE_CURVE('',#7609,#7610,#1074,.F.);
#5806=EDGE_CURVE('',#7606,#7609,#1075,.F.);
#5807=EDGE_CURVE('',#7610,#7605,#1076,.F.);
#5808=EDGE_CURVE('',#7611,#7608,#1077,.F.);
#5809=EDGE_CURVE('',#7612,#7611,#1078,.F.);
#5810=EDGE_CURVE('',#7607,#7612,#1079,.F.);
#5811=EDGE_CURVE('',#7611,#7612,#1080,.F.);
#5812=EDGE_CURVE('',#7610,#7609,#1081,.F.);
#5813=EDGE_CURVE('',#7610,#7613,#1082,.T.);
#5814=EDGE_CURVE('',#7614,#7613,#1083,.F.);
#5815=EDGE_CURVE('',#7614,#7609,#1084,.T.);
#5816=EDGE_CURVE('',#7615,#7612,#1085,.T.);
#5817=EDGE_CURVE('',#7611,#7616,#1086,.T.);
#5818=EDGE_CURVE('',#7615,#7616,#1087,.F.);
#5819=EDGE_CURVE('',#7616,#7615,#1088,.F.);
#5820=EDGE_CURVE('',#7613,#7614,#1089,.F.);
#5821=EDGE_CURVE('',#7615,#7613,#1090,.F.);
#5822=EDGE_CURVE('',#7614,#7616,#1091,.F.);
#7603=VERTEX_POINT('',#20461);
#7604=VERTEX_POINT('',#20462);
#7605=VERTEX_POINT('',#20573);
#7606=VERTEX_POINT('',#20574);
#7607=VERTEX_POINT('',#21065);
#7608=VERTEX_POINT('',#21066);
#7609=VERTEX_POINT('',#22227);
#7610=VERTEX_POINT('',#22228);
#7611=VERTEX_POINT('',#22738);
#7612=VERTEX_POINT('',#22746);
#7613=VERTEX_POINT('',#24347);
#7614=VERTEX_POINT('',#24355);
#7615=VERTEX_POINT('',#24862);
#7616=VERTEX_POINT('',#24882);
#8815=LINE('',#20460,#9643);
#8816=LINE('',#20572,#9644);
#9643=VECTOR('',#15707,1.);
#9644=VECTOR('',#15712,1.);
#10613=EDGE_LOOP('',(#2296,#2297));
#10614=EDGE_LOOP('',(#2298,#2299));
#10615=EDGE_LOOP('',(#2300,#2301));
#10616=EDGE_LOOP('',(#2302,#2303,#2304,#2305));
#10617=EDGE_LOOP('',(#2306,#2307,#2308,#2309));
#10618=EDGE_LOOP('',(#2310,#2311));
#10619=EDGE_LOOP('',(#2312,#2313,#2314,#2315));
#10620=EDGE_LOOP('',(#2316,#2317,#2318,#2319));
#10621=EDGE_LOOP('',(#2320,#2321,#2322,#2323));
#10622=EDGE_LOOP('',(#2324,#2325,#2326,#2327));
#10623=EDGE_LOOP('',(#2328,#2329,#2330,#2331));
#10624=EDGE_LOOP('',(#2332,#2333,#2334,#2335));
#10625=EDGE_LOOP('',(#2336,#2337,#2338,#2339));
#10626=EDGE_LOOP('',(#2340,#2341,#2342,#2343));
#10627=EDGE_LOOP('',(#2344,#2345,#2346,#2347));
#10628=EDGE_LOOP('',(#2348,#2349,#2350,#2351));
#11728=FACE_BOUND('',#10613,.T.);
#11729=FACE_BOUND('',#10614,.T.);
#11730=FACE_BOUND('',#10615,.T.);
#11731=FACE_BOUND('',#10616,.T.);
#11732=FACE_BOUND('',#10617,.T.);
#11733=FACE_BOUND('',#10618,.T.);
#11734=FACE_BOUND('',#10619,.T.);
#11735=FACE_BOUND('',#10620,.T.);
#11736=FACE_BOUND('',#10621,.T.);
#11737=FACE_BOUND('',#10622,.T.);
#11738=FACE_BOUND('',#10623,.T.);
#11739=FACE_BOUND('',#10624,.T.);
#11740=FACE_BOUND('',#10625,.T.);
#11741=FACE_BOUND('',#10626,.T.);
#11742=FACE_BOUND('',#10627,.T.);
#11743=FACE_BOUND('',#10628,.T.);
#12799=ADVANCED_FACE('',(#11728),#1233,.F.);
#12800=ADVANCED_FACE('',(#11729),#1234,.T.);
#12801=ADVANCED_FACE('',(#11730),#1235,.T.);
#12802=ADVANCED_FACE('',(#11731),#41,.T.);
#12803=ADVANCED_FACE('',(#11732),#42,.T.);
#12804=ADVANCED_FACE('',(#11733),#1236,.F.);
#12805=ADVANCED_FACE('',(#11734),#43,.T.);
#12806=ADVANCED_FACE('',(#11735),#44,.T.);
#12807=ADVANCED_FACE('',(#11736),#45,.T.);
#12808=ADVANCED_FACE('',(#11737),#46,.T.);
#12809=ADVANCED_FACE('',(#11738),#47,.T.);
#12810=ADVANCED_FACE('',(#11739),#48,.T.);
#12811=ADVANCED_FACE('',(#11740),#49,.T.);
#12812=ADVANCED_FACE('',(#11741),#50,.T.);
#12813=ADVANCED_FACE('',(#11742),#51,.T.);
#12814=ADVANCED_FACE('',(#11743),#52,.T.);
#13504=CLOSED_SHELL('',(#12799,#12800,#12801,#12802,#12803,#12804,#12805,
#12806,#12807,#12808,#12809,#12810,#12811,#12812,#12813,#12814));
#13531=STYLED_ITEM('',(#13558),#13721);
#13558=PRESENTATION_STYLE_ASSIGNMENT((#13585));
#13585=SURFACE_STYLE_USAGE(.BOTH.,#13612);
#13612=SURFACE_SIDE_STYLE('',(#13639));
#13639=SURFACE_STYLE_FILL_AREA(#13666);
#13666=FILL_AREA_STYLE('',(#13693));
#13693=FILL_AREA_STYLE_COLOUR('',#61);
#13721=MANIFOLD_SOLID_BREP('75632s_.prt',#13504);
#13749=SHAPE_DEFINITION_REPRESENTATION(#45528,#13777);
#13777=SHAPE_REPRESENTATION('75632s_.prt',(#13802),#45467);
#13802=AXIS2_PLACEMENT_3D('',#19109,#15295,#15296);
#13986=AXIS2_PLACEMENT_3D('',#20459,#15705,#15706);
#13987=AXIS2_PLACEMENT_3D('',#20563,#15708,#15709);
#13988=AXIS2_PLACEMENT_3D('',#20571,#15710,#15711);
#13989=AXIS2_PLACEMENT_3D('',#21572,#15713,#15714);
#15295=DIRECTION('',(0.,0.,1.));
#15296=DIRECTION('',(1.,0.,0.));
#15705=DIRECTION('',(0.,1.,0.));
#15706=DIRECTION('',(-1.,0.,0.));
#15707=DIRECTION('',(0.929776485888249,0.,0.368124552684684));
#15708=DIRECTION('',(0.368124552684685,0.,-0.929776485888249));
#15709=DIRECTION('',(0.929776485888249,0.,0.368124552684685));
#15710=DIRECTION('',(0.368124552684685,0.,0.929776485888249));
#15711=DIRECTION('',(0.929776485888249,0.,-0.368124552684685));
#15712=DIRECTION('',(0.929776485888249,0.,-0.368124552684684));
#15713=DIRECTION('',(0.,-1.,0.));
#15714=DIRECTION('',(1.,0.,0.));
#19109=CARTESIAN_POINT('',(0.,0.,0.));
#20459=CARTESIAN_POINT('',(0.0081026,-0.0149987,0.00954659375251877));
#20460=CARTESIAN_POINT('',(-0.00697862337013143,-0.0149987,-0.00276303245508544));
#20461=CARTESIAN_POINT('',(-0.00697838813503015,-0.0149986999999202,-0.00276293171953564));
#20462=CARTESIAN_POINT('',(-0.00586855331089345,-0.0149987000001014,-0.00232351824269545));
#20463=CARTESIAN_POINT('',(-0.00586855331089344,-0.0149987,-0.00232351824269545));
#20464=CARTESIAN_POINT('',(-0.00599779136539911,-0.0149987,-0.00199635660720541));
#20465=CARTESIAN_POINT('',(-0.0061497149337953,-0.0149987,-0.0014944673254811));
#20466=CARTESIAN_POINT('',(-0.00626830430592329,-0.0149987,-0.000821050784658449));
#20467=CARTESIAN_POINT('',(-0.00631547536017041,-0.0149987,-0.000277747312869822));
#20468=CARTESIAN_POINT('',(-0.00632000856749698,-0.0149987,0.00015929462411768));
#20469=CARTESIAN_POINT('',(-0.00629375135427824,-0.0149987,0.000623355245044501));
#20470=CARTESIAN_POINT('',(-0.00623620899930142,-0.0149987,0.00106910556953163));
#20471=CARTESIAN_POINT('',(-0.0061375129610423,-0.0149987,0.0015445813003547));
#20472=CARTESIAN_POINT('',(-0.00603763212681053,-0.0149987,0.00190296860679013));
#20473=CARTESIAN_POINT('',(-0.00590739644574497,-0.0149987,0.00228438984678247));
#20474=CARTESIAN_POINT('',(-0.00575937756486985,-0.0149987,0.00264292380533166));
#20475=CARTESIAN_POINT('',(-0.00557245894694935,-0.0149987,0.00302213298449338));
#20476=CARTESIAN_POINT('',(-0.00541853509390254,-0.0149987,0.00329368859104497));
#20477=CARTESIAN_POINT('',(-0.00517827337774273,-0.0149987,0.00367602487863288));
#20478=CARTESIAN_POINT('',(-0.00484358822980369,-0.0149987,0.00412251448769674));
#20479=CARTESIAN_POINT('',(-0.0044755270516579,-0.0149987,0.00452080082599289));
#20480=CARTESIAN_POINT('',(-0.00420113020130818,-0.0149987,0.00477711976686186));
#20481=CARTESIAN_POINT('',(-0.00402782270729364,-0.0149987,0.00492583884298841));
#20482=CARTESIAN_POINT('',(-0.00392453518784697,-0.0149987,0.00501167331557126));
#20483=CARTESIAN_POINT('',(-0.00370431548115027,-0.0149987,0.00518228504503203));
#20484=CARTESIAN_POINT('',(-0.00344389650213363,-0.0149987,0.00536626942805986));
#20485=CARTESIAN_POINT('',(-0.00309226575023302,-0.0149987,0.00558713368776282));
#20486=CARTESIAN_POINT('',(-0.00266255231181167,-0.0149987,0.00581308653683576));
#20487=CARTESIAN_POINT('',(-0.00203864766659636,-0.0149987,0.00607898500594078));
#20488=CARTESIAN_POINT('',(-0.00138277756767913,-0.0149987,0.0062807287260464));
#20489=CARTESIAN_POINT('',(-0.000456382127562958,-0.0149987,0.00643337330921512));
#20490=CARTESIAN_POINT('',(0.00015957483550569,-0.0149987,0.00645053065378608));
#20491=CARTESIAN_POINT('',(0.000677466861402992,-0.0149987,0.00642588067210073));
#20492=CARTESIAN_POINT('',(0.00109099272268039,-0.0149987,0.00637815025448105));
#20493=CARTESIAN_POINT('',(0.00139610309946203,-0.0149987,0.00632631389880589));
#20494=CARTESIAN_POINT('',(0.00183217795033315,-0.0149987,0.00623264988861146));
#20495=CARTESIAN_POINT('',(0.00235498770084253,-0.0149987,0.00607643471891711));
#20496=CARTESIAN_POINT('',(0.00295679228876969,-0.0149987,0.00583342874643564));
#20497=CARTESIAN_POINT('',(0.00357833557139731,-0.0149987,0.00550160366559475));
#20498=CARTESIAN_POINT('',(0.00402830733094401,-0.0149987,0.00520697635216527));
#20499=CARTESIAN_POINT('',(0.00449118687829753,-0.0149987,0.00485208586696231));
#20500=CARTESIAN_POINT('',(0.00484330182310477,-0.0149987,0.00453145167497373));
#20501=CARTESIAN_POINT('',(0.00508460958244847,-0.0149987,0.00428339144142465));
#20502=CARTESIAN_POINT('',(0.00521139975095086,-0.0149987,0.00414577193244223));
#20503=CARTESIAN_POINT('',(0.00532624379513806,-0.0149987,0.00401500546471082));
#20504=CARTESIAN_POINT('',(0.00535761453384072,-0.0149987,0.0039777739014523));
#20505=CARTESIAN_POINT('',(0.0054292549141877,-0.0149987,0.00389240085461715));
#20506=CARTESIAN_POINT('',(0.00554251733739671,-0.0149987,0.00375191503025411));
#20507=CARTESIAN_POINT('',(0.00571509837306046,-0.0149987,0.00352545361202452));
#20508=CARTESIAN_POINT('',(0.00589268626100846,-0.0149987,0.0032739742857001));
#20509=CARTESIAN_POINT('',(0.00603416113007693,-0.0149987,0.00306456557847418));
#20510=CARTESIAN_POINT('',(0.00619405534581928,-0.0149987,0.00281919005005542));
#20511=CARTESIAN_POINT('',(0.00628157614623252,-0.0149987,0.00268140069076854));
#20512=CARTESIAN_POINT('',(0.00636121993813283,-0.0149987,0.00257374771308024));
#20513=CARTESIAN_POINT('',(0.00646897408654251,-0.0149987,0.00258392973544523));
#20514=CARTESIAN_POINT('',(0.00643407102408375,-0.0149987,0.00267920952455317));
#20515=CARTESIAN_POINT('',(0.00638190829137443,-0.0149987,0.00293027097027729));
#20516=CARTESIAN_POINT('',(0.00630182432532361,-0.0149987,0.00316181661572083));
#20517=CARTESIAN_POINT('',(0.00621693397809521,-0.0149987,0.00337277795713077));
#20518=CARTESIAN_POINT('',(0.00613118669110985,-0.0149987,0.00355775221177337));
#20519=CARTESIAN_POINT('',(0.00607475008345043,-0.0149987,0.00367431078349054));
#20520=CARTESIAN_POINT('',(0.00595805328651394,-0.0149987,0.00389628684644505));
#20521=CARTESIAN_POINT('',(0.0058111379186003,-0.0149987,0.00414899740727856));
#20522=CARTESIAN_POINT('',(0.00560145356298951,-0.0149987,0.00446977563568582));
#20523=CARTESIAN_POINT('',(0.00537349142968617,-0.0149987,0.00476906799067895));
#20524=CARTESIAN_POINT('',(0.00516655017896163,-0.0149987,0.00501135781470711));
#20525=CARTESIAN_POINT('',(0.00502907279444013,-0.0149987,0.00516380028597474));
#20526=CARTESIAN_POINT('',(0.00478833180431244,-0.0149987,0.00540951530710551));
#20527=CARTESIAN_POINT('',(0.00448836823269244,-0.0149987,0.00568579113106821));
#20528=CARTESIAN_POINT('',(0.00407816864313292,-0.0149987,0.00601650811311655));
#20529=CARTESIAN_POINT('',(0.00364694800976718,-0.0149987,0.00630338858721496));
#20530=CARTESIAN_POINT('',(0.00327204128829861,-0.0149987,0.00651658046002988));
#20531=CARTESIAN_POINT('',(0.00301183190285494,-0.0149987,0.00665179701590169));
#20532=CARTESIAN_POINT('',(0.00262841659219902,-0.0149987,0.00682726803802908));
#20533=CARTESIAN_POINT('',(0.00214075254818061,-0.0149987,0.00701365129164976));
#20534=CARTESIAN_POINT('',(0.00153382137217885,-0.0149987,0.00719644222076747));
#20535=CARTESIAN_POINT('',(0.000758156059766897,-0.0149987,0.00733307054664956));
#20536=CARTESIAN_POINT('',(0.000157893043096049,-0.0149987,0.0073756635849659));
#20537=CARTESIAN_POINT('',(-0.000275947861242832,-0.0149987,0.00738212320653857));
#20538=CARTESIAN_POINT('',(-0.00080139976413858,-0.0149987,0.00735500387711496));
#20539=CARTESIAN_POINT('',(-0.00129897974408687,-0.0149987,0.00729168926470373));
#20540=CARTESIAN_POINT('',(-0.00179001180637925,-0.0149987,0.00719656643873165));
#20541=CARTESIAN_POINT('',(-0.0023086828513538,-0.0149987,0.00705470345348289));
#20542=CARTESIAN_POINT('',(-0.00269692127236669,-0.0149987,0.00692144102239403));
#20543=CARTESIAN_POINT('',(-0.00310967412185889,-0.0149987,0.00675366172174066));
#20544=CARTESIAN_POINT('',(-0.00349213106262486,-0.0149987,0.00657138531749029));
#20545=CARTESIAN_POINT('',(-0.00390858639104579,-0.0149987,0.00633765016949732));
#20546=CARTESIAN_POINT('',(-0.00415667325880236,-0.0149987,0.00618028307237662));
#20547=CARTESIAN_POINT('',(-0.00452971198711676,-0.0149987,0.00592538388379414));
#20548=CARTESIAN_POINT('',(-0.00495344066841688,-0.0149987,0.00558849047514652));
#20549=CARTESIAN_POINT('',(-0.00534805887266166,-0.0149987,0.00521559800980357));
#20550=CARTESIAN_POINT('',(-0.00565041908749544,-0.0149987,0.00488595952081331));
#20551=CARTESIAN_POINT('',(-0.00584671712296322,-0.0149987,0.00465505029489529));
#20552=CARTESIAN_POINT('',(-0.00611294319695769,-0.0149987,0.00430835586847634));
#20553=CARTESIAN_POINT('',(-0.00641390417825563,-0.0149987,0.00386020440961774));
#20554=CARTESIAN_POINT('',(-0.00673923705289183,-0.0149987,0.00329476077199415));
#20555=CARTESIAN_POINT('',(-0.00711749330497587,-0.0149987,0.00239359665867433));
#20556=CARTESIAN_POINT('',(-0.00735443530757019,-0.0149987,0.00155101673976854));
#20557=CARTESIAN_POINT('',(-0.00750924922811216,-0.0149987,0.000468096518621184));
#20558=CARTESIAN_POINT('',(-0.00751006361744199,-0.0149987,-0.000340745305600475));
#20559=CARTESIAN_POINT('',(-0.00742858049611148,-0.0149987,-0.00111766353747729));
#20560=CARTESIAN_POINT('',(-0.00728899156535579,-0.0149987,-0.00185729201443673));
#20561=CARTESIAN_POINT('',(-0.00711987284693758,-0.0149987,-0.00240489603628845));
#20562=CARTESIAN_POINT('',(-0.00697838813503015,-0.0149987,-0.00276293171953563));
#20563=CARTESIAN_POINT('',(-0.00642363978570473,-0.0149987,-0.00254329890958795));
#20564=CARTESIAN_POINT('',(-0.00697825083808498,-0.0149987000000119,-0.00276288495921407));
#20565=CARTESIAN_POINT('',(-0.00697825074522568,-0.0148409789485013,-0.00276288492244847));
#20566=CARTESIAN_POINT('',(-0.00685793302287164,-0.0145317701099072,-0.00271524776621376));
#20567=CARTESIAN_POINT('',(-0.00642401637047605,-0.0143370055991416,-0.0025434480100466));
#20568=CARTESIAN_POINT('',(-0.00598894144989318,-0.014531011342266,-0.00237118966306239));
#20569=CARTESIAN_POINT('',(-0.00586834301421938,-0.0148410151008114,-0.00232344136456195));
#20570=CARTESIAN_POINT('',(-0.00586834292136777,-0.0149986999999595,-0.0023234413277994));
#20571=CARTESIAN_POINT('',(-0.00642363978570473,0.0149987,0.00254329890958795));
#20572=CARTESIAN_POINT('',(-0.00697862337013143,0.0149987,0.00276303245508544));
#20573=CARTESIAN_POINT('',(-0.00697841856488692,0.0149986999999225,0.00276294376766862));
#20574=CARTESIAN_POINT('',(-0.00586852288100303,0.0149987000001005,0.00232350619462049));
#20575=CARTESIAN_POINT('',(-0.00697825083808499,0.0149987000000326,0.00276288495921407));
#20576=CARTESIAN_POINT('',(-0.0069782507471835,0.0148410138784296,0.00276288492322363));
#20577=CARTESIAN_POINT('',(-0.00685797052311819,0.0145320629891672,0.0027152626136117));
#20578=CARTESIAN_POINT('',(-0.00642393748064774,0.014337247250212,0.00254341677535397));
#20579=CARTESIAN_POINT('',(-0.005988930516056,0.014531353268975,0.00237118533405001));
#20580=CARTESIAN_POINT('',(-0.00586834301229698,0.0148409881450687,0.00232344136380081));
#20581=CARTESIAN_POINT('',(-0.00586834292136777,0.014998699999982,0.00232344132779939));
#20582=CARTESIAN_POINT('',(-0.00595197175455224,-0.0137865115759879,-0.00210067757078177));
#20583=CARTESIAN_POINT('',(-0.00572722807386818,-0.0138068062974582,-0.00273633214012084));
#20584=CARTESIAN_POINT('',(-0.00540062700556022,-0.0138271010189286,-0.00333605257006371));
#20585=CARTESIAN_POINT('',(-0.00446089457736053,-0.0138732614070653,-0.0045475063388789));
#20586=CARTESIAN_POINT('',(-0.00379371989130117,-0.0138991270737317,-0.00511734744676406));
#20587=CARTESIAN_POINT('',(-0.00228794941508494,-0.0139508584070646,-0.005945167953823));
#20588=CARTESIAN_POINT('',(-0.00144935362492807,-0.0139767240737311,-0.00620314735299679));
#20589=CARTESIAN_POINT('',(0.000261328143578779,-0.0140284554070643,-0.00636484946416264));
#20590=CARTESIAN_POINT('',(0.00113341412192876,-0.014054321073731,-0.00626857217615473));
#20591=CARTESIAN_POINT('',(0.00276762342257579,-0.0141060524070644,-0.00573758685231191));
#20592=CARTESIAN_POINT('',(0.00352974674487283,-0.0141319180737312,-0.00530287881647702));
#20593=CARTESIAN_POINT('',(0.00481866923934421,-0.0141836494070648,-0.00416654033650878));
#20594=CARTESIAN_POINT('',(0.00534546841151856,-0.0142095150737316,-0.00346490989237544));
#20595=CARTESIAN_POINT('',(0.0060770888172741,-0.0142612464070653,-0.00191013753954751));
#20596=CARTESIAN_POINT('',(0.00628191005085531,-0.0142871120737322,-0.00105699563085293));
#20597=CARTESIAN_POINT('',(0.00633588343265905,-0.014338843407066,0.000660465495998774));
#20598=CARTESIAN_POINT('',(0.00618503558088158,-0.0143647090737329,0.0015247847141559));
#20599=CARTESIAN_POINT('',(0.00555248386117227,-0.0144164404070667,0.00312242798679427));
#20600=CARTESIAN_POINT('',(0.00507077999324043,-0.0144423060737336,0.00385575204127552));
#20601=CARTESIAN_POINT('',(0.00385575204725291,-0.0144940374070673,0.00507077999924899));
#20602=CARTESIAN_POINT('',(0.00312242796919722,-0.0145199030737342,0.00555248390274121));
#20603=CARTESIAN_POINT('',(0.0015247847317121,-0.0145716344070679,0.00618503553932881));
#20604=CARTESIAN_POINT('',(0.000660465572282654,-0.0145975000737348,0.00633588327242417));
#20605=CARTESIAN_POINT('',(-0.00105699570718024,-0.0146492314070684,0.00628191021108882));
#20606=CARTESIAN_POINT('',(-0.00191013782721369,-0.0146750970737351,0.00607708941665809));
#20607=CARTESIAN_POINT('',(-0.00346490960474784,-0.0147268284070685,0.00534546781211641));
#20608=CARTESIAN_POINT('',(-0.00416653926224855,-0.0147526940737352,0.00481866700200547));
#20609=CARTESIAN_POINT('',(-0.0053028798907647,-0.0148044254070684,0.00352974898218043));
#20610=CARTESIAN_POINT('',(-0.00573759086178014,-0.0148302910737349,0.00276763177246633));
#20611=CARTESIAN_POINT('',(-0.00626856816669886,-0.0148820224070679,0.00113340577200012));
#20612=CARTESIAN_POINT('',(-0.00636483450060213,-0.0149078880737343,0.000261296981248004));
#20613=CARTESIAN_POINT('',(-0.00622057297407274,-0.0149540484021785,-0.00126510394998184));
#20614=CARTESIAN_POINT('',(-0.00604811884979192,-0.0149743430639563,-0.00192585323169751));
#20615=CARTESIAN_POINT('',(-0.00577681582588097,-0.014994637725734,-0.00254307154746529));
#20616=CARTESIAN_POINT('',(-0.00595190184505217,-0.0137902529083118,-0.00210065289705602));
#20617=CARTESIAN_POINT('',(-0.00572716080411827,-0.0138105476297821,-0.00273630000024857));
#20618=CARTESIAN_POINT('',(-0.00540056357193694,-0.0138308423512525,-0.00333601338611308));
#20619=CARTESIAN_POINT('',(-0.00446084218146172,-0.0138770027393892,-0.00454745292567268));
#20620=CARTESIAN_POINT('',(-0.00379367533177166,-0.0139028684060556,-0.00511728734043015));
#20621=CARTESIAN_POINT('',(-0.00228792254173836,-0.0139545997393885,-0.00594509812423768));
#20622=CARTESIAN_POINT('',(-0.00144933660139511,-0.013980465406055,-0.00620307449328773));
#20623=CARTESIAN_POINT('',(0.00026132507412203,-0.0140321967393882,-0.00636477470516471));
#20624=CARTESIAN_POINT('',(0.00113340080929592,-0.0140580624060549,-0.00626849854799165));
#20625=CARTESIAN_POINT('',(0.00276759091516852,-0.0141097937393883,-0.00573751946089189));
#20626=CARTESIAN_POINT('',(0.00352970528586722,-0.0141356594060551,-0.00530281653096521));
#20627=CARTESIAN_POINT('',(0.00481861264116609,-0.0141873907393887,-0.00416649139797816));
#20628=CARTESIAN_POINT('',(0.00534540562576625,-0.0142132564060555,-0.00346486919491779));
#20629=CARTESIAN_POINT('',(0.00607701743819862,-0.0142649877393892,-0.0019101151038294));
#20630=CARTESIAN_POINT('',(0.00628183626603084,-0.0142908534060561,-0.00105698321580138));
#20631=CARTESIAN_POINT('',(0.00633580901388464,-0.0143425847393899,0.000660457738432955));
#20632=CARTESIAN_POINT('',(0.00618496293390622,-0.0143684504060568,0.00152476680463927));
#20633=CARTESIAN_POINT('',(0.00555241864389858,-0.0144201817393906,0.00312239131199329));
#20634=CARTESIAN_POINT('',(0.00507072043386936,-0.0144460474060575,0.00385570675314098));
#20635=CARTESIAN_POINT('',(0.0038557067591183,-0.0144977787393912,0.00507072043987786));
#20636=CARTESIAN_POINT('',(0.00312239129439644,-0.0145236444060581,0.00555241868546704));
#20637=CARTESIAN_POINT('',(0.00152476682219527,-0.0145753757393918,0.00618496289235394));
#20638=CARTESIAN_POINT('',(0.000660457814715938,-0.0146012414060587,0.00633580885365165));
#20639=CARTESIAN_POINT('',(-0.0010569832921278,-0.0146529727393923,0.00628183642626247));
#20640=CARTESIAN_POINT('',(-0.0019101153914922,-0.014678838406059,0.00607701803757557));
#20641=CARTESIAN_POINT('',(-0.00346486890729358,-0.0147305697393924,0.00534540502637115));
#20642=CARTESIAN_POINT('',(-0.00416649032373055,-0.0147564354060591,0.00481861040385363));
#20643=CARTESIAN_POINT('',(-0.00530281760524028,-0.0148081667393923,0.00352970752314855));
#20644=CARTESIAN_POINT('',(-0.00573752347031303,-0.0148340324060588,0.00276759926496099));
#20645=CARTESIAN_POINT('',(-0.00626849453858287,-0.0148857637393918,0.00113339245946536));
#20646=CARTESIAN_POINT('',(-0.00636475974177996,-0.0149116294060582,0.000261293912157276));
#20647=CARTESIAN_POINT('',(-0.00622049990968925,-0.0149577897345023,-0.0012650890905725));
#20648=CARTESIAN_POINT('',(-0.00604804781098619,-0.0149780843962802,-0.00192583061138912));
#20649=CARTESIAN_POINT('',(-0.00577674797369298,-0.0149983790580579,-0.00254304167755531));
#20650=CARTESIAN_POINT('',(-0.00595186676701066,-0.01379399487195,-0.00210064051667888));
#20651=CARTESIAN_POINT('',(-0.00572712705060727,-0.0138142895934203,-0.00273628387363098));
#20652=CARTESIAN_POINT('',(-0.0054005317432546,-0.0138345843148906,-0.00333599372503347));
#20653=CARTESIAN_POINT('',(-0.0044608158911076,-0.0138807447030274,-0.00454742612487075));
#20654=CARTESIAN_POINT('',(-0.00379365297342232,-0.0139066103696938,-0.00511725718126046));
#20655=CARTESIAN_POINT('',(-0.00228790905767159,-0.0139583417030267,-0.00594506308629448));
#20656=CARTESIAN_POINT('',(-0.00144932805960615,-0.0139842073696932,-0.00620303793493879));
#20657=CARTESIAN_POINT('',(0.000261323533980402,-0.0140359387030264,-0.00636473719382177));
#20658=CARTESIAN_POINT('',(0.00113339412950152,-0.0140618043696931,-0.00626846160406045));
#20659=CARTESIAN_POINT('',(0.00276757460413525,-0.0141135357030265,-0.00573748564633126));
#20660=CARTESIAN_POINT('',(0.00352968448324787,-0.0141394013696933,-0.0053027852783634));
#20661=CARTESIAN_POINT('',(0.00481858424226123,-0.0141911327030269,-0.00416646684240551));
#20662=CARTESIAN_POINT('',(0.00534537412216198,-0.0142169983696937,-0.00346484877441547));
#20663=CARTESIAN_POINT('',(0.00607698162277769,-0.0142687297030274,-0.00191010384640302));
#20664=CARTESIAN_POINT('',(0.00628179924349267,-0.0142945953696943,-0.00105697698638059));
#20665=CARTESIAN_POINT('',(0.00633577167325347,-0.0143463267030281,0.000660453845968905));
#20666=CARTESIAN_POINT('',(0.0061849264822993,-0.014372192369695,0.00152475781829597));
#20667=CARTESIAN_POINT('',(0.00555238592024542,-0.0144239237030288,0.0031223729099136));
#20668=CARTESIAN_POINT('',(0.00507069054914571,-0.0144497893696957,0.00385568402920415));
#20669=CARTESIAN_POINT('',(0.00385568403518144,-0.0145015207030294,0.00507069055515417));
#20670=CARTESIAN_POINT('',(0.00312237289231686,-0.0145273863696963,0.00555238596181363));
#20671=CARTESIAN_POINT('',(0.00152475783585187,-0.01457911770303,0.00618492644074726));
#20672=CARTESIAN_POINT('',(0.000660453922251439,-0.0146049833696969,0.00633577151302142));
#20673=CARTESIAN_POINT('',(-0.00105697706270655,-0.0146567147030304,0.00628179940372335));
#20674=CARTESIAN_POINT('',(-0.00191010413406412,-0.0146825803696972,0.00607698222215111));
#20675=CARTESIAN_POINT('',(-0.00346484848679295,-0.0147343117030306,0.00534537352277041));
#20676=CARTESIAN_POINT('',(-0.00416646576816423,-0.0147601773696973,0.00481858200496196));
#20677=CARTESIAN_POINT('',(-0.00530278635263214,-0.0148119087030305,0.00352968672051601));
#20678=CARTESIAN_POINT('',(-0.00573748965572877,-0.014837774369697,0.00276758295387851));
#20679=CARTESIAN_POINT('',(-0.00626845759467531,-0.01488950570303,0.00113338577972016));
#20680=CARTESIAN_POINT('',(-0.0063647222305252,-0.0149153713696963,0.000261292372199303));
#20681=CARTESIAN_POINT('',(-0.00622046324864212,-0.0149615316981405,-0.00126508163466197));
#20682=CARTESIAN_POINT('',(-0.00604801216630023,-0.0149818263599183,-0.00192581926134205));
#20683=CARTESIAN_POINT('',(-0.00577671392793577,-0.0150021210216961,-0.00254302668992214));
#20684=CARTESIAN_POINT('',(-0.00595186676701067,-0.013953649428554,-0.00210064051667888));
#20685=CARTESIAN_POINT('',(-0.00572712705060728,-0.0139739441500243,-0.00273628387363098));
#20686=CARTESIAN_POINT('',(-0.00540053174325461,-0.0139942388714947,-0.00333599372503347));
#20687=CARTESIAN_POINT('',(-0.00446081589110761,-0.0140403992596314,-0.00454742612487077));
#20688=CARTESIAN_POINT('',(-0.00379365297342232,-0.0140662649262978,-0.00511725718126046));
#20689=CARTESIAN_POINT('',(-0.00228790905767159,-0.0141179962596307,-0.0059450630862945));
#20690=CARTESIAN_POINT('',(-0.00144932805960615,-0.0141438619262972,-0.0062030379349388));
#20691=CARTESIAN_POINT('',(0.000261323533980404,-0.0141955932596304,-0.00636473719382177));
#20692=CARTESIAN_POINT('',(0.00113339412950152,-0.0142214589262971,-0.00626846160406046));
#20693=CARTESIAN_POINT('',(0.00276757460413525,-0.0142731902596306,-0.00573748564633127));
#20694=CARTESIAN_POINT('',(0.00352968448324787,-0.0142990559262973,-0.00530278527836341));
#20695=CARTESIAN_POINT('',(0.00481858424226123,-0.0143507872596309,-0.00416646684240551));
#20696=CARTESIAN_POINT('',(0.00534537412216198,-0.0143766529262977,-0.00346484877441547));
#20697=CARTESIAN_POINT('',(0.00607698162277769,-0.0144283842596314,-0.00191010384640302));
#20698=CARTESIAN_POINT('',(0.00628179924349267,-0.0144542499262983,-0.00105697698638059));
#20699=CARTESIAN_POINT('',(0.00633577167325347,-0.0145059812596321,0.000660453845968901));
#20700=CARTESIAN_POINT('',(0.0061849264822993,-0.014531846926299,0.00152475781829598));
#20701=CARTESIAN_POINT('',(0.00555238592024542,-0.0145835782596327,0.0031223729099136));
#20702=CARTESIAN_POINT('',(0.00507069054914571,-0.0146094439262997,0.00385568402920416));
#20703=CARTESIAN_POINT('',(0.00385568403518144,-0.0146611752596335,0.00507069055515417));
#20704=CARTESIAN_POINT('',(0.00312237289231686,-0.0146870409263003,0.00555238596181364));
#20705=CARTESIAN_POINT('',(0.00152475783585187,-0.014738772259634,0.00618492644074727));
#20706=CARTESIAN_POINT('',(0.000660453922251436,-0.0147646379263009,0.00633577151302144));
#20707=CARTESIAN_POINT('',(-0.00105697706270656,-0.0148163692596345,0.00628179940372336));
#20708=CARTESIAN_POINT('',(-0.00191010413406411,-0.0148422349263012,0.00607698222215111));
#20709=CARTESIAN_POINT('',(-0.00346484848679295,-0.0148939662596346,0.00534537352277041));
#20710=CARTESIAN_POINT('',(-0.00416646576816423,-0.0149198319263013,0.00481858200496196));
#20711=CARTESIAN_POINT('',(-0.00530278635263215,-0.0149715632596345,0.003529686720516));
#20712=CARTESIAN_POINT('',(-0.00573748965572878,-0.014997428926301,0.00276758295387852));
#20713=CARTESIAN_POINT('',(-0.00626845759467531,-0.015049160259634,0.00113338577972016));
#20714=CARTESIAN_POINT('',(-0.00636472223052521,-0.0150750259263004,0.000261292372199302));
#20715=CARTESIAN_POINT('',(-0.00622046324864213,-0.0151211862547446,-0.00126508163466197));
#20716=CARTESIAN_POINT('',(-0.00604801216630023,-0.0151414809165224,-0.00192581926134205));
#20717=CARTESIAN_POINT('',(-0.00577671392793576,-0.0151617755783002,-0.00254302668992214));
#20718=CARTESIAN_POINT('',(-0.006012764145877,-0.0141095620215199,-0.00212213352154841));
#20719=CARTESIAN_POINT('',(-0.00578572497281708,-0.0141298567429902,-0.00276428055471631));
#20720=CARTESIAN_POINT('',(-0.00545578805871373,-0.0141501514644605,-0.00337012642351642));
#20721=CARTESIAN_POINT('',(-0.00450645736898466,-0.0141963118525973,-0.00459395376778236));
#20722=CARTESIAN_POINT('',(-0.00383246827817517,-0.0142221775192636,-0.00516961513239118));
#20723=CARTESIAN_POINT('',(-0.00231131812748966,-0.0142739088525966,-0.0060058908523253));
#20724=CARTESIAN_POINT('',(-0.00146415706761363,-0.0142997745192631,-0.0062665052076506));
#20725=CARTESIAN_POINT('',(0.000263997303215911,-0.0143515058525963,-0.00642985891570324));
#20726=CARTESIAN_POINT('',(0.00114499061416944,-0.014377371519263,-0.00633259826843059));
#20727=CARTESIAN_POINT('',(0.00279589144081968,-0.0144291028525964,-0.00579618955399959));
#20728=CARTESIAN_POINT('',(0.00356579895651638,-0.0144549685192632,-0.00535704148684126));
#20729=CARTESIAN_POINT('',(0.00486788627835968,-0.0145066998525967,-0.00420909664575432));
#20730=CARTESIAN_POINT('',(0.00540006608450627,-0.0145325655192636,-0.00350029987182573));
#20731=CARTESIAN_POINT('',(0.00613915913224367,-0.0145842968525973,-0.00192964734799031));
#20732=CARTESIAN_POINT('',(0.00634607237383449,-0.0146101625192642,-0.00106779159808349));
#20733=CARTESIAN_POINT('',(0.00640059703025495,-0.0146618938525979,0.000667211374263152));
#20734=CARTESIAN_POINT('',(0.0062482084450846,-0.0146877595192648,0.00154035859670298));
#20735=CARTESIAN_POINT('',(0.00560919595350615,-0.0147394908525986,0.00315431991637398));
#20736=CARTESIAN_POINT('',(0.00512257204709806,-0.0147653565192655,0.00389513401360513));
#20737=CARTESIAN_POINT('',(0.00389513401964358,-0.0148170878525993,0.00512257205316799));
#20738=CARTESIAN_POINT('',(0.0031543198985972,-0.0148429535192662,0.00560919599549967));
#20739=CARTESIAN_POINT('',(0.0015403586144385,-0.0148946848525999,0.00624820840310741));
#20740=CARTESIAN_POINT('',(0.000667211451326186,-0.0149205505192667,0.00640059686838347));
#20741=CARTESIAN_POINT('',(-0.0010677916751904,-0.0149722818526003,0.00634607253570459));
#20742=CARTESIAN_POINT('',(-0.00192964763859466,-0.0149981475192671,0.00613915973774966));
#20743=CARTESIAN_POINT('',(-0.00350029958126036,-0.0150498788526005,0.00540006547898194));
#20744=CARTESIAN_POINT('',(-0.00420909556052178,-0.0150757445192672,0.00486788401816916));
#20745=CARTESIAN_POINT('',(-0.00535704257210152,-0.0151274758526004,0.00356580121667545));
#20746=CARTESIAN_POINT('',(-0.00579619360441983,-0.0151533415192669,0.00279589987599453));
#20747=CARTESIAN_POINT('',(-0.00633259421802285,-0.0152050728525998,0.00114498217895609));
#20748=CARTESIAN_POINT('',(-0.00642984379930755,-0.0152309385192662,0.000263965822598579));
#20749=CARTESIAN_POINT('',(-0.00628410881095147,-0.0152770988477104,-0.00127802549893492));
#20750=CARTESIAN_POINT('',(-0.0061098932706154,-0.0152973935094883,-0.00194552355745231));
#20751=CARTESIAN_POINT('',(-0.00583581920539624,-0.015317688171266,-0.00256904603240167));
#20752=CARTESIAN_POINT('',(-0.00622068080271541,-0.014330055725037,-0.00219551523027012));
#20753=CARTESIAN_POINT('',(-0.0059857907935527,-0.0143503504465073,-0.00285986720297926));
#20754=CARTESIAN_POINT('',(-0.00564444492036105,-0.0143706451679776,-0.0034866627455973));
#20755=CARTESIAN_POINT('',(-0.00466228712175928,-0.0144168055561143,-0.0047528090772364));
#20756=CARTESIAN_POINT('',(-0.00396499201809,-0.0144426712227807,-0.00534837635923974));
#20757=CARTESIAN_POINT('',(-0.00239124169114502,-0.0144944025561137,-0.00621356983607658));
#20758=CARTESIAN_POINT('',(-0.00151478646786931,-0.0145202682227802,-0.00648319603091008));
#20759=CARTESIAN_POINT('',(0.000273126122402447,-0.0145719995561134,-0.00665219838175603));
#20760=CARTESIAN_POINT('',(0.00118458348939849,-0.01459786522278,-0.00655157453776847));
#20761=CARTESIAN_POINT('',(0.00289257116867112,-0.0146495965561135,-0.0059966172317251));
#20762=CARTESIAN_POINT('',(0.0036891014809477,-0.0146754622227802,-0.00554228376966927));
#20763=CARTESIAN_POINT('',(0.00503621395865962,-0.0147271935561138,-0.00435464389850914));
#20764=CARTESIAN_POINT('',(0.00558679612409495,-0.0147530592227806,-0.00362133748940482));
#20765=CARTESIAN_POINT('',(0.00635144642833699,-0.0148047905561144,-0.00199637303616592));
#20766=CARTESIAN_POINT('',(0.0065655145671437,-0.0148306562227812,-0.00110471499203134));
#20767=CARTESIAN_POINT('',(0.00662192464331508,-0.014882387556115,0.000690283019013507));
#20768=CARTESIAN_POINT('',(0.00646426658067974,-0.0149082532227819,0.00159362298592376));
#20769=CARTESIAN_POINT('',(0.00580315753954379,-0.0149599845561157,0.00326339381910821));
#20770=CARTESIAN_POINT('',(0.00529970656104317,-0.0149858502227826,0.00402982468538238));
#20771=CARTESIAN_POINT('',(0.00402982469162964,-0.0150375815561164,0.00529970656732299));
#20772=CARTESIAN_POINT('',(0.00326339380071673,-0.0150634472227833,0.00580315758298941));
#20773=CARTESIAN_POINT('',(0.00159362300427257,-0.015115178556117,0.00646426653725101));
#20774=CARTESIAN_POINT('',(0.000690283098741327,-0.0151410442227838,0.0066219244758462));
#20775=CARTESIAN_POINT('',(-0.00110471507180453,-0.0151927755561174,0.00656551473461114));
#20776=CARTESIAN_POINT('',(-0.00199637333681914,-0.0152186412227842,0.0063514470547809));
#20777=CARTESIAN_POINT('',(-0.00362133718879192,-0.0152703725561176,0.00558679549763207));
#20778=CARTESIAN_POINT('',(-0.0043546427757501,-0.0152962382227842,0.00503621162031348));
#20779=CARTESIAN_POINT('',(-0.00554228489245698,-0.0153479695561175,0.0036891038192613));
#20780=CARTESIAN_POINT('',(-0.00599662142220568,-0.015373835222784,0.0028925798955277));
#20781=CARTESIAN_POINT('',(-0.00655157034730082,-0.0154255665561169,0.00118457476250211));
#20782=CARTESIAN_POINT('',(-0.00665218274264726,-0.0154514322227833,0.000273093553210122));
#20783=CARTESIAN_POINT('',(-0.00650140835297288,-0.0154975925512275,-0.00132221861588513));
#20784=CARTESIAN_POINT('',(-0.00632116857622288,-0.0155178872130053,-0.002012798232469));
#20785=CARTESIAN_POINT('',(-0.0060376172453096,-0.0155381818747831,-0.00265788162437932));
#20786=CARTESIAN_POINT('',(-0.00636770008068748,-0.0143946368355882,-0.00224740393412229));
#20787=CARTESIAN_POINT('',(-0.00612725869207852,-0.0144149315570585,-0.00292745717015689));
#20788=CARTESIAN_POINT('',(-0.00577784546654924,-0.0144352262785288,-0.00356906636919523));
#20789=CARTESIAN_POINT('',(-0.00477247539665684,-0.0144813866666655,-0.00486513674377885));
#20790=CARTESIAN_POINT('',(-0.00405870045325198,-0.0145072523333319,-0.00547477963495758));
#20791=CARTESIAN_POINT('',(-0.00244775618498231,-0.0145589836666649,-0.00636042105379704));
#20792=CARTESIAN_POINT('',(-0.0015505868601175,-0.0145848493333314,-0.00663641958145776));
#20793=CARTESIAN_POINT('',(0.000279581172353473,-0.0146365806666646,-0.00680941612592736));
#20794=CARTESIAN_POINT('',(0.00121257987995963,-0.0146624463333313,-0.00670641414273623));
#20795=CARTESIAN_POINT('',(0.00296093405983815,-0.0147141776666647,-0.00613834100178227));
#20796=CARTESIAN_POINT('',(0.0037762895321105,-0.0147400433333314,-0.00567326984401944));
#20797=CARTESIAN_POINT('',(0.00515523960286111,-0.014791774666665,-0.00445756134791513));
#20798=CARTESIAN_POINT('',(0.00571883420133934,-0.0148176403333318,-0.00370692400957366));
#20799=CARTESIAN_POINT('',(0.00650155621496434,-0.0148693716666656,-0.00204355522275424));
#20800=CARTESIAN_POINT('',(0.0067206836301111,-0.0148952373333324,-0.00113082377427628));
#20801=CARTESIAN_POINT('',(0.00677842689937372,-0.0149469686666662,0.000706597135469611));
#20802=CARTESIAN_POINT('',(0.00661704275348959,-0.0149728343333331,0.00163128659673755));
#20803=CARTESIAN_POINT('',(0.0059403090923207,-0.0150245656666669,0.00334052071538206));
#20804=CARTESIAN_POINT('',(0.00542495957703594,-0.0150504313333339,0.00412506537275865));
#20805=CARTESIAN_POINT('',(0.00412506537915355,-0.0151021626666676,0.00542495958346417));
#20806=CARTESIAN_POINT('',(0.00334052069655592,-0.0151280283333345,0.00594030913679311));
#20807=CARTESIAN_POINT('',(0.00163128661552,-0.0151797596666682,0.00661704270903447));
#20808=CARTESIAN_POINT('',(0.000706597217081717,-0.015205625333335,0.0067784267279469));
#20809=CARTESIAN_POINT('',(-0.00113082385593482,-0.0152573566666687,0.00672068380153646));
#20810=CARTESIAN_POINT('',(-0.00204355553051307,-0.0152832223333354,0.00650155685621359));
#20811=CARTESIAN_POINT('',(-0.00370692370185609,-0.0153349536666688,0.00571883356007067));
#20812=CARTESIAN_POINT('',(-0.00445756019862087,-0.0153608193333355,0.00515523720925061));
#20813=CARTESIAN_POINT('',(-0.00567327099334306,-0.0154125506666686,0.0037762919256877));
#20814=CARTESIAN_POINT('',(-0.00613834529130048,-0.0154384163333352,0.00296094299294485));
#20815=CARTESIAN_POINT('',(-0.00670640985323126,-0.0154901476666682,0.00121257094681219));
#20816=CARTESIAN_POINT('',(-0.00680940011720463,-0.0155160133333345,0.000279547833422385));
#20817=CARTESIAN_POINT('',(-0.00665506233268495,-0.0155621736617787,-0.0013534678685624));
#20818=CARTESIAN_POINT('',(-0.00647056277751519,-0.0155824683235565,-0.00206036861137542));
#20819=CARTESIAN_POINT('',(-0.00618031000776251,-0.0156027629853343,-0.00272069787387743));
#20820=CARTESIAN_POINT('',(-0.00666173863663163,-0.0143946368355882,-0.00235118134182664));
#20821=CARTESIAN_POINT('',(-0.00641019448913015,-0.0144149315570585,-0.00306263710451214));
#20822=CARTESIAN_POINT('',(-0.00604464655892563,-0.0144352262785288,-0.0037338736163911));
#20823=CARTESIAN_POINT('',(-0.00499285194645195,-0.0144813866666655,-0.00508979207686375));
#20824=CARTESIAN_POINT('',(-0.00424611732357595,-0.0145072523333319,-0.00572758618639328));
#20825=CARTESIAN_POINT('',(-0.00256078517265692,-0.0145589836666649,-0.00665412348923796));
#20826=CARTESIAN_POINT('',(-0.00162218764461389,-0.0145848493333314,-0.00694286668255311));
#20827=CARTESIAN_POINT('',(0.000292491272255523,-0.0146365806666646,-0.00712385161427001));
#20828=CARTESIAN_POINT('',(0.00126857266108191,-0.0146624463333313,-0.00701609335267175));
#20829=CARTESIAN_POINT('',(0.00309765984217221,-0.0147141776666647,-0.00642178854189663));
#20830=CARTESIAN_POINT('',(0.00395066563443612,-0.0147400433333314,-0.00593524199271977));
#20831=CARTESIAN_POINT('',(0.00539329089126408,-0.014791774666665,-0.00466339624672713));
#20832=CARTESIAN_POINT('',(0.00598291035582812,-0.0148176403333318,-0.00387809704991134));
#20833=CARTESIAN_POINT('',(0.00680177578821902,-0.0148693716666656,-0.00213791959593085));
#20834=CARTESIAN_POINT('',(0.00703102175604589,-0.0148952373333324,-0.00118304133876616));
#20835=CARTESIAN_POINT('',(0.00709143141149102,-0.0149469686666662,0.000739225368381816));
#20836=CARTESIAN_POINT('',(0.00692259509910929,-0.0149728343333331,0.0017066138183651));
#20837=CARTESIAN_POINT('',(0.00621461219787452,-0.0150245656666669,0.00349477450792978));
#20838=CARTESIAN_POINT('',(0.00567546560902149,-0.0150504313333339,0.00431554674751118));
#20839=CARTESIAN_POINT('',(0.00431554675420138,-0.0151021626666676,0.00567546561574655));
#20840=CARTESIAN_POINT('',(0.00349477448823432,-0.0151280283333345,0.00621461224440051));
#20841=CARTESIAN_POINT('',(0.00170661383801487,-0.0151797596666682,0.00692259505260138));
#20842=CARTESIAN_POINT('',(0.000739225453762495,-0.015205625333335,0.00709143123214829));
#20843=CARTESIAN_POINT('',(-0.00118304142419541,-0.0152573566666687,0.00703102193538709));
#20844=CARTESIAN_POINT('',(-0.00213791991790094,-0.0152832223333354,0.00680177645907897));
#20845=CARTESIAN_POINT('',(-0.00387809672798443,-0.0153349536666688,0.00598290968494786));
#20846=CARTESIAN_POINT('',(-0.00466339504436239,-0.0153608193333355,0.00539328838712486));
#20847=CARTESIAN_POINT('',(-0.00593524319511522,-0.0154125506666686,0.00395066813854051));
#20848=CARTESIAN_POINT('',(-0.00642179302949008,-0.0154384163333352,0.00309766918777915));
#20849=CARTESIAN_POINT('',(-0.00701608886509214,-0.0154901476666682,0.00126856331543235));
#20850=CARTESIAN_POINT('',(-0.00712383486631935,-0.0155160133333345,0.000292456393846915));
#20851=CARTESIAN_POINT('',(-0.00696237029210909,-0.0155621736617787,-0.00141596637391693));
#20852=CARTESIAN_POINT('',(-0.00676935118009981,-0.0155824683235565,-0.00215550936918826));
#20853=CARTESIAN_POINT('',(-0.0064656955326683,-0.0156027629853343,-0.00284633037287366));
#20854=CARTESIAN_POINT('',(-0.0068087579146037,-0.014330055725037,-0.00240307004567882));
#20855=CARTESIAN_POINT('',(-0.00655166238765596,-0.0143503504465073,-0.00313022707168977));
#20856=CARTESIAN_POINT('',(-0.00617804710511382,-0.0143706451679776,-0.00381627723998903));
#20857=CARTESIAN_POINT('',(-0.00510304022134951,-0.0144168055561143,-0.00520211974340619));
#20858=CARTESIAN_POINT('',(-0.00433982575873793,-0.0144426712227807,-0.00585398946211112));
#20859=CARTESIAN_POINT('',(-0.00261729966649421,-0.0144944025561137,-0.00680097470695842));
#20860=CARTESIAN_POINT('',(-0.00165798803686209,-0.0145202682227802,-0.00709609023310079));
#20861=CARTESIAN_POINT('',(0.000298946322206545,-0.0145719995561134,-0.00728106935844133));
#20862=CARTESIAN_POINT('',(0.00129656905164305,-0.01459786522278,-0.00717093295763951));
#20863=CARTESIAN_POINT('',(0.00316602273333924,-0.0146495965561135,-0.00656351231195381));
#20864=CARTESIAN_POINT('',(0.00403785368559892,-0.0146754622227802,-0.00606622806706994));
#20865=CARTESIAN_POINT('',(0.00551231653546556,-0.0147271935561138,-0.00476631369613313));
#20866=CARTESIAN_POINT('',(0.00611494843307251,-0.0147530592227806,-0.00396368357008018));
#20867=CARTESIAN_POINT('',(0.00695188557484637,-0.0148047905561143,-0.00218510178251917));
#20868=CARTESIAN_POINT('',(0.00718619081901328,-0.0148306562227812,-0.0012091501210111));
#20869=CARTESIAN_POINT('',(0.00724793366754967,-0.014882387556115,0.000755539484837918));
#20870=CARTESIAN_POINT('',(0.00707537127191914,-0.0149082532227819,0.00174427742917887));
#20871=CARTESIAN_POINT('',(0.00635176375065143,-0.0149599845561157,0.00357190140420364));
#20872=CARTESIAN_POINT('',(0.00580071862501426,-0.0149858502227826,0.00441078743488745));
#20873=CARTESIAN_POINT('',(0.0044107874417253,-0.0150375815561164,0.00580071863188774));
#20874=CARTESIAN_POINT('',(0.00357190138407352,-0.0150634472227833,0.00635176379820421));
#20875=CARTESIAN_POINT('',(0.00174427744926231,-0.015115178556117,0.00707537122438484));
#20876=CARTESIAN_POINT('',(0.000755539572102883,-0.0151410442227838,0.00724793348424899));
#20877=CARTESIAN_POINT('',(-0.00120915020832571,-0.0151927755561174,0.0071861910023124));
#20878=CARTESIAN_POINT('',(-0.00218510211159487,-0.0152186412227842,0.00695188626051166));
#20879=CARTESIAN_POINT('',(-0.0039636832410486,-0.0152703725561176,0.00611494774738645));
#20880=CARTESIAN_POINT('',(-0.00476631246723315,-0.0152962382227842,0.00551231397606199));
#20881=CARTESIAN_POINT('',(-0.00606622929600129,-0.0153479695561175,0.00403785624496691));
#20882=CARTESIAN_POINT('',(-0.00656351689858488,-0.015373835222784,0.00316603228519629));
#20883=CARTESIAN_POINT('',(-0.00717092837102258,-0.0154255665561169,0.00129655949974243));
#20884=CARTESIAN_POINT('',(-0.00728105224087671,-0.0154514322227833,0.000298910674059181));
#20885=CARTESIAN_POINT('',(-0.00711602427182116,-0.0154975925512275,-0.00144721562659419));
#20886=CARTESIAN_POINT('',(-0.00691874538139212,-0.0155178872130053,-0.00220307974809468));
#20887=CARTESIAN_POINT('',(-0.0066083882951212,-0.0155381818747831,-0.00290914662237177));
#20888=CARTESIAN_POINT('',(-0.00701667457144212,-0.0141095620215199,-0.00247645175440052));
#20889=CARTESIAN_POINT('',(-0.00675172820839158,-0.0141298567429902,-0.00322581371995272));
#20890=CARTESIAN_POINT('',(-0.00636670396676113,-0.0141501514644605,-0.00393281356206992));
#20891=CARTESIAN_POINT('',(-0.00525886997412413,-0.0141963118525972,-0.00536097505286025));
#20892=CARTESIAN_POINT('',(-0.00447234949865277,-0.0142221775192636,-0.00603275068895968));
#20893=CARTESIAN_POINT('',(-0.00269722323014958,-0.0142739088525966,-0.0070086536907097));
#20894=CARTESIAN_POINT('',(-0.00170861743711776,-0.0142997745192631,-0.00731278105636027));
#20895=CARTESIAN_POINT('',(0.000308075141393081,-0.0143515058525963,-0.00750340882449413));
#20896=CARTESIAN_POINT('',(0.0013361619268721,-0.014377371519263,-0.0073899092269774));
#20897=CARTESIAN_POINT('',(0.00326270246119069,-0.0144291028525964,-0.00676393998967931));
#20898=CARTESIAN_POINT('',(0.00416115621003024,-0.0144549685192631,-0.00625147034989796));
#20899=CARTESIAN_POINT('',(0.0056806442157655,-0.0145066998525967,-0.00491186094888794));
#20900=CARTESIAN_POINT('',(0.00630167847266119,-0.0145325655192636,-0.00408472118765927));
#20901=CARTESIAN_POINT('',(0.00716417287093968,-0.0145842968525973,-0.00225182747069477));
#20902=CARTESIAN_POINT('',(0.00740563301232249,-0.0146101625192642,-0.00124607351495895));
#20903=CARTESIAN_POINT('',(0.00746926128060979,-0.0146618938525979,0.000778611129588272));
#20904=CARTESIAN_POINT('',(0.00729142940751428,-0.0146877595192648,0.00179754181839966));
#20905=CARTESIAN_POINT('',(0.00654572533668907,-0.0147394908525986,0.00368097530693788));
#20906=CARTESIAN_POINT('',(0.00597785313895937,-0.0147653565192655,0.00454547810666471));
#20907=CARTESIAN_POINT('',(0.00454547811371136,-0.0148170878525993,0.00597785314604275));
#20908=CARTESIAN_POINT('',(0.00368097528619306,-0.0148429535192662,0.00654572538569395));
#20909=CARTESIAN_POINT('',(0.00179754183909638,-0.0148946848525999,0.00729142935852844));
#20910=CARTESIAN_POINT('',(0.000778611219518018,-0.0149205505192667,0.00746926109171173));
#20911=CARTESIAN_POINT('',(-0.00124607360493985,-0.0149722818526003,0.00740563320121896));
#20912=CARTESIAN_POINT('',(-0.00225182780981934,-0.0149981475192671,0.0071641735775429));
#20913=CARTESIAN_POINT('',(-0.00408472084858016,-0.0150498788526005,0.00630167776603658));
#20914=CARTESIAN_POINT('',(-0.00491185968246147,-0.0150757445192672,0.00568064157820631));
#20915=CARTESIAN_POINT('',(-0.00625147161635675,-0.0151274758526004,0.00416115884755274));
#20916=CARTESIAN_POINT('',(-0.00676394471637073,-0.0151533415192669,0.00326271230472946));
#20917=CARTESIAN_POINT('',(-0.00738990450030057,-0.0152050728525998,0.00133615208328845));
#20918=CARTESIAN_POINT('',(-0.00750339118421643,-0.0152309385192662,0.00030803840467072));
#20919=CARTESIAN_POINT('',(-0.00733332381384257,-0.0152770988477104,-0.0014914087435444));
#20920=CARTESIAN_POINT('',(-0.00713002068699959,-0.0152973935094882,-0.00227035442311136));
#20921=CARTESIAN_POINT('',(-0.00681018633503457,-0.015317688171266,-0.00299798221434941));
#20922=CARTESIAN_POINT('',(-0.00707757195030846,-0.013953649428554,-0.00249794475927006));
#20923=CARTESIAN_POINT('',(-0.0068103261306014,-0.0139739441500243,-0.00325381040103805));
#20924=CARTESIAN_POINT('',(-0.00642196028222026,-0.0139942388714947,-0.00396694626055288));
#20925=CARTESIAN_POINT('',(-0.0053045114520012,-0.0140403992596314,-0.00540750269577186));
#20926=CARTESIAN_POINT('',(-0.00451116480340562,-0.0140662649262978,-0.0060851086400904));
#20927=CARTESIAN_POINT('',(-0.00272063229996765,-0.0141179962596307,-0.00706948145674051));
#20928=CARTESIAN_POINT('',(-0.00172344644512524,-0.0141438619262972,-0.00737624832907208));
#20929=CARTESIAN_POINT('',(0.000310748910628592,-0.0141955932596305,-0.00756853054637559));
#20930=CARTESIAN_POINT('',(0.00134775841154002,-0.0142214589262971,-0.00745404589134754));
#20931=CARTESIAN_POINT('',(0.00329101929787511,-0.0142731902596305,-0.00682264389734764));
#20932=CARTESIAN_POINT('',(0.00419727068329876,-0.0142990559262973,-0.00630572655837581));
#20933=CARTESIAN_POINT('',(0.00572994625186395,-0.0143507872596309,-0.00495449075223675));
#20934=CARTESIAN_POINT('',(0.00635637043500548,-0.0143766529262977,-0.00412017228506952));
#20935=CARTESIAN_POINT('',(0.00722635038040566,-0.0144283842596314,-0.00227137097228207));
#20936=CARTESIAN_POINT('',(0.00746990614266431,-0.0144542499262983,-0.00125688812666184));
#20937=CARTESIAN_POINT('',(0.00753408663761127,-0.0145059812596321,0.000785368657882526));
#20938=CARTESIAN_POINT('',(0.00735471137029958,-0.014531846926299,0.00181314259680667));
#20939=CARTESIAN_POINT('',(0.00660253536994981,-0.0145835782596328,0.00371292231339825));
#20940=CARTESIAN_POINT('',(0.00602973463691172,-0.0146094439262997,0.00458492809106569));
#20941=CARTESIAN_POINT('',(0.00458492809817351,-0.0146611752596334,0.00602973464405657));
#20942=CARTESIAN_POINT('',(0.00371292229247339,-0.0146870409263003,0.00660253541937999));
#20943=CARTESIAN_POINT('',(0.00181314261768301,-0.014738772259634,0.0073547113208886));
#20944=CARTESIAN_POINT('',(0.000785368748592763,-0.0147646379263009,0.00753408644707377));
#20945=CARTESIAN_POINT('',(-0.00125688821742369,-0.0148163692596345,0.0074699063332002));
#20946=CARTESIAN_POINT('',(-0.00227137131434988,-0.0148422349263012,0.00722635109314146));
#20947=CARTESIAN_POINT('',(-0.00412017194304756,-0.0148939662596347,0.0063563697222481));
#20948=CARTESIAN_POINT('',(-0.00495448947481903,-0.0149198319263013,0.0057299435914135));
#20949=CARTESIAN_POINT('',(-0.00630572783582614,-0.0149715632596345,0.00419727334371219));
#20950=CARTESIAN_POINT('',(-0.00682264866506179,-0.014997428926301,0.00329102922684548));
#20951=CARTESIAN_POINT('',(-0.00745404112364812,-0.015049160259634,0.00134774848252438));
#20952=CARTESIAN_POINT('',(-0.0075685127529988,-0.0150750259263004,0.000310711855069994));
#20953=CARTESIAN_POINT('',(-0.00739696937615192,-0.0151211862547445,-0.00150435260781735));
#20954=CARTESIAN_POINT('',(-0.00719190179131477,-0.0151414809165224,-0.00229005871922163));
#20955=CARTESIAN_POINT('',(-0.00686929161249504,-0.0151617755783001,-0.00302400155682894));
#20956=CARTESIAN_POINT('',(-0.00707757195030845,-0.0137939948724753,-0.00249794475927006));
#20957=CARTESIAN_POINT('',(-0.0068103261306014,-0.0138142895939456,-0.00325381040103805));
#20958=CARTESIAN_POINT('',(-0.00642196028222026,-0.0138345843154159,-0.00396694626055287));
#20959=CARTESIAN_POINT('',(-0.0053045114520012,-0.0138807447035526,-0.00540750269577185));
#20960=CARTESIAN_POINT('',(-0.00451116480340562,-0.013906610370219,-0.0060851086400904));
#20961=CARTESIAN_POINT('',(-0.00272063229996764,-0.013958341703552,-0.00706948145674052));
#20962=CARTESIAN_POINT('',(-0.00172344644512524,-0.0139842073702185,-0.00737624832907208));
#20963=CARTESIAN_POINT('',(0.000310748910628593,-0.0140359387035517,-0.00756853054637559));
#20964=CARTESIAN_POINT('',(0.00134775841154002,-0.0140618043702184,-0.00745404589134754));
#20965=CARTESIAN_POINT('',(0.00329101929787511,-0.0141135357035518,-0.00682264389734764));
#20966=CARTESIAN_POINT('',(0.00419727068329876,-0.0141394013702185,-0.00630572655837581));
#20967=CARTESIAN_POINT('',(0.00572994625186394,-0.0141911327035521,-0.00495449075223675));
#20968=CARTESIAN_POINT('',(0.00635637043500548,-0.014216998370219,-0.00412017228506952));
#20969=CARTESIAN_POINT('',(0.00722635038040566,-0.0142687297035527,-0.00227137097228208));
#20970=CARTESIAN_POINT('',(0.00746990614266432,-0.0142945953702195,-0.00125688812666185));
#20971=CARTESIAN_POINT('',(0.00753408663761127,-0.0143463267035533,0.000785368657882525));
#20972=CARTESIAN_POINT('',(0.00735471137029958,-0.0143721923702202,0.00181314259680667));
#20973=CARTESIAN_POINT('',(0.0066025353699498,-0.014423923703554,0.00371292231339825));
#20974=CARTESIAN_POINT('',(0.00602973463691171,-0.0144497893702209,0.00458492809106569));
#20975=CARTESIAN_POINT('',(0.00458492809817351,-0.0145015207035547,0.00602973464405656));
#20976=CARTESIAN_POINT('',(0.00371292229247339,-0.0145273863702216,0.00660253541937999));
#20977=CARTESIAN_POINT('',(0.00181314261768301,-0.0145791177035553,0.00735471132088859));
#20978=CARTESIAN_POINT('',(0.000785368748592767,-0.0146049833702221,0.00753408644707377));
#20979=CARTESIAN_POINT('',(-0.00125688821742368,-0.0146567147035557,0.0074699063332002));
#20980=CARTESIAN_POINT('',(-0.00227137131434989,-0.0146825803702225,0.00722635109314146));
#20981=CARTESIAN_POINT('',(-0.00412017194304756,-0.0147343117035559,0.00635636972224811));
#20982=CARTESIAN_POINT('',(-0.00495448947481903,-0.0147601773702226,0.00572994359141351));
#20983=CARTESIAN_POINT('',(-0.00630572783582614,-0.0148119087035558,0.00419727334371219));
#20984=CARTESIAN_POINT('',(-0.00682264866506179,-0.0148377743702223,0.00329102922684548));
#20985=CARTESIAN_POINT('',(-0.0074540411236481,-0.0148895057035552,0.00134774848252438));
#20986=CARTESIAN_POINT('',(-0.00756851275299878,-0.0149153713702216,0.000310711855069997));
#20987=CARTESIAN_POINT('',(-0.00739696937615191,-0.0149615316986658,-0.00150435260781735));
#20988=CARTESIAN_POINT('',(-0.00719190179131477,-0.0149818263604436,-0.00229005871922163));
#20989=CARTESIAN_POINT('',(-0.00686929161249505,-0.0150021210222214,-0.00302400155682894));
#20990=CARTESIAN_POINT('',(-0.0070775368722768,-0.0137902529093624,-0.0024979323788964));
#20991=CARTESIAN_POINT('',(-0.00681029237709987,-0.0138105476308327,-0.00325379427442499));
#20992=CARTESIAN_POINT('',(-0.00642192845354686,-0.013830842352303,-0.00396692659947878));
#20993=CARTESIAN_POINT('',(-0.00530448516165446,-0.0138770027404397,-0.00540747589497744));
#20994=CARTESIAN_POINT('',(-0.00451114244506255,-0.0139028684071061,-0.00608507848092918));
#20995=CARTESIAN_POINT('',(-0.00272061881590466,-0.0139545997404391,-0.00706944641880716));
#20996=CARTESIAN_POINT('',(-0.00172343790333868,-0.0139804654071056,-0.0073762117707334));
#20997=CARTESIAN_POINT('',(0.000310747370487398,-0.0140321967404388,-0.00756849303504318));
#20998=CARTESIAN_POINT('',(0.00134775173174749,-0.0140580624071055,-0.00745400894742672));
#20999=CARTESIAN_POINT('',(0.00329100298684642,-0.0141097937404389,-0.00682261008279651));
#21000=CARTESIAN_POINT('',(0.00419724988068525,-0.0141356594071056,-0.00630569530578278));
#21001=CARTESIAN_POINT('',(0.00572991785296706,-0.0141873907404392,-0.00495446619667099));
#21002=CARTESIAN_POINT('',(0.00635633893141005,-0.0142132564071061,-0.00412015186457294));
#21003=CARTESIAN_POINT('',(0.00722631456499478,-0.0142649877404398,-0.00227135971485885));
#21004=CARTESIAN_POINT('',(0.00746986912013654,-0.0142908534071066,-0.0012568818972428));
#21005=CARTESIAN_POINT('',(0.00753404929699058,-0.0143425847404404,0.000785364765419568));
#21006=CARTESIAN_POINT('',(0.00735467491870289,-0.0143684504071073,0.00181313361046589));
#21007=CARTESIAN_POINT('',(0.00660250264630582,-0.0144201817404411,0.00371290391132373));
#21008=CARTESIAN_POINT('',(0.00602970475219645,-0.014446047407108,0.00458490536713524));
#21009=CARTESIAN_POINT('',(0.00458490537424303,-0.0144977787404418,0.00602970475934126));
#21010=CARTESIAN_POINT('',(0.00371290389039897,-0.0145236444071087,0.00660250269573577));
#21011=CARTESIAN_POINT('',(0.00181313363134214,-0.0145753757404424,0.00735467486929215));
#21012=CARTESIAN_POINT('',(0.00078536485612936,-0.0146012414071092,0.00753404910645403));
#21013=CARTESIAN_POINT('',(-0.00125688198800419,-0.0146529727404428,0.00746986931067148));
#21014=CARTESIAN_POINT('',(-0.00227136005692497,-0.0146788384071096,0.00722631527772705));
#21015=CARTESIAN_POINT('',(-0.00412015152255267,-0.014730569740443,0.00635633821865621));
#21016=CARTESIAN_POINT('',(-0.0049544649192596,-0.0147564354071097,0.00572991519252981));
#21017=CARTESIAN_POINT('',(-0.00630569658322677,-0.0148081667404429,0.00419725254108549));
#21018=CARTESIAN_POINT('',(-0.00682261485048703,-0.0148340324071094,0.00329101291576758));
#21019=CARTESIAN_POINT('',(-0.00745400417975091,-0.0148857637404423,0.00134774180278106));
#21020=CARTESIAN_POINT('',(-0.00756847524175456,-0.0149116294071087,0.000310710315112458));
#21021=CARTESIAN_POINT('',(-0.00739693271511507,-0.0149577897355529,-0.00150434515190892));
#21022=CARTESIAN_POINT('',(-0.00719186614663881,-0.0149780843973307,-0.00229004736917774));
#21023=CARTESIAN_POINT('',(-0.00686925756674739,-0.0149983790591085,-0.00302398656919998));
#21024=CARTESIAN_POINT('',(-0.00707746696279632,-0.0137865115775635,-0.00249790770517756));
#21025=CARTESIAN_POINT('',(-0.00681022510736881,-0.0138068062990338,-0.00325376213456173));
#21026=CARTESIAN_POINT('',(-0.00642186501994136,-0.0138271010205041,-0.00396688741553913));
#21027=CARTESIAN_POINT('',(-0.00530443276577034,-0.0138732614086409,-0.00540742248178619));
#21028=CARTESIAN_POINT('',(-0.00451109788554553,-0.0138991270753072,-0.00608501837461211));
#21029=CARTESIAN_POINT('',(-0.00272059194256561,-0.0139508584086402,-0.00706937658924141));
#21030=CARTESIAN_POINT('',(-0.00172342087981049,-0.0139767240753067,-0.00737613891104477));
#21031=CARTESIAN_POINT('',(0.000310744301031509,-0.0140284554086399,-0.0075684182760662));
#21032=CARTESIAN_POINT('',(0.00134773841911838,-0.0140543210753066,-0.00745393531928427));
#21033=CARTESIAN_POINT('',(0.00329097047944826,-0.01410605240864,-0.00682254269139537));
#21034=CARTESIAN_POINT('',(0.00419720842169126,-0.0141319180753068,-0.00630563302028842));
#21035=CARTESIAN_POINT('',(0.0057298612548048,-0.0141836494086403,-0.00495441725815409));
#21036=CARTESIAN_POINT('',(0.00635627614567535,-0.0142095150753072,-0.0041201111671267));
#21037=CARTESIAN_POINT('',(0.00722624318593931,-0.0142612464086409,-0.00227133727914703));
#21038=CARTESIAN_POINT('',(0.00746979533533275,-0.0142871120753078,-0.00125686948219474));
#21039=CARTESIAN_POINT('',(0.00753397487823703,-0.0143388434086415,0.000785357007855923));
#21040=CARTESIAN_POINT('',(0.00735460227174789,-0.0143647090753085,0.00181311570095429));
#21041=CARTESIAN_POINT('',(0.00660243742905041,-0.0144164404086423,0.00371286723653302));
#21042=CARTESIAN_POINT('',(0.00602964519284208,-0.0144423060753091,0.0045848600790134));
#21043=CARTESIAN_POINT('',(0.00458486008612111,-0.0144940374086429,0.00602964519998682));
#21044=CARTESIAN_POINT('',(0.00371286721560847,-0.0145199030753098,0.00660243747847987));
#21045=CARTESIAN_POINT('',(0.00181311572183033,-0.0145716344086435,0.00735460222233764));
#21046=CARTESIAN_POINT('',(0.000785357098564819,-0.0145975000753104,0.00753397468770236));
#21047=CARTESIAN_POINT('',(-0.00125686957295523,-0.0146492314086439,0.0074697955258658));
#21048=CARTESIAN_POINT('',(-0.00227133762120977,-0.0146750970753107,0.00722624389866454));
#21049=CARTESIAN_POINT('',(-0.00412011082510981,-0.0147268284086441,0.00635627543292855));
#21050=CARTESIAN_POINT('',(-0.00495441598075532,-0.0147526940753108,0.00572985859439383));
#21051=CARTESIAN_POINT('',(-0.0063056342977198,-0.014804425408644,0.00419721108206523));
#21052=CARTESIAN_POINT('',(-0.0068225474590388,-0.0148302910753105,0.00329098040827135));
#21053=CARTESIAN_POINT('',(-0.00745393055165556,-0.0148820224086434,0.00134772849025003));
#21054=CARTESIAN_POINT('',(-0.00756840048295334,-0.0149078880753098,0.000310707246022589));
#21055=CARTESIAN_POINT('',(-0.00739685965075207,-0.014954048403754,-0.00150433029250374));
#21056=CARTESIAN_POINT('',(-0.007191795107853,-0.0149743430655318,-0.00229002474887569));
#21057=CARTESIAN_POINT('',(-0.00686918971457842,-0.0149946377273096,-0.00302395669929837));
#21058=CARTESIAN_POINT('',(-0.00586834150890119,-0.0138049000806154,-0.00232344489035294));
#21059=CARTESIAN_POINT('',(-0.00586834159177923,-0.0139608126196482,-0.00232344492316673));
#21060=CARTESIAN_POINT('',(-0.00598842721148222,-0.0142726376300705,-0.00237099026780637));
#21061=CARTESIAN_POINT('',(-0.00642329533287495,-0.0144663808213605,-0.0025431670426404));
#21062=CARTESIAN_POINT('',(-0.00685816345475783,-0.0142726376313009,-0.00271534381766851));
#21063=CARTESIAN_POINT('',(-0.00697824907519072,-0.0139608126212183,-0.00276288916259713));
#21064=CARTESIAN_POINT('',(-0.00697824915847185,-0.0138049000821855,-0.00276288919557052));
#21065=CARTESIAN_POINT('',(-0.00697843089362731,-0.013804899963342,-0.00276295619394444));
#21066=CARTESIAN_POINT('',(-0.00586849430092666,-0.013804899964658,-0.00232350132797368));
#21067=CARTESIAN_POINT('',(-0.00697825089046431,-0.0138048997861662,-0.00276288482710193));
#21068=CARTESIAN_POINT('',(-0.00625400807864927,-0.0138546414753982,-0.00458958735145836));
#21069=CARTESIAN_POINT('',(-0.00330460840350429,-0.0139541248538628,-0.00763147687281364));
#21070=CARTESIAN_POINT('',(0.0030621357297459,-0.0141033499215613,-0.00773406117409333));
#21071=CARTESIAN_POINT('',(0.00763353556729034,-0.0142525749892608,-0.00330332218243761));
#21072=CARTESIAN_POINT('',(0.00773371924336336,-0.0144018000569608,0.00306199180738646));
#21073=CARTESIAN_POINT('',(0.00330333556286005,-0.0145510251246608,0.00763352977367144));
#21074=CARTESIAN_POINT('',(-0.00306212095780749,-0.0147002501923603,0.00773406701808752));
#21075=CARTESIAN_POINT('',(-0.00763305811154286,-0.0148494752600588,0.00330095436087306));
#21076=CARTESIAN_POINT('',(-0.0077007653178123,-0.0149489586385234,-0.00093549061401399));
#21077=CARTESIAN_POINT('',(-0.00697825341078448,-0.0149987003277554,-0.00276287845231342));
#21078=CARTESIAN_POINT('',(-0.00586834506485856,-0.0149987002524587,-0.0023234359064578));
#21079=CARTESIAN_POINT('',(-0.00647593969287228,-0.0149489585632873,-0.000786698594375238));
#21080=CARTESIAN_POINT('',(-0.00641900151649344,-0.0148494751849436,0.00277592940882954));
#21081=CARTESIAN_POINT('',(-0.00257508317452219,-0.0147002501174267,0.00650394465486067));
#21082=CARTESIAN_POINT('',(0.00277793186253437,-0.0145510250499086,0.00641939816488278));
#21083=CARTESIAN_POINT('',(0.00650365218961118,-0.0144017999823902,0.00257497457819126));
#21084=CARTESIAN_POINT('',(0.00641940304225482,-0.0142525749148716,-0.00277792059801396));
#21085=CARTESIAN_POINT('',(0.00257509562175463,-0.0141033498473536,-0.00650393973044446));
#21086=CARTESIAN_POINT('',(-0.00277900223015413,-0.0139541247798366,-0.00641767179346711));
#21087=CARTESIAN_POINT('',(-0.00525929268773173,-0.013854641401493,-0.00385960230652013));
#21088=CARTESIAN_POINT('',(-0.00586834292757561,-0.0138048997123215,-0.00232344131214153));
#21089=CARTESIAN_POINT('',(-0.0069782482560913,-0.0138058164296786,-0.00276288945313269));
#21090=CARTESIAN_POINT('',(-0.00671751942259483,-0.0138237235055873,-0.00342050460393881));
#21091=CARTESIAN_POINT('',(-0.00636415962312206,-0.0138416305814961,-0.00404145862550986));
#21092=CARTESIAN_POINT('',(-0.00530451092621718,-0.0138854033240712,-0.00540750215977932));
#21093=CARTESIAN_POINT('',(-0.00451116435625826,-0.0139112689907376,-0.00608510803693347));
#21094=CARTESIAN_POINT('',(-0.00272063203029814,-0.0139630003240705,-0.00706948075601239));
#21095=CARTESIAN_POINT('',(-0.00172344627429696,-0.0139888659907371,-0.00737624759793717));
#21096=CARTESIAN_POINT('',(0.000310748879827101,-0.0140405973240703,-0.00756852979618164));
#21097=CARTESIAN_POINT('',(0.00134775827794998,-0.0140664629907369,-0.00745404515250133));
#21098=CARTESIAN_POINT('',(0.00329101897166874,-0.0141181943240703,-0.0068226432210861));
#21099=CARTESIAN_POINT('',(0.00419727026726461,-0.0141440599907371,-0.00630572593335119));
#21100=CARTESIAN_POINT('',(0.00572994568391076,-0.0141957913240707,-0.00495449026114685));
#21101=CARTESIAN_POINT('',(0.00635636980496102,-0.0142216569907375,-0.00412017187667741));
#21102=CARTESIAN_POINT('',(0.00722634966412866,-0.0142733883240712,-0.00227137074714344));
#21103=CARTESIAN_POINT('',(0.00746990540224603,-0.0142992539907381,-0.00125688800207892));
#21104=CARTESIAN_POINT('',(0.00753408589083141,-0.0143509853240719,0.000785368580036637));
#21105=CARTESIAN_POINT('',(0.00735471064129942,-0.0143768509907388,0.00181314241708767));
#21106=CARTESIAN_POINT('',(0.00660253471550546,-0.0144285823240726,0.00371292194537279));
#21107=CARTESIAN_POINT('',(0.00602973403924347,-0.0144544479907395,0.00458492763660688));
#21108=CARTESIAN_POINT('',(0.00458492764371473,-0.0145061793240733,0.00602973404638829));
#21109=CARTESIAN_POINT('',(0.00371292192444796,-0.0145320449907402,0.00660253476493562));
#21110=CARTESIAN_POINT('',(0.00181314243796406,-0.0145837763240739,0.00735471059188843));
#21111=CARTESIAN_POINT('',(0.000785368670746929,-0.0146096419907407,0.00753408570029392));
#21112=CARTESIAN_POINT('',(-0.00125688809284068,-0.0146613733240743,0.00746990559278191));
#21113=CARTESIAN_POINT('',(-0.00227137108921116,-0.014687238990741,0.0072263503768644));
#21114=CARTESIAN_POINT('',(-0.00412017153465543,-0.0147389703240745,0.00635636909220375));
#21115=CARTESIAN_POINT('',(-0.00495448898372923,-0.0147648359907411,0.00572994302346061));
#21116=CARTESIAN_POINT('',(-0.00630572721080138,-0.0148165673240743,0.00419727292767782));
#21117=CARTESIAN_POINT('',(-0.00682264798879975,-0.0148424329907408,0.00329102890063817));
#21118=CARTESIAN_POINT('',(-0.00745404038480235,-0.0148941643240738,0.00134774834893538));
#21119=CARTESIAN_POINT('',(-0.00756851200280659,-0.0149200299907402,0.000310711824272237));
#21120=CARTESIAN_POINT('',(-0.00740584135015542,-0.0149638027765913,-0.001410472206315));
#21121=CARTESIAN_POINT('',(-0.0072383566310885,-0.0149817098957761,-0.00210502129056344));
#21122=CARTESIAN_POINT('',(-0.00697825014639974,-0.0149996170149608,-0.00276288468535656));
#21123=CARTESIAN_POINT('',(-0.0069782487171706,-0.0138055108774392,-0.00276288963568727));
#21124=CARTESIAN_POINT('',(-0.00671751986644679,-0.0138234179533479,-0.00342050482994451));
#21125=CARTESIAN_POINT('',(-0.00636416004362621,-0.0138413250292567,-0.00404145889254434));
#21126=CARTESIAN_POINT('',(-0.00530451127670632,-0.0138850977718318,-0.00540750251707348));
#21127=CARTESIAN_POINT('',(-0.00451116465432798,-0.0139109634384982,-0.00608510843899961));
#21128=CARTESIAN_POINT('',(-0.00272063221006061,-0.0139626947718311,-0.00706948122311977));
#21129=CARTESIAN_POINT('',(-0.00172344638817159,-0.0139885604384977,-0.0073762480853138));
#21130=CARTESIAN_POINT('',(0.000310748900359457,-0.0140402917718309,-0.00756853029626308));
#21131=CARTESIAN_POINT('',(0.00134775836700148,-0.0140661574384975,-0.00745404564501834));
#21132=CARTESIAN_POINT('',(0.00329101918911883,-0.0141178887718309,-0.006822643671884));
#21133=CARTESIAN_POINT('',(0.00419727054459417,-0.0141437544384977,-0.0063057263499944));
#21134=CARTESIAN_POINT('',(0.00572994606250998,-0.0141954857718313,-0.0049544905885088));
#21135=CARTESIAN_POINT('',(0.00635637022495046,-0.0142213514384981,-0.00412017214891278));
#21136=CARTESIAN_POINT('',(0.00722635014160097,-0.0142730827718318,-0.00227137089722152));
#21137=CARTESIAN_POINT('',(0.00746990589581098,-0.0142989484384987,-0.00125688808512627));
#21138=CARTESIAN_POINT('',(0.00753408638863701,-0.0143506797718325,0.000785368631928915));
#21139=CARTESIAN_POINT('',(0.00735471112725302,-0.0143765454384994,0.00181314253688886));
#21140=CARTESIAN_POINT('',(0.00660253515175994,-0.0144282767718332,0.00371292219069961));
#21141=CARTESIAN_POINT('',(0.00602973443765085,-0.0144541424385001,0.00458492793955042));
#21142=CARTESIAN_POINT('',(0.00458492794665827,-0.0145058737718339,0.00602973444479567));
#21143=CARTESIAN_POINT('',(0.00371292216977478,-0.0145317394385007,0.00660253520119011));
#21144=CARTESIAN_POINT('',(0.00181314255776525,-0.0145834707718344,0.00735471107784203));
#21145=CARTESIAN_POINT('',(0.000785368722639213,-0.0146093364385013,0.00753408619809951));
#21146=CARTESIAN_POINT('',(-0.00125688817588804,-0.0146610677718349,0.00746990608634688));
#21147=CARTESIAN_POINT('',(-0.00227137123928926,-0.0146869334385016,0.00722635085433675));
#21148=CARTESIAN_POINT('',(-0.00412017180689078,-0.0147386647718351,0.00635636951219315));
#21149=CARTESIAN_POINT('',(-0.00495448931109109,-0.0147645304385017,0.00572994340205966));
#21150=CARTESIAN_POINT('',(-0.00630572762744468,-0.0148162617718349,0.00419727320500755));
#21151=CARTESIAN_POINT('',(-0.00682264843959796,-0.0148421274385014,0.00329102911808892));
#21152=CARTESIAN_POINT('',(-0.00745404087731905,-0.0148938587718344,0.00134774843798622));
#21153=CARTESIAN_POINT('',(-0.00756851250288686,-0.0149197244385008,0.000310711844802144));
#21154=CARTESIAN_POINT('',(-0.00740584183948742,-0.0149634972243519,-0.00141047229951024));
#21155=CARTESIAN_POINT('',(-0.00723835710935415,-0.0149814043435367,-0.00210502142965017));
#21156=CARTESIAN_POINT('',(-0.00697825060747917,-0.0149993114627214,-0.00276288486791082));
#21157=CARTESIAN_POINT('',(-0.00697824894777644,-0.0138052053248561,-0.00276288972699076));
#21158=CARTESIAN_POINT('',(-0.00671752008843649,-0.0138231124007648,-0.0034205049429798));
#21159=CARTESIAN_POINT('',(-0.00636416025393864,-0.0138410194766736,-0.00404145902609992));
#21160=CARTESIAN_POINT('',(-0.0053045114520012,-0.0138847922192487,-0.00540750269577185));
#21161=CARTESIAN_POINT('',(-0.00451116480340563,-0.0139106578859151,-0.0060851086400904));
#21162=CARTESIAN_POINT('',(-0.00272063229996765,-0.013962389219248,-0.00706948145674051));
#21163=CARTESIAN_POINT('',(-0.00172344644512525,-0.0139882548859145,-0.00737624832907208));
#21164=CARTESIAN_POINT('',(0.000310748910628583,-0.0140399862192477,-0.00756853054637559));
#21165=CARTESIAN_POINT('',(0.00134775841154001,-0.0140658518859144,-0.00745404589134754));
#21166=CARTESIAN_POINT('',(0.00329101929787509,-0.0141175832192478,-0.00682264389734765));
#21167=CARTESIAN_POINT('',(0.00419727068329875,-0.0141434488859146,-0.00630572655837581));
#21168=CARTESIAN_POINT('',(0.00572994625186394,-0.0141951802192481,-0.00495449075223676));
#21169=CARTESIAN_POINT('',(0.00635637043500547,-0.014221045885915,-0.00412017228506954));
#21170=CARTESIAN_POINT('',(0.00722635038040566,-0.0142727772192487,-0.0022713709722821));
#21171=CARTESIAN_POINT('',(0.00746990614266431,-0.0142986428859156,-0.00125688812666187));
#21172=CARTESIAN_POINT('',(0.00753408663761127,-0.0143503742192494,0.000785368657882503));
#21173=CARTESIAN_POINT('',(0.00735471137029958,-0.0143762398859162,0.00181314259680665));
#21174=CARTESIAN_POINT('',(0.00660253536994981,-0.0144279712192501,0.00371292231339824));
#21175=CARTESIAN_POINT('',(0.00602973463691173,-0.014453836885917,0.00458492809106568));
#21176=CARTESIAN_POINT('',(0.00458492809817353,-0.0145055682192507,0.00602973464405655));
#21177=CARTESIAN_POINT('',(0.00371292229247341,-0.0145314338859176,0.00660253541937998));
#21178=CARTESIAN_POINT('',(0.00181314261768305,-0.0145831652192513,0.00735471132088858));
#21179=CARTESIAN_POINT('',(0.000785368748592804,-0.0146090308859182,0.00753408644707376));
#21180=CARTESIAN_POINT('',(-0.00125688821742364,-0.0146607622192517,0.00746990633320021));
#21181=CARTESIAN_POINT('',(-0.00227137131434985,-0.0146866278859185,0.00722635109314147));
#21182=CARTESIAN_POINT('',(-0.00412017194304753,-0.0147383592192519,0.00635636972224813));
#21183=CARTESIAN_POINT('',(-0.00495448947481901,-0.0147642248859186,0.00572994359141353));
#21184=CARTESIAN_POINT('',(-0.00630572783582613,-0.0148159562192518,0.00419727334371222));
#21185=CARTESIAN_POINT('',(-0.00682264866506177,-0.0148418218859183,0.00329102922684551));
#21186=CARTESIAN_POINT('',(-0.00745404112364809,-0.0148935532192512,0.00134774848252442));
#21187=CARTESIAN_POINT('',(-0.00756851275299878,-0.0149194188859176,0.000310711855070045));
#21188=CARTESIAN_POINT('',(-0.00740584208422366,-0.0149631916717688,-0.00141047234612124));
#21189=CARTESIAN_POINT('',(-0.00723835734855563,-0.0149810987909535,-0.00210502149921351));
#21190=CARTESIAN_POINT('',(-0.00697825083808507,-0.0149990059101382,-0.00276288495921415));
#21191=CARTESIAN_POINT('',(-0.00697824894777643,-0.0136489871793071,-0.00276288972699076));
#21192=CARTESIAN_POINT('',(-0.00671752008843648,-0.0136668942552158,-0.00342050494297979));
#21193=CARTESIAN_POINT('',(-0.00636416025393864,-0.0136848013311246,-0.00404145902609991));
#21194=CARTESIAN_POINT('',(-0.00530451145200118,-0.0137285740736997,-0.00540750269577185));
#21195=CARTESIAN_POINT('',(-0.00451116480340563,-0.0137544397403661,-0.0060851086400904));
#21196=CARTESIAN_POINT('',(-0.00272063229996765,-0.013806171073699,-0.00706948145674051));
#21197=CARTESIAN_POINT('',(-0.00172344644512525,-0.0138320367403656,-0.00737624832907206));
#21198=CARTESIAN_POINT('',(0.000310748910628584,-0.0138837680736988,-0.00756853054637558));
#21199=CARTESIAN_POINT('',(0.00134775841154,-0.0139096337403654,-0.00745404589134751));
#21200=CARTESIAN_POINT('',(0.00329101929787509,-0.0139613650736988,-0.00682264389734765));
#21201=CARTESIAN_POINT('',(0.00419727068329874,-0.0139872307403656,-0.00630572655837582));
#21202=CARTESIAN_POINT('',(0.00572994625186393,-0.0140389620736992,-0.00495449075223676));
#21203=CARTESIAN_POINT('',(0.00635637043500546,-0.014064827740366,-0.00412017228506954));
#21204=CARTESIAN_POINT('',(0.00722635038040564,-0.0141165590736997,-0.0022713709722821));
#21205=CARTESIAN_POINT('',(0.0074699061426643,-0.0141424247403666,-0.00125688812666187));
#21206=CARTESIAN_POINT('',(0.00753408663761126,-0.0141941560737003,0.000785368657882502));
#21207=CARTESIAN_POINT('',(0.00735471137029958,-0.0142200217403673,0.00181314259680665));
#21208=CARTESIAN_POINT('',(0.00660253536994981,-0.0142717530737011,0.00371292231339823));
#21209=CARTESIAN_POINT('',(0.00602973463691171,-0.014297618740368,0.00458492809106568));
#21210=CARTESIAN_POINT('',(0.00458492809817351,-0.0143493500737018,0.00602973464405654));
#21211=CARTESIAN_POINT('',(0.0037129222924734,-0.0143752157403687,0.00660253541937998));
#21212=CARTESIAN_POINT('',(0.00181314261768305,-0.0144269470737023,0.00735471132088859));
#21213=CARTESIAN_POINT('',(0.000785368748592803,-0.0144528127403691,0.00753408644707377));
#21214=CARTESIAN_POINT('',(-0.00125688821742364,-0.0145045440737028,0.00746990633320021));
#21215=CARTESIAN_POINT('',(-0.00227137131434984,-0.0145304097403695,0.00722635109314145));
#21216=CARTESIAN_POINT('',(-0.00412017194304752,-0.0145821410737029,0.00635636972224812));
#21217=CARTESIAN_POINT('',(-0.00495448947481899,-0.0146080067403696,0.00572994359141353));
#21218=CARTESIAN_POINT('',(-0.00630572783582612,-0.0146597380737028,0.00419727334371222));
#21219=CARTESIAN_POINT('',(-0.00682264866506177,-0.0146856037403693,0.00329102922684551));
#21220=CARTESIAN_POINT('',(-0.0074540411236481,-0.0147373350737023,0.00134774848252442));
#21221=CARTESIAN_POINT('',(-0.00756851275299876,-0.0147632007403686,0.000310711855070046));
#21222=CARTESIAN_POINT('',(-0.00740584208422365,-0.0148069735262198,-0.00141047234612124));
#21223=CARTESIAN_POINT('',(-0.00723835734855561,-0.0148248806454045,-0.0021050214992135));
#21224=CARTESIAN_POINT('',(-0.00697825083808506,-0.0148427877645893,-0.00276288495921415));
#21225=CARTESIAN_POINT('',(-0.00691820617138646,-0.0134930745863413,-0.00273911706262906));
#21226=CARTESIAN_POINT('',(-0.00665972069498067,-0.01351098166225,-0.00339107397613279));
#21227=CARTESIAN_POINT('',(-0.00630940126584622,-0.0135288887381587,-0.00400668519925462));
#21228=CARTESIAN_POINT('',(-0.00525886997412414,-0.0135726614807338,-0.00536097505286025));
#21229=CARTESIAN_POINT('',(-0.00447234949865277,-0.0135985271474002,-0.00603275068895968));
#21230=CARTESIAN_POINT('',(-0.00269722323014959,-0.0136502584807331,-0.00700865369070969));
#21231=CARTESIAN_POINT('',(-0.00170861743711776,-0.0136761241473997,-0.00731278105636027));
#21232=CARTESIAN_POINT('',(0.000308075141393075,-0.0137278554807329,-0.00750340882449412));
#21233=CARTESIAN_POINT('',(0.00133616192687209,-0.0137537211473996,-0.0073899092269774));
#21234=CARTESIAN_POINT('',(0.00326270246119067,-0.013805452480733,-0.00676393998967932));
#21235=CARTESIAN_POINT('',(0.00416115621003024,-0.0138313181473997,-0.00625147034989796));
#21236=CARTESIAN_POINT('',(0.00568064421576549,-0.0138830494807333,-0.00491186094888795));
#21237=CARTESIAN_POINT('',(0.00630167847266118,-0.0139089151474001,-0.00408472118765929));
#21238=CARTESIAN_POINT('',(0.00716417287093968,-0.0139606464807338,-0.0022518274706948));
#21239=CARTESIAN_POINT('',(0.00740563301232249,-0.0139865121474007,-0.00124607351495897));
#21240=CARTESIAN_POINT('',(0.00746926128060979,-0.0140382434807345,0.000778611129588249));
#21241=CARTESIAN_POINT('',(0.00729142940751429,-0.0140641091474014,0.00179754181839964));
#21242=CARTESIAN_POINT('',(0.00654572533668908,-0.0141158404807352,0.00368097530693786));
#21243=CARTESIAN_POINT('',(0.00597785313895938,-0.0141417061474021,0.00454547810666469));
#21244=CARTESIAN_POINT('',(0.00454547811371137,-0.0141934374807359,0.00597785314604273));
#21245=CARTESIAN_POINT('',(0.00368097528619307,-0.0142193031474028,0.00654572538569394));
#21246=CARTESIAN_POINT('',(0.00179754183909641,-0.0142710344807365,0.00729142935852844));
#21247=CARTESIAN_POINT('',(0.000778611219518056,-0.0142969001474033,0.00746926109171172));
#21248=CARTESIAN_POINT('',(-0.0012460736049398,-0.0143486314807369,0.00740563320121896));
#21249=CARTESIAN_POINT('',(-0.00225182780981931,-0.0143744971474037,0.00716417357754291));
#21250=CARTESIAN_POINT('',(-0.00408472084858013,-0.0144262284807371,0.0063016777660366));
#21251=CARTESIAN_POINT('',(-0.00491185968246145,-0.0144520941474037,0.00568064157820633));
#21252=CARTESIAN_POINT('',(-0.00625147161635674,-0.0145038254807369,0.00416115884755278));
#21253=CARTESIAN_POINT('',(-0.00676394471637072,-0.0145296911474035,0.00326271230472949));
#21254=CARTESIAN_POINT('',(-0.00738990450030056,-0.0145814224807364,0.00133615208328849));
#21255=CARTESIAN_POINT('',(-0.00750339118421642,-0.0146072881474028,0.000308038404670769));
#21256=CARTESIAN_POINT('',(-0.00734212017868972,-0.0146510609332539,-0.00139833625348307));
#21257=CARTESIAN_POINT('',(-0.00717607652782788,-0.0146689680524387,-0.00208690931432024));
#21258=CARTESIAN_POINT('',(-0.00691820804543036,-0.0146868751716234,-0.00273911233587572));
#21259=CARTESIAN_POINT('',(-0.00671320730991327,-0.0132725808828242,-0.00265795210955161));
#21260=CARTESIAN_POINT('',(-0.00646238122194688,-0.0132904879587329,-0.00329059036997));
#21261=CARTESIAN_POINT('',(-0.00612244238603927,-0.0133083950346416,-0.00388795992802378));
#21262=CARTESIAN_POINT('',(-0.00510304022134952,-0.0133521677772168,-0.00520211974340619));
#21263=CARTESIAN_POINT('',(-0.00433982575873794,-0.0133780334438831,-0.00585398946211112));
#21264=CARTESIAN_POINT('',(-0.00261729966649422,-0.0134297647772161,-0.00680097470695842));
#21265=CARTESIAN_POINT('',(-0.00165798803686209,-0.0134556304438826,-0.00709609023310079));
#21266=CARTESIAN_POINT('',(0.000298946322206539,-0.0135073617772158,-0.00728106935844134));
#21267=CARTESIAN_POINT('',(0.00129656905164304,-0.0135332274438825,-0.00717093295763951));
#21268=CARTESIAN_POINT('',(0.00316602273333922,-0.0135849587772159,-0.00656351231195381));
#21269=CARTESIAN_POINT('',(0.00403785368559892,-0.0136108244438827,-0.00606622806706994));
#21270=CARTESIAN_POINT('',(0.00551231653546556,-0.0136625557772162,-0.00476631369613314));
#21271=CARTESIAN_POINT('',(0.0061149484330725,-0.0136884214438831,-0.0039636835700802));
#21272=CARTESIAN_POINT('',(0.00695188557484636,-0.0137401527772168,-0.00218510178251919));
#21273=CARTESIAN_POINT('',(0.00718619081901328,-0.0137660184438837,-0.00120915012101113));
#21274=CARTESIAN_POINT('',(0.00724793366754968,-0.0138177497772174,0.000755539484837897));
#21275=CARTESIAN_POINT('',(0.00707537127191915,-0.0138436154438843,0.00174427742917886));
#21276=CARTESIAN_POINT('',(0.00635176375065145,-0.0138953467772181,0.00357190140420363));
#21277=CARTESIAN_POINT('',(0.00580071862501427,-0.013921212443885,0.00441078743488744));
#21278=CARTESIAN_POINT('',(0.00441078744172532,-0.0139729437772188,0.00580071863188773));
#21279=CARTESIAN_POINT('',(0.00357190138407354,-0.0139988094438857,0.00635176379820421));
#21280=CARTESIAN_POINT('',(0.00174427744926234,-0.0140505407772194,0.00707537122438483));
#21281=CARTESIAN_POINT('',(0.000755539572102914,-0.0140764064438862,0.00724793348424898));
#21282=CARTESIAN_POINT('',(-0.00120915020832567,-0.0141281377772198,0.00718619100231241));
#21283=CARTESIAN_POINT('',(-0.00218510211159483,-0.0141540034438866,0.00695188626051167));
#21284=CARTESIAN_POINT('',(-0.00396368324104856,-0.01420573477722,0.00611494774738647));
#21285=CARTESIAN_POINT('',(-0.00476631246723314,-0.0142316004438867,0.005512313976062));
#21286=CARTESIAN_POINT('',(-0.00606622929600128,-0.0142833317772199,0.00403785624496693));
#21287=CARTESIAN_POINT('',(-0.00656351689858486,-0.0143091974438864,0.00316603228519632));
#21288=CARTESIAN_POINT('',(-0.00717092837102258,-0.0143609287772193,0.00129655949974247));
#21289=CARTESIAN_POINT('',(-0.00728105224087672,-0.0143867944438857,0.000298910674059226));
#21290=CARTESIAN_POINT('',(-0.00712455998459551,-0.0144305672297369,-0.00135690104140363));
#21291=CARTESIAN_POINT('',(-0.00696343650502349,-0.0144484743489216,-0.00202507044701344));
#21292=CARTESIAN_POINT('',(-0.0067132091284259,-0.0144663814681063,-0.00265794752286045));
#21293=CARTESIAN_POINT('',(-0.00656825122483005,-0.013207999772273,-0.00260055982083585));
#21294=CARTESIAN_POINT('',(-0.00632284114236892,-0.0132259068481817,-0.00321953773065421));
#21295=CARTESIAN_POINT('',(-0.00599024249432473,-0.0132438139240904,-0.00380400848363825));
#21296=CARTESIAN_POINT('',(-0.00499285194645196,-0.0132875866666655,-0.00508979207686375));
#21297=CARTESIAN_POINT('',(-0.00424611732357595,-0.0133134523333319,-0.00572758618639327));
#21298=CARTESIAN_POINT('',(-0.00256078517265693,-0.0133651836666649,-0.00665412348923796));
#21299=CARTESIAN_POINT('',(-0.0016221876446139,-0.0133910493333314,-0.00694286668255311));
#21300=CARTESIAN_POINT('',(0.000292491272255514,-0.0134427806666646,-0.00712385161427001));
#21301=CARTESIAN_POINT('',(0.0012685726610819,-0.0134686463333313,-0.00701609335267175));
#21302=CARTESIAN_POINT('',(0.0030976598421722,-0.0135203776666647,-0.00642178854189664));
#21303=CARTESIAN_POINT('',(0.00395066563443611,-0.0135462433333314,-0.00593524199271978));
#21304=CARTESIAN_POINT('',(0.00539329089126407,-0.013597974666665,-0.00466339624672714));
#21305=CARTESIAN_POINT('',(0.00598291035582811,-0.0136238403333319,-0.00387809704991136));
#21306=CARTESIAN_POINT('',(0.00680177578821901,-0.0136755716666656,-0.00213791959593088));
#21307=CARTESIAN_POINT('',(0.00703102175604588,-0.0137014373333324,-0.00118304133876618));
#21308=CARTESIAN_POINT('',(0.00709143141149102,-0.0137531686666662,0.000739225368381796));
#21309=CARTESIAN_POINT('',(0.00692259509910929,-0.0137790343333331,0.00170661381836508));
#21310=CARTESIAN_POINT('',(0.00621461219787453,-0.0138307656666669,0.00349477450792977));
#21311=CARTESIAN_POINT('',(0.0056754656090215,-0.0138566313333338,0.00431554674751117));
#21312=CARTESIAN_POINT('',(0.0043155467542014,-0.0139083626666676,0.00567546561574654));
#21313=CARTESIAN_POINT('',(0.00349477448823434,-0.0139342283333345,0.0062146122444005));
#21314=CARTESIAN_POINT('',(0.0017066138380149,-0.0139859596666682,0.00692259505260138));
#21315=CARTESIAN_POINT('',(0.00073922545376252,-0.014011825333335,0.00709143123214829));
#21316=CARTESIAN_POINT('',(-0.00118304142419538,-0.0140635566666686,0.00703102193538709));
#21317=CARTESIAN_POINT('',(-0.0021379199179009,-0.0140894223333354,0.00680177645907898));
#21318=CARTESIAN_POINT('',(-0.0038780967279844,-0.0141411536666688,0.00598290968494787));
#21319=CARTESIAN_POINT('',(-0.00466339504436237,-0.0141670193333355,0.00539328838712488));
#21320=CARTESIAN_POINT('',(-0.0059352431951152,-0.0142187506666686,0.00395066813854053));
#21321=CARTESIAN_POINT('',(-0.00642179302949006,-0.0142446163333352,0.00309766918777917));
#21322=CARTESIAN_POINT('',(-0.00701608886509214,-0.0142963476666681,0.00126856331543239));
#21323=CARTESIAN_POINT('',(-0.00712383486631935,-0.0143222133333345,0.000292456393846961));
#21324=CARTESIAN_POINT('',(-0.00697072169603521,-0.0143659861191856,-0.00132760192196235));
#21325=CARTESIAN_POINT('',(-0.00681307730294682,-0.0143838932383704,-0.00198134376459991));
#21326=CARTESIAN_POINT('',(-0.00656825300407612,-0.0144018003575551,-0.00260055533318361));
#21327=CARTESIAN_POINT('',(-0.00627833905466362,-0.013207999772273,-0.00248577524340433));
#21328=CARTESIAN_POINT('',(-0.00604376098321297,-0.0132259068481817,-0.00307743245202264));
#21329=CARTESIAN_POINT('',(-0.00572584271089564,-0.0132438139240904,-0.00363610559486718));
#21330=CARTESIAN_POINT('',(-0.00477247539665684,-0.0132875866666655,-0.00486513674377885));
#21331=CARTESIAN_POINT('',(-0.00405870045325199,-0.0133134523333319,-0.00547477963495758));
#21332=CARTESIAN_POINT('',(-0.00244775618498232,-0.0133651836666649,-0.00636042105379704));
#21333=CARTESIAN_POINT('',(-0.00155058686011751,-0.0133910493333314,-0.00663641958145776));
#21334=CARTESIAN_POINT('',(0.000279581172353464,-0.0134427806666646,-0.00680941612592736));
#21335=CARTESIAN_POINT('',(0.00121257987995962,-0.0134686463333313,-0.00670641414273624));
#21336=CARTESIAN_POINT('',(0.00296093405983814,-0.0135203776666647,-0.00613834100178228));
#21337=CARTESIAN_POINT('',(0.0037762895321105,-0.0135462433333314,-0.00567326984401944));
#21338=CARTESIAN_POINT('',(0.0051552396028611,-0.013597974666665,-0.00445756134791514));
#21339=CARTESIAN_POINT('',(0.00571883420133933,-0.0136238403333319,-0.00370692400957368));
#21340=CARTESIAN_POINT('',(0.00650155621496433,-0.0136755716666656,-0.00204355522275425));
#21341=CARTESIAN_POINT('',(0.00672068363011109,-0.0137014373333324,-0.0011308237742763));
#21342=CARTESIAN_POINT('',(0.00677842689937372,-0.0137531686666662,0.000706597135469592));
#21343=CARTESIAN_POINT('',(0.00661704275348959,-0.0137790343333331,0.00163128659673753));
#21344=CARTESIAN_POINT('',(0.00594030909232071,-0.0138307656666669,0.00334052071538205));
#21345=CARTESIAN_POINT('',(0.00542495957703595,-0.0138566313333338,0.00412506537275864));
#21346=CARTESIAN_POINT('',(0.00412506537915357,-0.0139083626666676,0.00542495958346416));
#21347=CARTESIAN_POINT('',(0.00334052069655595,-0.0139342283333345,0.0059403091367931));
#21348=CARTESIAN_POINT('',(0.00163128661552003,-0.0139859596666682,0.00661704270903446));
#21349=CARTESIAN_POINT('',(0.000706597217081738,-0.014011825333335,0.00677842672794689));
#21350=CARTESIAN_POINT('',(-0.0011308238559348,-0.0140635566666686,0.00672068380153647));
#21351=CARTESIAN_POINT('',(-0.00204355553051304,-0.0140894223333354,0.0065015568562136));
#21352=CARTESIAN_POINT('',(-0.00370692370185607,-0.0141411536666688,0.00571883356007068));
#21353=CARTESIAN_POINT('',(-0.00445756019862085,-0.0141670193333355,0.00515523720925063));
#21354=CARTESIAN_POINT('',(-0.00567327099334305,-0.0142187506666686,0.00377629192568772));
#21355=CARTESIAN_POINT('',(-0.00613834529130047,-0.0142446163333352,0.00296094299294487));
#21356=CARTESIAN_POINT('',(-0.00670640985323126,-0.0142963476666681,0.00121257094681222));
#21357=CARTESIAN_POINT('',(-0.00680940011720462,-0.0143222133333345,0.000279547833422429));
#21358=CARTESIAN_POINT('',(-0.00666304511891462,-0.0143659861191856,-0.0012690036830798));
#21359=CARTESIAN_POINT('',(-0.0065123588987935,-0.0143838932383704,-0.00189389039977284));
#21360=CARTESIAN_POINT('',(-0.0062783407553766,-0.0144018003575551,-0.00248577095382993));
#21361=CARTESIAN_POINT('',(-0.00613338296958041,-0.0132725808828242,-0.00242838295468858));
#21362=CARTESIAN_POINT('',(-0.005904220903635,-0.0132904879587329,-0.00300637981270685));
#21363=CARTESIAN_POINT('',(-0.0055936428191811,-0.0133083950346417,-0.00355215415048165));
#21364=CARTESIAN_POINT('',(-0.00466228712175929,-0.0133521677772168,-0.00475280907723641));
#21365=CARTESIAN_POINT('',(-0.00396499201809001,-0.0133780334438831,-0.00534837635923974));
#21366=CARTESIAN_POINT('',(-0.00239124169114502,-0.0134297647772161,-0.00621356983607658));
#21367=CARTESIAN_POINT('',(-0.00151478646786932,-0.0134556304438826,-0.00648319603091008));
#21368=CARTESIAN_POINT('',(0.000273126122402439,-0.0135073617772158,-0.00665219838175603));
#21369=CARTESIAN_POINT('',(0.00118458348939848,-0.0135332274438825,-0.00655157453776848));
#21370=CARTESIAN_POINT('',(0.00289257116867111,-0.0135849587772159,-0.0059966172317251));
#21371=CARTESIAN_POINT('',(0.0036891014809477,-0.0136108244438827,-0.00554228376966928));
#21372=CARTESIAN_POINT('',(0.00503621395865961,-0.0136625557772162,-0.00435464389850914));
#21373=CARTESIAN_POINT('',(0.00558679612409495,-0.0136884214438831,-0.00362133748940483));
#21374=CARTESIAN_POINT('',(0.00635144642833699,-0.0137401527772168,-0.00199637303616594));
#21375=CARTESIAN_POINT('',(0.0065655145671437,-0.0137660184438837,-0.00110471499203136));
#21376=CARTESIAN_POINT('',(0.00662192464331508,-0.0138177497772174,0.00069028301901349));
#21377=CARTESIAN_POINT('',(0.00646426658067975,-0.0138436154438843,0.00159362298592375));
#21378=CARTESIAN_POINT('',(0.0058031575395438,-0.0138953467772181,0.0032633938191082));
#21379=CARTESIAN_POINT('',(0.00529970656104318,-0.0139212124438851,0.00402982468538238));
#21380=CARTESIAN_POINT('',(0.00402982469162966,-0.0139729437772188,0.00529970656732298));
#21381=CARTESIAN_POINT('',(0.00326339380071675,-0.0139988094438857,0.0058031575829894));
#21382=CARTESIAN_POINT('',(0.0015936230042726,-0.0140505407772194,0.00646426653725101));
#21383=CARTESIAN_POINT('',(0.00069028309874135,-0.0140764064438862,0.0066219244758462));
#21384=CARTESIAN_POINT('',(-0.0011047150718045,-0.0141281377772198,0.00656551473461115));
#21385=CARTESIAN_POINT('',(-0.00199637333681911,-0.0141540034438866,0.00635144705478091));
#21386=CARTESIAN_POINT('',(-0.0036213371887919,-0.01420573477722,0.00558679549763209));
#21387=CARTESIAN_POINT('',(-0.00435464277575009,-0.0142316004438867,0.0050362116203135));
#21388=CARTESIAN_POINT('',(-0.00554228489245697,-0.0142833317772199,0.00368910381926132));
#21389=CARTESIAN_POINT('',(-0.00599662142220567,-0.0143091974438864,0.00289257989552772));
#21390=CARTESIAN_POINT('',(-0.00655157034730081,-0.0143609287772193,0.00118457476250214));
#21391=CARTESIAN_POINT('',(-0.00665218274264726,-0.0143867944438857,0.000273093553210163));
#21392=CARTESIAN_POINT('',(-0.00650920683035433,-0.0144305672297368,-0.00123970456363852));
#21393=CARTESIAN_POINT('',(-0.00636199969671684,-0.0144484743489216,-0.00185016371735931));
#21394=CARTESIAN_POINT('',(-0.00613338463102684,-0.0144663814681063,-0.00242837876415309));
#21395=CARTESIAN_POINT('',(-0.00592838410810722,-0.0134930745863413,-0.00234721800161112));
#21396=CARTESIAN_POINT('',(-0.00570688143060122,-0.01351098166225,-0.00290589620654406));
#21397=CARTESIAN_POINT('',(-0.00540668393937414,-0.0135288887381587,-0.00343342887925082));
#21398=CARTESIAN_POINT('',(-0.00450645736898467,-0.0135726614807338,-0.00459395376778235));
#21399=CARTESIAN_POINT('',(-0.00383246827817518,-0.0135985271474002,-0.00516961513239117));
#21400=CARTESIAN_POINT('',(-0.00231131812748966,-0.0136502584807331,-0.0060058908523253));
#21401=CARTESIAN_POINT('',(-0.00146415706761364,-0.0136761241473997,-0.0062665052076506));
#21402=CARTESIAN_POINT('',(0.000263997303215905,-0.0137278554807329,-0.00642985891570324));
#21403=CARTESIAN_POINT('',(0.00114499061416943,-0.0137537211473995,-0.00633259826843059));
#21404=CARTESIAN_POINT('',(0.00279589144081966,-0.013805452480733,-0.0057961895539996));
#21405=CARTESIAN_POINT('',(0.00356579895651638,-0.0138313181473997,-0.00535704148684126));
#21406=CARTESIAN_POINT('',(0.00486788627835968,-0.0138830494807333,-0.00420909664575433));
#21407=CARTESIAN_POINT('',(0.00540006608450626,-0.0139089151474001,-0.00350029987182574));
#21408=CARTESIAN_POINT('',(0.00613915913224366,-0.0139606464807339,-0.00192964734799033));
#21409=CARTESIAN_POINT('',(0.00634607237383448,-0.0139865121474007,-0.00106779159808351));
#21410=CARTESIAN_POINT('',(0.00640059703025495,-0.0140382434807345,0.000667211374263139));
#21411=CARTESIAN_POINT('',(0.0062482084450846,-0.0140641091474014,0.00154035859670296));
#21412=CARTESIAN_POINT('',(0.00560919595350616,-0.0141158404807352,0.00315431991637396));
#21413=CARTESIAN_POINT('',(0.00512257204709807,-0.0141417061474021,0.00389513401360513));
#21414=CARTESIAN_POINT('',(0.0038951340196436,-0.0141934374807359,0.00512257205316798));
#21415=CARTESIAN_POINT('',(0.00315431989859721,-0.0142193031474028,0.00560919599549966));
#21416=CARTESIAN_POINT('',(0.00154035861443853,-0.0142710344807365,0.00624820840310741));
#21417=CARTESIAN_POINT('',(0.000667211451326215,-0.0142969001474033,0.00640059686838347));
#21418=CARTESIAN_POINT('',(-0.00106779167519036,-0.0143486314807369,0.0063460725357046));
#21419=CARTESIAN_POINT('',(-0.00192964763859463,-0.0143744971474037,0.00613915973774967));
#21420=CARTESIAN_POINT('',(-0.00350029958126033,-0.0144262284807371,0.00540006547898196));
#21421=CARTESIAN_POINT('',(-0.00420909556052176,-0.0144520941474037,0.00486788401816917));
#21422=CARTESIAN_POINT('',(-0.00535704257210151,-0.0145038254807369,0.00356580121667547));
#21423=CARTESIAN_POINT('',(-0.00579619360441982,-0.0145296911474035,0.00279589987599456));
#21424=CARTESIAN_POINT('',(-0.00633259421802284,-0.0145814224807364,0.00114498217895613));
#21425=CARTESIAN_POINT('',(-0.00642984379930755,-0.0146072881474028,0.000263965822598622));
#21426=CARTESIAN_POINT('',(-0.0062916466362601,-0.0146510609332539,-0.00119826935155907));
#21427=CARTESIAN_POINT('',(-0.00614935967391244,-0.0146689680524387,-0.00178832485005251));
#21428=CARTESIAN_POINT('',(-0.00592838571402237,-0.0146868751716234,-0.00234721395113782));
#21429=CARTESIAN_POINT('',(-0.00586834133171724,-0.0136489871793071,-0.00232344533724942));
#21430=CARTESIAN_POINT('',(-0.0056490820371454,-0.0136668942552158,-0.00287646523969706));
#21431=CARTESIAN_POINT('',(-0.00535192495128173,-0.0136848013311246,-0.00339865505240552));
#21432=CARTESIAN_POINT('',(-0.0044608158911076,-0.0137285740736997,-0.00454742612487075));
#21433=CARTESIAN_POINT('',(-0.00379365297342232,-0.0137544397403661,-0.00511725718126045));
#21434=CARTESIAN_POINT('',(-0.0022879090576716,-0.013806171073699,-0.00594506308629447));
#21435=CARTESIAN_POINT('',(-0.00144932805960616,-0.0138320367403655,-0.00620303793493879));
#21436=CARTESIAN_POINT('',(0.000261323533980394,-0.0138837680736987,-0.00636473719382178));
#21437=CARTESIAN_POINT('',(0.00113339412950151,-0.0139096337403654,-0.00626846160406045));
#21438=CARTESIAN_POINT('',(0.00276757460413524,-0.0139613650736988,-0.00573748564633127));
#21439=CARTESIAN_POINT('',(0.00352968448324787,-0.0139872307403656,-0.00530278527836341));
#21440=CARTESIAN_POINT('',(0.00481858424226122,-0.0140389620736992,-0.00416646684240552));
#21441=CARTESIAN_POINT('',(0.00534537412216196,-0.014064827740366,-0.00346484877441549));
#21442=CARTESIAN_POINT('',(0.00607698162277768,-0.0141165590736997,-0.00191010384640304));
#21443=CARTESIAN_POINT('',(0.00628179924349266,-0.0141424247403666,-0.00105697698638061));
#21444=CARTESIAN_POINT('',(0.00633577167325347,-0.0141941560737004,0.00066045384596889));
#21445=CARTESIAN_POINT('',(0.0061849264822993,-0.0142200217403673,0.00152475781829596));
#21446=CARTESIAN_POINT('',(0.00555238592024542,-0.0142717530737011,0.00312237290991359));
#21447=CARTESIAN_POINT('',(0.00507069054914572,-0.014297618740368,0.00385568402920414));
#21448=CARTESIAN_POINT('',(0.00385568403518145,-0.0143493500737018,0.00507069055515415));
#21449=CARTESIAN_POINT('',(0.00312237289231688,-0.0143752157403686,0.00555238596181362));
#21450=CARTESIAN_POINT('',(0.00152475783585189,-0.0144269470737023,0.00618492644074726));
#21451=CARTESIAN_POINT('',(0.000660453922251468,-0.0144528127403692,0.00633577151302143));
#21452=CARTESIAN_POINT('',(-0.00105697706270652,-0.0145045440737028,0.00628179940372336));
#21453=CARTESIAN_POINT('',(-0.00191010413406409,-0.0145304097403695,0.00607698222215111));
#21454=CARTESIAN_POINT('',(-0.00346484848679293,-0.0145821410737029,0.00534537352277042));
#21455=CARTESIAN_POINT('',(-0.00416646576816421,-0.0146080067403696,0.00481858200496197));
#21456=CARTESIAN_POINT('',(-0.00530278635263212,-0.0146597380737028,0.00352968672051603));
#21457=CARTESIAN_POINT('',(-0.00573748965572876,-0.0146856037403693,0.00276758295387853));
#21458=CARTESIAN_POINT('',(-0.0062684575946753,-0.0147373350737023,0.00113338577972019));
#21459=CARTESIAN_POINT('',(-0.0063647222305252,-0.0147632007403686,0.000261292372199345));
#21460=CARTESIAN_POINT('',(-0.00622792473072616,-0.0148069735262198,-0.0011861332589209));
#21461=CARTESIAN_POINT('',(-0.00608707885318468,-0.0148248806454046,-0.00177021266515924));
#21462=CARTESIAN_POINT('',(-0.00586834292136765,-0.0148427877645893,-0.00232344132779938));
#21463=CARTESIAN_POINT('',(-0.00586834133171724,-0.0138052053248561,-0.00232344533724942));
#21464=CARTESIAN_POINT('',(-0.0056490820371454,-0.0138231124007648,-0.00287646523969706));
#21465=CARTESIAN_POINT('',(-0.00535192495128173,-0.0138410194766736,-0.00339865505240552));
#21466=CARTESIAN_POINT('',(-0.00446081589110761,-0.0138847922192487,-0.00454742612487075));
#21467=CARTESIAN_POINT('',(-0.00379365297342232,-0.0139106578859151,-0.00511725718126046));
#21468=CARTESIAN_POINT('',(-0.0022879090576716,-0.013962389219248,-0.00594506308629448));
#21469=CARTESIAN_POINT('',(-0.00144932805960616,-0.0139882548859145,-0.00620303793493879));
#21470=CARTESIAN_POINT('',(0.000261323533980396,-0.0140399862192477,-0.00636473719382177));
#21471=CARTESIAN_POINT('',(0.00113339412950151,-0.0140658518859144,-0.00626846160406045));
#21472=CARTESIAN_POINT('',(0.00276757460413524,-0.0141175832192478,-0.00573748564633127));
#21473=CARTESIAN_POINT('',(0.00352968448324786,-0.0141434488859146,-0.00530278527836341));
#21474=CARTESIAN_POINT('',(0.00481858424226122,-0.0141951802192481,-0.00416646684240552));
#21475=CARTESIAN_POINT('',(0.00534537412216197,-0.014221045885915,-0.00346484877441549));
#21476=CARTESIAN_POINT('',(0.00607698162277769,-0.0142727772192487,-0.00191010384640303));
#21477=CARTESIAN_POINT('',(0.00628179924349266,-0.0142986428859156,-0.00105697698638061));
#21478=CARTESIAN_POINT('',(0.00633577167325347,-0.0143503742192493,0.000660453845968888));
#21479=CARTESIAN_POINT('',(0.0061849264822993,-0.0143762398859163,0.00152475781829596));
#21480=CARTESIAN_POINT('',(0.00555238592024543,-0.0144279712192501,0.00312237290991359));
#21481=CARTESIAN_POINT('',(0.00507069054914573,-0.014453836885917,0.00385568402920414));
#21482=CARTESIAN_POINT('',(0.00385568403518145,-0.0145055682192507,0.00507069055515416));
#21483=CARTESIAN_POINT('',(0.00312237289231688,-0.0145314338859176,0.00555238596181362));
#21484=CARTESIAN_POINT('',(0.00152475783585189,-0.0145831652192513,0.00618492644074726));
#21485=CARTESIAN_POINT('',(0.000660453922251466,-0.0146090308859181,0.00633577151302142));
#21486=CARTESIAN_POINT('',(-0.00105697706270652,-0.0146607622192517,0.00628179940372335));
#21487=CARTESIAN_POINT('',(-0.00191010413406409,-0.0146866278859185,0.00607698222215111));
#21488=CARTESIAN_POINT('',(-0.00346484848679293,-0.0147383592192519,0.00534537352277042));
#21489=CARTESIAN_POINT('',(-0.00416646576816421,-0.0147642248859186,0.00481858200496197));
#21490=CARTESIAN_POINT('',(-0.00530278635263212,-0.0148159562192518,0.00352968672051603));
#21491=CARTESIAN_POINT('',(-0.00573748965572876,-0.0148418218859183,0.00276758295387854));
#21492=CARTESIAN_POINT('',(-0.0062684575946753,-0.0148935532192512,0.0011333857797202));
#21493=CARTESIAN_POINT('',(-0.0063647222305252,-0.0149194188859176,0.000261292372199344));
#21494=CARTESIAN_POINT('',(-0.00622792473072616,-0.0149631916717688,-0.00118613325892091));
#21495=CARTESIAN_POINT('',(-0.00608707885318469,-0.0149810987909535,-0.00177021266515924));
#21496=CARTESIAN_POINT('',(-0.00586834292136765,-0.0149990059101383,-0.00232344132779938));
#21497=CARTESIAN_POINT('',(-0.00586834156232308,-0.0138055108774392,-0.00232344542855291));
#21498=CARTESIAN_POINT('',(-0.0056490822591351,-0.0138234179533479,-0.00287646535273235));
#21499=CARTESIAN_POINT('',(-0.00535192516159416,-0.0138413250292567,-0.00339865518596109));
#21500=CARTESIAN_POINT('',(-0.00446081606640248,-0.0138850977718318,-0.00454742630356912));
#21501=CARTESIAN_POINT('',(-0.00379365312249997,-0.0139109634384982,-0.00511725738235125));
#21502=CARTESIAN_POINT('',(-0.00228790914757864,-0.0139626947718311,-0.00594506331991522));
#21503=CARTESIAN_POINT('',(-0.00144932811655982,-0.0139885604384977,-0.00620303817869707));
#21504=CARTESIAN_POINT('',(0.000261323544249522,-0.0140402917718309,-0.00636473744393428));
#21505=CARTESIAN_POINT('',(0.00113339417404004,-0.0140661574384975,-0.00626846185038965));
#21506=CARTESIAN_POINT('',(0.0027675747128915,-0.0141178887718309,-0.00573748587179492));
#21507=CARTESIAN_POINT('',(0.00352968462195244,-0.0141437544384977,-0.00530278548674482));
#21508=CARTESIAN_POINT('',(0.00481858443161518,-0.0141954857718313,-0.00416646700613348));
#21509=CARTESIAN_POINT('',(0.00534537433221698,-0.0142213514384981,-0.00346484891057225));
#21510=CARTESIAN_POINT('',(0.00607698186158238,-0.0142730827718318,-0.00191010392146361));
#21511=CARTESIAN_POINT('',(0.00628179949034599,-0.0142989484384987,-0.00105697702791621));
#21512=CARTESIAN_POINT('',(0.00633577192222773,-0.0143506797718325,0.000660453871922476));
#21513=CARTESIAN_POINT('',(0.00618492672534586,-0.0143765454384994,0.00152475787821375));
#21514=CARTESIAN_POINT('',(0.00555238613843529,-0.0144282767718332,0.00312237303261221));
#21515=CARTESIAN_POINT('',(0.00507069074840661,-0.0144541424385001,0.00385568418071939));
#21516=CARTESIAN_POINT('',(0.00385568418669671,-0.0145058737718339,0.00507069075441504));
#21517=CARTESIAN_POINT('',(0.00312237301501551,-0.0145317394385008,0.00555238618000349));
#21518=CARTESIAN_POINT('',(0.00152475789576968,-0.0145834707718345,0.00618492668379381));
#21519=CARTESIAN_POINT('',(0.000660453948205057,-0.0146093364385013,0.00633577176199567));
#21520=CARTESIAN_POINT('',(-0.00105697710424212,-0.0146610677718349,0.00628179965057668));
#21521=CARTESIAN_POINT('',(-0.00191010420912468,-0.0146869334385016,0.00607698246095582));
#21522=CARTESIAN_POINT('',(-0.00346484862294968,-0.0147386647718351,0.0053453737328254));
#21523=CARTESIAN_POINT('',(-0.00416646593189213,-0.0147645304385017,0.00481858219431584));
#21524=CARTESIAN_POINT('',(-0.00530278656101357,-0.0148162617718349,0.0035296868592207));
#21525=CARTESIAN_POINT('',(-0.00573748988119257,-0.0148421274385014,0.00276758306263513));
#21526=CARTESIAN_POINT('',(-0.00626845784100435,-0.0148938587718344,0.0011333858242584));
#21527=CARTESIAN_POINT('',(-0.00636472248063712,-0.0149197244385008,0.000261292382467245));
#21528=CARTESIAN_POINT('',(-0.0062279249754624,-0.0149634972243519,-0.00118613330553191));
#21529=CARTESIAN_POINT('',(-0.00608707909238616,-0.0149814043435367,-0.00177021273472257));
#21530=CARTESIAN_POINT('',(-0.00586834315197355,-0.0149993114627214,-0.00232344141910271));
#21531=CARTESIAN_POINT('',(-0.00586834202340238,-0.0138058164296786,-0.00232344561110749));
#21532=CARTESIAN_POINT('',(-0.00564908270298706,-0.0138237235055873,-0.00287646557873805));
#21533=CARTESIAN_POINT('',(-0.00535192558209831,-0.0138416305814961,-0.00339865545299558));
#21534=CARTESIAN_POINT('',(-0.00446081641689162,-0.0138854033240712,-0.00454742666086328));
#21535=CARTESIAN_POINT('',(-0.00379365342056969,-0.0139112689907376,-0.00511725778441739));
#21536=CARTESIAN_POINT('',(-0.00228790932734111,-0.0139630003240705,-0.0059450637870226));
#21537=CARTESIAN_POINT('',(-0.00144932823043444,-0.0139888659907371,-0.0062030386660737));
#21538=CARTESIAN_POINT('',(0.000261323564781878,-0.0140405973240703,-0.00636473794401572));
#21539=CARTESIAN_POINT('',(0.00113339426309154,-0.0140664629907369,-0.00626846234290666));
#21540=CARTESIAN_POINT('',(0.0027675749303416,-0.0141181943240703,-0.00573748632259282));
#21541=CARTESIAN_POINT('',(0.003529684899282,-0.0141440599907371,-0.00530278590338803));
#21542=CARTESIAN_POINT('',(0.0048185848102144,-0.0141957913240707,-0.00416646733349543));
#21543=CARTESIAN_POINT('',(0.00534537475220642,-0.0142216569907375,-0.00346484918280762));
#21544=CARTESIAN_POINT('',(0.00607698233905469,-0.0142733883240712,-0.00191010407154168));
#21545=CARTESIAN_POINT('',(0.00628179998391094,-0.0142992539907381,-0.00105697711096356));
#21546=CARTESIAN_POINT('',(0.00633577242003333,-0.0143509853240719,0.000660453923814754));
#21547=CARTESIAN_POINT('',(0.00618492721129946,-0.0143768509907388,0.00152475799801494));
#21548=CARTESIAN_POINT('',(0.00555238657468978,-0.0144285823240726,0.00312237327793903));
#21549=CARTESIAN_POINT('',(0.00507069114681398,-0.0144544479907395,0.00385568448366294));
#21550=CARTESIAN_POINT('',(0.00385568448964025,-0.0145061793240733,0.00507069115282241));
#21551=CARTESIAN_POINT('',(0.00312237326034233,-0.0145320449907402,0.00555238661625798));
#21552=CARTESIAN_POINT('',(0.00152475801557087,-0.0145837763240739,0.00618492716974741));
#21553=CARTESIAN_POINT('',(0.000660454000097341,-0.0146096419907407,0.00633577225980127));
#21554=CARTESIAN_POINT('',(-0.00105697718728948,-0.0146613733240743,0.00628180014414165));
#21555=CARTESIAN_POINT('',(-0.00191010435920278,-0.014687238990741,0.00607698293842818));
#21556=CARTESIAN_POINT('',(-0.00346484889518503,-0.0147389703240745,0.0053453741528148));
#21557=CARTESIAN_POINT('',(-0.00416646625925399,-0.0147648359907411,0.00481858257291489));
#21558=CARTESIAN_POINT('',(-0.00530278697765686,-0.0148165673240743,0.00352968713655043));
#21559=CARTESIAN_POINT('',(-0.00573749033199078,-0.0148424329907408,0.00276758328008588));
#21560=CARTESIAN_POINT('',(-0.00626845833352104,-0.0148941643240738,0.00113338591330924));
#21561=CARTESIAN_POINT('',(-0.00636472298071739,-0.0149200299907402,0.000261292402997153));
#21562=CARTESIAN_POINT('',(-0.0062279254647944,-0.0149638027765913,-0.00118613339872715));
#21563=CARTESIAN_POINT('',(-0.00608707957065181,-0.0149817098957761,-0.00177021287380931));
#21564=CARTESIAN_POINT('',(-0.00586834361305298,-0.0149996170149608,-0.00232344160165698));
#21565=CARTESIAN_POINT('',(-0.00697824894777635,-0.0138049000966563,-0.00276288972699073));
#21566=CARTESIAN_POINT('',(-0.00697824903105753,-0.0136489874497574,-0.00276288975996415));
#21567=CARTESIAN_POINT('',(-0.00685816354230486,-0.0133371620879765,-0.00271534445659099));
#21568=CARTESIAN_POINT('',(-0.0064232951405584,-0.0131434186147288,-0.00254316753244141));
#21569=CARTESIAN_POINT('',(-0.0059884267383218,-0.0133371620867462,-0.00237099060809777));
#21570=CARTESIAN_POINT('',(-0.00586834124883921,-0.0136489874481873,-0.00232344530443563));
#21571=CARTESIAN_POINT('',(-0.00586834133171732,-0.0138049000950862,-0.00232344533724946));
#21572=CARTESIAN_POINT('',(-0.0081026,0.0149987,0.00954659375251877));
#21573=CARTESIAN_POINT('',(-0.00586852288100303,0.0149987,0.00232350619462048));
#21574=CARTESIAN_POINT('',(-0.00599813361737052,0.0149987,0.00199544445134711));
#21575=CARTESIAN_POINT('',(-0.00615036467398835,0.0149987,0.00149215405397291));
#21576=CARTESIAN_POINT('',(-0.00626888096798645,0.0149987,0.000816811812020128));
#21577=CARTESIAN_POINT('',(-0.00631571566898991,0.0149987,0.000271946568879761));
#21578=CARTESIAN_POINT('',(-0.00631979103216071,0.0149987,-0.000166419746807652));
#21579=CARTESIAN_POINT('',(-0.00629286640124922,0.0149987,-0.0006317674431288));
#21580=CARTESIAN_POINT('',(-0.00623449486695781,0.0149987,-0.00107869939733934));
#21581=CARTESIAN_POINT('',(-0.0061347047227266,0.0149987,-0.00155532379232996));
#21582=CARTESIAN_POINT('',(-0.0060338297040928,0.0149987,-0.00191460501928228));
#21583=CARTESIAN_POINT('',(-0.00590240684976963,0.0149987,-0.00229687646076972));
#21584=CARTESIAN_POINT('',(-0.00575311671963906,0.0149987,-0.00265615694245076));
#21585=CARTESIAN_POINT('',(-0.00556470003546006,0.0149987,-0.00303603777911812));
#21586=CARTESIAN_POINT('',(-0.00540951335031477,0.0149987,-0.00330813488594238));
#21587=CARTESIAN_POINT('',(-0.00516748245708881,0.0149987,-0.00369094054829892));
#21588=CARTESIAN_POINT('',(-0.00482982949957805,0.0149987,-0.00413835572156689));
#21589=CARTESIAN_POINT('',(-0.00446112385613488,0.0149987,-0.00453464678378625));
#21590=CARTESIAN_POINT('',(-0.00418584385722875,0.0149987,-0.00479017172870383));
#21591=CARTESIAN_POINT('',(-0.00401225692663932,0.0149987,-0.00493819821573241));
#21592=CARTESIAN_POINT('',(-0.00390829841184597,0.0149987,-0.00502401671172254));
#21593=CARTESIAN_POINT('',(-0.00368920130906923,0.0149987,-0.00519269073095229));
#21594=CARTESIAN_POINT('',(-0.00342976117916472,0.0149987,-0.00537492155999436));
#21595=CARTESIAN_POINT('',(-0.00307976849749122,0.0149987,-0.00559356980612197));
#21596=CARTESIAN_POINT('',(-0.00265202463847078,0.0149987,-0.00581741034134192));
#21597=CARTESIAN_POINT('',(-0.00203200389002907,0.0149987,-0.00608060728739528));
#21598=CARTESIAN_POINT('',(-0.00137560083704515,0.0149987,-0.00628233330086265));
#21599=CARTESIAN_POINT('',(-0.000449164143146347,0.0149987,-0.00643265513261176));
#21600=CARTESIAN_POINT('',(0.000282590277332738,0.0149987,-0.00645692920940098));
#21601=CARTESIAN_POINT('',(0.00112268962581157,0.0149987,-0.00638463486570212));
#21602=CARTESIAN_POINT('',(0.00174144901375654,0.0149987,-0.00625866853906934));
#21603=CARTESIAN_POINT('',(0.00239194599947828,0.0149987,-0.00606587477666004));
#21604=CARTESIAN_POINT('',(0.00290790460604307,0.0149987,-0.00584976292120319));
#21605=CARTESIAN_POINT('',(0.00330462789445912,0.0149987,-0.00564960698791436));
#21606=CARTESIAN_POINT('',(0.00361882339497395,0.0149987,-0.00546923879547015));
#21607=CARTESIAN_POINT('',(0.00384299450027782,0.0149987,-0.00532662824985322));
#21608=CARTESIAN_POINT('',(0.00416212926193885,0.0149987,-0.00510689346148155));
#21609=CARTESIAN_POINT('',(0.00453521879647297,0.0149987,-0.00481256371189878));
#21610=CARTESIAN_POINT('',(0.00488723381178878,0.0149987,-0.00448669065789026));
#21611=CARTESIAN_POINT('',(0.00512661788284246,0.0149987,-0.00423556252169337));
#21612=CARTESIAN_POINT('',(0.00525204938765184,0.0149987,-0.00409682965133543));
#21613=CARTESIAN_POINT('',(0.00536734521233373,0.0149987,-0.00396297362800762));
#21614=CARTESIAN_POINT('',(0.00539352292456894,0.0149987,-0.00393124136567307));
#21615=CARTESIAN_POINT('',(0.00546027930440312,0.0149987,-0.00385046561140097));
#21616=CARTESIAN_POINT('',(0.00556424825583872,0.0149987,-0.0037198945025107));
#21617=CARTESIAN_POINT('',(0.00572426624445618,0.0149987,-0.00350871218461249));
#21618=CARTESIAN_POINT('',(0.00589047976960149,0.0149987,-0.00327366681131062));
#21619=CARTESIAN_POINT('',(0.00602152779309136,0.0149987,-0.00308108272382827));
#21620=CARTESIAN_POINT('',(0.00613846929603434,0.0149987,-0.00290345021921962));
#21621=CARTESIAN_POINT('',(0.00619281986756365,0.0149987,-0.00282009893917783));
#21622=CARTESIAN_POINT('',(0.00627282434906237,0.0149987,-0.00269243691200387));
#21623=CARTESIAN_POINT('',(0.00630906243799169,0.0149987,-0.00264532479259586));
#21624=CARTESIAN_POINT('',(0.00635875497946399,0.0149987,-0.00260087005047891));
#21625=CARTESIAN_POINT('',(0.00642241978508077,0.0149987,-0.00256956131751183));
#21626=CARTESIAN_POINT('',(0.00645179410204332,0.0149987,-0.00259471707091186));
#21627=CARTESIAN_POINT('',(0.00643651691696919,0.0149987,-0.00269405563403255));
#21628=CARTESIAN_POINT('',(0.00639400553087227,0.0149987,-0.00288451905087659));
#21629=CARTESIAN_POINT('',(0.00632909652561322,0.0149987,-0.00308798541396548));
#21630=CARTESIAN_POINT('',(0.00623507620707644,0.0149987,-0.00333292149193221));
#21631=CARTESIAN_POINT('',(0.00614730154764063,0.0149987,-0.00352716105907205));
#21632=CARTESIAN_POINT('',(0.00608699524330738,0.0149987,-0.0036536273522041));
#21633=CARTESIAN_POINT('',(0.00597346390559083,0.0149987,-0.0038717266200523));
#21634=CARTESIAN_POINT('',(0.00582819366820487,0.0149987,-0.00412439000312725));
#21635=CARTESIAN_POINT('',(0.0056212361382006,0.0149987,-0.00444390717139348));
#21636=CARTESIAN_POINT('',(0.00539548072186256,0.0149987,-0.00474309520366593));
#21637=CARTESIAN_POINT('',(0.00519017052664321,0.0149987,-0.00498568766096538));
#21638=CARTESIAN_POINT('',(0.00505399676650015,0.0149987,-0.00513815523356757));
#21639=CARTESIAN_POINT('',(0.00481388210436201,0.0149987,-0.00538561010023584));
#21640=CARTESIAN_POINT('',(0.00451483722849798,0.0149987,-0.00566364051147178));
#21641=CARTESIAN_POINT('',(0.00410549859317541,0.0149987,-0.005996807984814));
#21642=CARTESIAN_POINT('',(0.00367483036801044,0.0149987,-0.00628612149675208));
#21643=CARTESIAN_POINT('',(0.00330025304143102,0.0149987,-0.0065013399358742));
#21644=CARTESIAN_POINT('',(0.00304000119389682,0.0149987,-0.00663802952057298));
#21645=CARTESIAN_POINT('',(0.00265721623275325,0.0149987,-0.00681524311387696));
#21646=CARTESIAN_POINT('',(0.00217007333390863,0.0149987,-0.007003890009028));
#21647=CARTESIAN_POINT('',(0.0015636341380728,0.0149987,-0.00718940436680364));
#21648=CARTESIAN_POINT('',(0.000788625433471163,0.0149987,-0.00732937468007596));
#21649=CARTESIAN_POINT('',(0.000188561236036738,0.0149987,-0.00737459670681537));
#21650=CARTESIAN_POINT('',(-0.000245356403268555,0.0149987,-0.00738295831685497));
#21651=CARTESIAN_POINT('',(-0.000770556059278252,0.0149987,-0.00735815400665872));
#21652=CARTESIAN_POINT('',(-0.00126821903781768,0.0149987,-0.00729702843855239));
#21653=CARTESIAN_POINT('',(-0.00175951251098515,0.0149987,-0.00720405474476678));
#21654=CARTESIAN_POINT('',(-0.00227858648456211,0.0149987,-0.00706449573405289));
#21655=CARTESIAN_POINT('',(-0.00266767376332445,0.0149987,-0.00693282703917595));
#21656=CARTESIAN_POINT('',(-0.00308118761978522,0.0149987,-0.00676681939138545));
#21657=CARTESIAN_POINT('',(-0.00346455142098867,0.0149987,-0.00658612068558278));
#21658=CARTESIAN_POINT('',(-0.00388165842624475,0.0149987,-0.00635436861091288));
#21659=CARTESIAN_POINT('',(-0.00413151223126944,0.0149987,-0.00619736451589457));
#21660=CARTESIAN_POINT('',(-0.00450649725080915,0.0149987,-0.00594334153252775));
#21661=CARTESIAN_POINT('',(-0.00493277186581828,0.0149987,-0.00560710240166229));
#21662=CARTESIAN_POINT('',(-0.00532982478874629,0.0149987,-0.00523458823734003));
#21663=CARTESIAN_POINT('',(-0.00563417246466138,0.0149987,-0.00490502780542735));
#21664=CARTESIAN_POINT('',(-0.00583180618591253,0.0149987,-0.00467408667637399));
#21665=CARTESIAN_POINT('',(-0.0060998993556408,0.0149987,-0.00432721456698508));
#21666=CARTESIAN_POINT('',(-0.00640306507679717,0.0149987,-0.00387861753812989));
#21667=CARTESIAN_POINT('',(-0.00673091292818374,0.0149987,-0.00331234831644476));
#21668=CARTESIAN_POINT('',(-0.00711251338688112,0.0149987,-0.00240915825510923));
#21669=CARTESIAN_POINT('',(-0.00735180985367311,0.0149987,-0.00156460169581665));
#21670=CARTESIAN_POINT('',(-0.00750881517846443,0.0149987,-0.00047852369279238));
#21671=CARTESIAN_POINT('',(-0.00751054978552773,0.0149987,0.000332880065926781));
#21672=CARTESIAN_POINT('',(-0.00742945849251632,0.0149987,0.00111231420612745));
#21673=CARTESIAN_POINT('',(-0.00728986753147895,0.0149987,0.00185434184076015));
#21674=CARTESIAN_POINT('',(-0.00712035040730489,0.0149987,0.00240373416514147));
#21675=CARTESIAN_POINT('',(-0.00697841856488692,0.0149987,0.00276294376766862));
#21676=CARTESIAN_POINT('',(-0.0069782482656729,0.0138058421337995,0.00276288935849655));
#21677=CARTESIAN_POINT('',(-0.00671751942982434,0.0138237492104805,0.00342050453854716));
#21678=CARTESIAN_POINT('',(-0.00636415961979208,0.0138416562871614,0.00404145858742542));
#21679=CARTESIAN_POINT('',(-0.00530451090786062,0.0138854290305087,0.00540750214106635));
#21680=CARTESIAN_POINT('',(-0.00451116434064711,0.0139112946971751,0.0060851080158756));
#21681=CARTESIAN_POINT('',(-0.00272063202088324,0.0139630260305081,0.00706948073154804));
#21682=CARTESIAN_POINT('',(-0.00172344626833288,0.0139888916971746,0.00737624757241125));
#21683=CARTESIAN_POINT('',(0.000310748878751736,0.0140406230305078,0.00756852976999031));
#21684=CARTESIAN_POINT('',(0.00134775827328599,0.0140664886971745,0.00745404512670618));
#21685=CARTESIAN_POINT('',(0.00329101896027998,0.0141182200305079,0.00682264319747595));
#21686=CARTESIAN_POINT('',(0.00419727025273972,0.0141440856971746,0.00630572591152988));
#21687=CARTESIAN_POINT('',(0.00572994566408194,0.0141958170305082,0.00495449024400156));
#21688=CARTESIAN_POINT('',(0.00635636978296444,0.014221682697175,0.00412017186241933));
#21689=CARTESIAN_POINT('',(0.00722634963912147,0.0142734140305088,0.00227137073928324));
#21690=CARTESIAN_POINT('',(0.00746990537639599,0.0142992796971756,0.00125688799772938));
#21691=CARTESIAN_POINT('',(0.00753408586475928,0.0143510110305094,-0.000785368577318825));
#21692=CARTESIAN_POINT('',(0.00735471061584803,0.0143768766971763,-0.00181314241081318));
#21693=CARTESIAN_POINT('',(0.00660253469265701,0.0144286080305101,-0.00371292193252399));
#21694=CARTESIAN_POINT('',(0.00602973401837723,0.014454473697177,-0.00458492762074047));
#21695=CARTESIAN_POINT('',(0.00458492762784832,0.0145062050305108,-0.00602973402552206));
#21696=CARTESIAN_POINT('',(0.00371292191159918,0.0145320706971777,-0.00660253474208717));
#21697=CARTESIAN_POINT('',(0.00181314243168958,0.0145838020305114,-0.00735471056643703));
#21698=CARTESIAN_POINT('',(0.000785368668029122,0.0146096676971782,-0.00753408567422178));
#21699=CARTESIAN_POINT('',(-0.00125688808849114,0.0146613990305118,-0.00746990556693187));
#21700=CARTESIAN_POINT('',(-0.00227137108135095,0.0146872646971786,-0.0072263503518572));
#21701=CARTESIAN_POINT('',(-0.00412017152039734,0.014738996030512,-0.00635636907020718));
#21702=CARTESIAN_POINT('',(-0.00495448896658392,0.0147648616971786,-0.00572994300363182));
#21703=CARTESIAN_POINT('',(-0.00630572718898005,0.0148165930305118,-0.00419727291315293));
#21704=CARTESIAN_POINT('',(-0.00682264796518959,0.0148424586971784,-0.00329102888924939));
#21705=CARTESIAN_POINT('',(-0.00745404035900722,0.0148941900305113,-0.00134774834427143));
#21706=CARTESIAN_POINT('',(-0.00756851197661531,0.0149200556971777,-0.000310711823197));
#21707=CARTESIAN_POINT('',(-0.00740584132452708,0.0149638284830288,0.00141047220143395));
#21708=CARTESIAN_POINT('',(-0.00723835660603977,0.0149817356022136,0.00210502128327883));
#21709=CARTESIAN_POINT('',(-0.00697825012225115,0.0149996427213983,0.00276288467579534));
#21710=CARTESIAN_POINT('',(-0.00697824874285721,0.0138055280127714,0.00276288954742755));
#21711=CARTESIAN_POINT('',(-0.00671751988917958,0.0138234350894524,0.00342050477244699));
#21712=CARTESIAN_POINT('',(-0.00636416005498398,0.0138413421661333,0.00404145886378712));
#21713=CARTESIAN_POINT('',(-0.00530451127059196,0.0138851149094806,0.00540750251084041));
#21714=CARTESIAN_POINT('',(-0.00451116464912809,0.013910980576147,0.00608510843198548));
#21715=CARTESIAN_POINT('',(-0.00272063220692462,0.01396271190948,0.00706948121497098));
#21716=CARTESIAN_POINT('',(-0.00172344638618502,0.0139885775761465,0.00737624807681142));
#21717=CARTESIAN_POINT('',(0.000310748900001265,0.0140403089094797,0.00756853028753906));
#21718=CARTESIAN_POINT('',(0.00134775836544796,0.0140661745761464,0.00745404563642627));
#21719=CARTESIAN_POINT('',(0.00329101918532537,0.0141179059094798,0.00682264366401973));
#21720=CARTESIAN_POINT('',(0.00419727053975609,0.0141437715761465,0.00630572634272598));
#21721=CARTESIAN_POINT('',(0.00572994605590523,0.0141955029094801,0.00495449058279791));
#21722=CARTESIAN_POINT('',(0.00635637021762366,0.014221368576147,0.00412017214416358));
#21723=CARTESIAN_POINT('',(0.00722635013327136,0.0142730999094807,0.00227137089460337));
#21724=CARTESIAN_POINT('',(0.00746990588720064,0.0142989655761476,0.00125688808367749));
#21725=CARTESIAN_POINT('',(0.00753408637995269,0.0143506969094813,-0.000785368631023644));
#21726=CARTESIAN_POINT('',(0.00735471111877547,0.0143765625761482,-0.00181314253479889));
#21727=CARTESIAN_POINT('',(0.00660253514414939,0.014428293909482,-0.00371292218641982));
#21728=CARTESIAN_POINT('',(0.00602973443070055,0.0144541595761489,-0.0045849279342655));
#21729=CARTESIAN_POINT('',(0.00458492794137336,0.0145058909094827,-0.00602973443784537));
#21730=CARTESIAN_POINT('',(0.003712922165495,0.0145317565761496,-0.00660253519357956));
#21731=CARTESIAN_POINT('',(0.0018131425556753,0.0145834879094833,-0.00735471106936446));
#21732=CARTESIAN_POINT('',(0.000785368721733948,0.0146093535761501,-0.00753408618941518));
#21733=CARTESIAN_POINT('',(-0.00125688817443926,0.0146610849094837,-0.00746990607773653));
#21734=CARTESIAN_POINT('',(-0.00227137123667111,0.0146869505761505,-0.00722635084600715));
#21735=CARTESIAN_POINT('',(-0.00412017180214157,0.0147386819094839,-0.00635636950486635));
#21736=CARTESIAN_POINT('',(-0.00495448930538018,0.0147645475761505,-0.00572994339545493));
#21737=CARTESIAN_POINT('',(-0.00630572762017624,0.0148162789094838,-0.00419727320016948));
#21738=CARTESIAN_POINT('',(-0.00682264843173369,0.0148421445761503,-0.00329102911429546));
#21739=CARTESIAN_POINT('',(-0.00745404086872699,0.0148938759094832,-0.00134774843643272));
#21740=CARTESIAN_POINT('',(-0.00756851249416284,0.0149197415761496,-0.000310711844443995));
#21741=CARTESIAN_POINT('',(-0.00740584183095092,0.0149635143620007,0.0014104722978844));
#21742=CARTESIAN_POINT('',(-0.00723835710101072,0.0149814214811855,0.00210502142722371));
#21743=CARTESIAN_POINT('',(-0.00697825059943558,0.0149993286003702,0.00276288486472603));
#21744=CARTESIAN_POINT('',(-0.00697824898150667,0.0138052138913639,0.00276288964191574));
#21745=CARTESIAN_POINT('',(-0.00671752011891237,0.0138231209680448,0.003420504889425));
#21746=CARTESIAN_POINT('',(-0.0063641602726322,0.0138410280447258,0.00404145900200117));
#21747=CARTESIAN_POINT('',(-0.0053045114520012,0.0138848007880731,0.00540750269577185));
#21748=CARTESIAN_POINT('',(-0.00451116480340563,0.0139106664547395,0.0060851086400904));
#21749=CARTESIAN_POINT('',(-0.00272063229996765,0.0139623977880724,0.00706948145674051));
#21750=CARTESIAN_POINT('',(-0.00172344644512525,0.013988263454739,0.00737624832907208));
#21751=CARTESIAN_POINT('',(0.000310748910628582,0.0140399947880721,0.00756853054637559));
#21752=CARTESIAN_POINT('',(0.00134775841154001,0.0140658604547388,0.00745404589134754));
#21753=CARTESIAN_POINT('',(0.0032910192978751,0.0141175917880722,0.00682264389734765));
#21754=CARTESIAN_POINT('',(0.00419727068329875,0.014143457454739,0.00630572655837582));
#21755=CARTESIAN_POINT('',(0.00572994625186393,0.0141951887880726,0.00495449075223677));
#21756=CARTESIAN_POINT('',(0.00635637043500547,0.0142210544547394,0.00412017228506955));
#21757=CARTESIAN_POINT('',(0.00722635038040566,0.0142727857880731,0.0022713709722821));
#21758=CARTESIAN_POINT('',(0.00746990614266431,0.01429865145474,0.00125688812666186));
#21759=CARTESIAN_POINT('',(0.00753408663761128,0.0143503827880738,-0.000785368657882504));
#21760=CARTESIAN_POINT('',(0.00735471137029959,0.0143762484547407,-0.00181314259680664));
#21761=CARTESIAN_POINT('',(0.00660253536994981,0.0144279797880745,-0.00371292231339822));
#21762=CARTESIAN_POINT('',(0.00602973463691173,0.0144538454547414,-0.00458492809106567));
#21763=CARTESIAN_POINT('',(0.00458492809817353,0.0145055767880752,-0.00602973464405655));
#21764=CARTESIAN_POINT('',(0.00371292229247341,0.014531442454742,-0.00660253541937998));
#21765=CARTESIAN_POINT('',(0.00181314261768305,0.0145831737880757,-0.00735471132088858));
#21766=CARTESIAN_POINT('',(0.000785368748592811,0.0146090394547426,-0.00753408644707376));
#21767=CARTESIAN_POINT('',(-0.00125688821742364,0.0146607707880762,-0.00746990633320021));
#21768=CARTESIAN_POINT('',(-0.00227137131434984,0.0146866364547429,-0.00722635109314147));
#21769=CARTESIAN_POINT('',(-0.00412017194304752,0.0147383677880763,-0.00635636972224814));
#21770=CARTESIAN_POINT('',(-0.004954489474819,0.014764233454743,-0.00572994359141354));
#21771=CARTESIAN_POINT('',(-0.00630572783582612,0.0148159647880762,-0.00419727334371223));
#21772=CARTESIAN_POINT('',(-0.00682264866506177,0.0148418304547427,-0.00329102922684552));
#21773=CARTESIAN_POINT('',(-0.00745404112364809,0.0148935617880757,-0.00134774848252443));
#21774=CARTESIAN_POINT('',(-0.00756851275299877,0.0149194274547421,-0.000310711855070044));
#21775=CARTESIAN_POINT('',(-0.00740584208422367,0.0149632002405932,0.00141047234612122));
#21776=CARTESIAN_POINT('',(-0.00723835734855565,0.0149811073597779,0.00210502149921344));
#21777=CARTESIAN_POINT('',(-0.00697825083808511,0.0149990144789627,0.00276288495921406));
#21778=CARTESIAN_POINT('',(-0.00697824898150667,0.0136799987751258,0.00276288964191574));
#21779=CARTESIAN_POINT('',(-0.00671752011891237,0.0136979058518067,0.003420504889425));
#21780=CARTESIAN_POINT('',(-0.00636416027263221,0.0137158129284877,0.00404145900200118));
#21781=CARTESIAN_POINT('',(-0.00530451145200121,0.013759585671835,0.00540750269577187));
#21782=CARTESIAN_POINT('',(-0.00451116480340563,0.0137854513385014,0.00608510864009041));
#21783=CARTESIAN_POINT('',(-0.00272063229996765,0.0138371826718343,0.00706948145674051));
#21784=CARTESIAN_POINT('',(-0.00172344644512526,0.0138630483385009,0.00737624832907209));
#21785=CARTESIAN_POINT('',(0.000310748910628586,0.0139147796718341,0.00756853054637561));
#21786=CARTESIAN_POINT('',(0.00134775841154003,0.0139406453385007,0.00745404589134754));
#21787=CARTESIAN_POINT('',(0.00329101929787511,0.0139923766718341,0.00682264389734765));
#21788=CARTESIAN_POINT('',(0.00419727068329876,0.0140182423385009,0.00630572655837583));
#21789=CARTESIAN_POINT('',(0.00572994625186394,0.0140699736718345,0.00495449075223678));
#21790=CARTESIAN_POINT('',(0.00635637043500548,0.0140958393385013,0.00412017228506955));
#21791=CARTESIAN_POINT('',(0.00722635038040566,0.014147570671835,0.00227137097228209));
#21792=CARTESIAN_POINT('',(0.00746990614266432,0.0141734363385019,0.00125688812666186));
#21793=CARTESIAN_POINT('',(0.00753408663761128,0.0142251676718357,-0.000785368657882517));
#21794=CARTESIAN_POINT('',(0.00735471137029959,0.0142510333385026,-0.00181314259680666));
#21795=CARTESIAN_POINT('',(0.00660253536994981,0.0143027646718364,-0.00371292231339824));
#21796=CARTESIAN_POINT('',(0.00602973463691173,0.0143286303385033,-0.00458492809106568));
#21797=CARTESIAN_POINT('',(0.00458492809817352,0.0143803616718371,-0.00602973464405656));
#21798=CARTESIAN_POINT('',(0.00371292229247341,0.014406227338504,-0.00660253541937999));
#21799=CARTESIAN_POINT('',(0.00181314261768303,0.0144579586718377,-0.0073547113208886));
#21800=CARTESIAN_POINT('',(0.00078536874859279,0.0144838243385045,-0.00753408644707379));
#21801=CARTESIAN_POINT('',(-0.00125688821742367,0.0145355556718381,-0.00746990633320024));
#21802=CARTESIAN_POINT('',(-0.00227137131434988,0.0145614213385048,-0.00722635109314148));
#21803=CARTESIAN_POINT('',(-0.00412017194304755,0.0146131526718383,-0.00635636972224814));
#21804=CARTESIAN_POINT('',(-0.00495448947481901,0.0146390183385049,-0.00572994359141354));
#21805=CARTESIAN_POINT('',(-0.00630572783582613,0.0146907496718381,-0.00419727334371224));
#21806=CARTESIAN_POINT('',(-0.00682264866506178,0.0147166153385046,-0.00329102922684553));
#21807=CARTESIAN_POINT('',(-0.00745404112364811,0.0147683466718376,-0.00134774848252442));
#21808=CARTESIAN_POINT('',(-0.00756851275299878,0.014794212338504,-0.000310711855070028));
#21809=CARTESIAN_POINT('',(-0.00740584208422367,0.0148379851243551,0.00141047234612124));
#21810=CARTESIAN_POINT('',(-0.00723835734855564,0.0148558922435399,0.00210502149921347));
#21811=CARTESIAN_POINT('',(-0.0069782508380851,0.0148737993627246,0.00276288495921409));
#21812=CARTESIAN_POINT('',(-0.00694051807885813,0.0135550977802952,0.00274795089146644));
#21813=CARTESIAN_POINT('',(-0.00668119895893111,0.0135730048569762,0.00340201045947075));
#21814=CARTESIAN_POINT('',(-0.00632974970454803,0.0135909119336571,0.00401960711672642));
#21815=CARTESIAN_POINT('',(-0.00527583033074515,0.0136346846770044,0.00537826470808661));
#21816=CARTESIAN_POINT('',(-0.00448677325181727,0.0136605503436708,0.00605220688460511));
#21817=CARTESIAN_POINT('',(-0.00270592203200149,0.0137122816770038,0.00703125726649926));
#21818=CARTESIAN_POINT('',(-0.00171412789111359,0.0137381473436703,0.00733636547187492));
#21819=CARTESIAN_POINT('',(0.000309068713070982,0.0137898786770035,0.00752760803272001));
#21820=CARTESIAN_POINT('',(0.00134047117636765,0.0138157443436701,0.00741374238818944));
#21821=CARTESIAN_POINT('',(0.00327322498742965,0.0138674756770036,0.00678575434047189));
#21822=CARTESIAN_POINT('',(0.00417457633519497,0.0138933413436703,0.00627163193728492));
#21823=CARTESIAN_POINT('',(0.00569896483449356,0.0139450726770039,0.00492770216834686));
#21824=CARTESIAN_POINT('',(0.00632200198602682,0.0139709383436707,0.00409789480259576));
#21825=CARTESIAN_POINT('',(0.00718727801090008,0.0140226696770045,0.00225908982879452));
#21826=CARTESIAN_POINT('',(0.00742951688424009,0.0140485353436713,0.00125009222074437));
#21827=CARTESIAN_POINT('',(0.00749335035975379,0.0141002666770051,-0.000781122224650859));
#21828=CARTESIAN_POINT('',(0.00731494496192747,0.014126132343672,-0.00180333906199593));
#21829=CARTESIAN_POINT('',(0.00656683592443887,0.0141778636770058,-0.00369284680294858));
#21830=CARTESIAN_POINT('',(0.00599713228477658,0.0142037293436727,-0.00456013770655617));
#21831=CARTESIAN_POINT('',(0.0045601377136256,0.0142554606770065,-0.00599713229188276));
#21832=CARTESIAN_POINT('',(0.0036928467821369,0.0142813263436734,-0.00656683597360176));
#21833=CARTESIAN_POINT('',(0.00180333908275946,0.0143330576770071,-0.00731494491278364));
#21834=CARTESIAN_POINT('',(0.000781122314870693,0.0143589233436739,-0.00749335017024651));
#21835=CARTESIAN_POINT('',(-0.0012500923110154,0.0144106546770075,-0.00742951707374578));
#21836=CARTESIAN_POINT('',(-0.00225909016901274,0.0144365203436743,-0.00718727871978218));
#21837=CARTESIAN_POINT('',(-0.00409789446242304,0.0144882516770077,-0.00632200127712331));
#21838=CARTESIAN_POINT('',(-0.00492770089783601,0.0145141173436743,-0.00569896218842803));
#21839=CARTESIAN_POINT('',(-0.00627163320782814,0.0145658486770075,-0.00417457898122379));
#21840=CARTESIAN_POINT('',(-0.00678575908240731,0.0145917143436741,-0.00327323486271482));
#21841=CARTESIAN_POINT('',(-0.00741373764626861,0.014643445677007,-0.00134046130103755));
#21842=CARTESIAN_POINT('',(-0.00752759033555073,0.0146693113436734,-0.000309031857869243));
#21843=CARTESIAN_POINT('',(-0.0073657992156687,0.0147130841295245,0.00140284602110459));
#21844=CARTESIAN_POINT('',(-0.0071992200582157,0.0147309912487093,0.00209363979565566));
#21845=CARTESIAN_POINT('',(-0.00694051992539818,0.014748898367894,0.00274794623408381));
#21846=CARTESIAN_POINT('',(-0.00680400639064949,0.0133530037254307,0.00269390198459144));
#21847=CARTESIAN_POINT('',(-0.00654978776760812,0.0133709108021116,0.00333509698329374));
#21848=CARTESIAN_POINT('',(-0.00620525109964731,0.0133888178787926,0.00394054625308408));
#21849=CARTESIAN_POINT('',(-0.00517206105920528,0.0134325906221399,0.00527248067487872));
#21850=CARTESIAN_POINT('',(-0.00439852378913224,0.0134584562888063,0.00593316721496976));
#21851=CARTESIAN_POINT('',(-0.00265269978251629,0.0135101876221392,0.00689296084701396));
#21852=CARTESIAN_POINT('',(-0.00168041304597339,0.0135360532888058,0.00719206793896711));
#21853=CARTESIAN_POINT('',(0.000302989701199763,0.013587784622139,0.007379548987409));
#21854=CARTESIAN_POINT('',(0.00131410571183001,0.0136136502888056,0.00726792294389772));
#21855=CARTESIAN_POINT('',(0.00320884456743163,0.013665381622139,0.00665228666986547));
#21856=CARTESIAN_POINT('',(0.004092467412403,0.0136912472888058,0.00614827643934451));
#21857=CARTESIAN_POINT('',(0.0055868730134279,0.0137429786221394,0.00483078016132269));
#21858=CARTESIAN_POINT('',(0.00619765576948143,0.0137688442888062,0.00401729411382185));
#21859=CARTESIAN_POINT('',(0.00704591285000791,0.0138205756221399,0.00221465623423577));
#21860=CARTESIAN_POINT('',(0.00728338717448087,0.0138464412888068,0.00122550440215052));
#21861=CARTESIAN_POINT('',(0.00734596512189023,0.0138981726221406,-0.000765758484887794));
#21862=CARTESIAN_POINT('',(0.00717106874482664,0.0139240382888075,-0.00176786953984086));
#21863=CARTESIAN_POINT('',(0.00643767411720073,0.0139757696221413,-0.00362021292380028));
#21864=CARTESIAN_POINT('',(0.0058791758666384,0.0140016352888082,-0.00447044525280663));
#21865=CARTESIAN_POINT('',(0.00447044525973701,0.014053366622142,-0.00587917587360481));
#21866=CARTESIAN_POINT('',(0.00362021290339795,0.0140792322888089,-0.00643767416539665));
#21867=CARTESIAN_POINT('',(0.00176786956019601,0.0141309636221426,-0.0071710686966494));
#21868=CARTESIAN_POINT('',(0.000765758573333131,0.0141568292888094,-0.00734596493611032));
#21869=CARTESIAN_POINT('',(-0.00122550449064601,0.014208560622143,-0.00728338736025919));
#21870=CARTESIAN_POINT('',(-0.00221465656776228,0.0142344262888097,-0.00704591354494715));
#21871=CARTESIAN_POINT('',(-0.00401729378033991,0.0142861576221432,-0.00619765507452121));
#21872=CARTESIAN_POINT('',(-0.00483077891580127,0.0143120232888098,-0.00558687041940731));
#21873=CARTESIAN_POINT('',(-0.00614827768489766,0.014363754622143,-0.00409247000638758));
#21874=CARTESIAN_POINT('',(-0.0066522913185327,0.0143896202888096,-0.00320885424848175));
#21875=CARTESIAN_POINT('',(-0.0072679182952448,0.0144413516221425,-0.00131409603073584));
#21876=CARTESIAN_POINT('',(-0.00737953163832187,0.0144672172888089,-0.000302953570895764));
#21877=CARTESIAN_POINT('',(-0.00722092275622978,0.01451099007466,0.00137525371798514));
#21878=CARTESIAN_POINT('',(-0.00705762001153818,0.0145288971938448,0.00205246040533372));
#21879=CARTESIAN_POINT('',(-0.00680400820087031,0.0145468043130295,0.00269389741881393));
#21880=CARTESIAN_POINT('',(-0.00670522560508939,0.0132758106653968,0.00265479182816572));
#21881=CARTESIAN_POINT('',(-0.00645469773626639,0.0132937177420777,0.00328667793707097));
#21882=CARTESIAN_POINT('',(-0.00611516306283078,0.0133116248187586,0.0038833372747165));
#21883=CARTESIAN_POINT('',(-0.00509697290892147,0.0133553975621059,0.00519593462935609));
#21884=CARTESIAN_POINT('',(-0.00433466587803557,0.0133812632287723,0.00584702930081972));
#21885=CARTESIAN_POINT('',(-0.00261418780099727,0.0134329945621053,0.00679288861776991));
#21886=CARTESIAN_POINT('',(-0.00165601675484486,0.0134588602287718,0.00708765326325648));
#21887=CARTESIAN_POINT('',(0.000298590886886145,0.013510591562105,0.00727241245575358));
#21888=CARTESIAN_POINT('',(0.00129502748246474,0.0135364572287717,0.00716240700276411));
#21889=CARTESIAN_POINT('',(0.00316225845787907,0.0135881885621051,0.00655570855613482));
#21890=CARTESIAN_POINT('',(0.00403305283771479,0.0136140542287718,0.00605901556249499));
#21891=CARTESIAN_POINT('',(0.00550576260973261,0.0136657855621054,0.00476064673818844));
#21892=CARTESIAN_POINT('',(0.00610767800191469,0.0136916512287723,0.00395897090752172));
#21893=CARTESIAN_POINT('',(0.00694362005862132,0.013743382562106,0.00218250378316458));
#21894=CARTESIAN_POINT('',(0.00717764672314586,0.0137692482287729,0.00120771248947416));
#21895=CARTESIAN_POINT('',(0.00723931616188417,0.0138209795621066,-0.000754641178356387));
#21896=CARTESIAN_POINT('',(0.00706695893609794,0.0138468452287735,-0.00174220355249652));
#21897=CARTESIAN_POINT('',(0.00634421175547354,0.0138985765621073,-0.00356765455510162));
#21898=CARTESIAN_POINT('',(0.00579382180063537,0.0139244422287742,-0.00440554318356659));
#21899=CARTESIAN_POINT('',(0.00440554319039635,0.013976173562108,-0.00579382180750065));
#21900=CARTESIAN_POINT('',(0.00356765453499548,0.0140020392287749,-0.00634421180296975));
#21901=CARTESIAN_POINT('',(0.00174220357255614,0.0140537705621086,-0.00706695888862013));
#21902=CARTESIAN_POINT('',(0.000754641265517664,0.0140796362287754,-0.00723931597880142));
#21903=CARTESIAN_POINT('',(-0.00120771257668489,0.014131367562109,-0.00717764690622705));
#21904=CARTESIAN_POINT('',(-0.00218250411184896,0.0141572332287758,-0.0069436207434714));
#21905=CARTESIAN_POINT('',(-0.00395897057888128,0.0142089645621092,-0.00610767731704393));
#21906=CARTESIAN_POINT('',(-0.00476064551074954,0.0142348302287759,-0.0055057600533721));
#21907=CARTESIAN_POINT('',(-0.00605901678996516,0.0142865615621091,-0.00403305539403983));
#21908=CARTESIAN_POINT('',(-0.00655571313731254,0.0143124272287756,-0.00316226799837939));
#21909=CARTESIAN_POINT('',(-0.00716240242160049,0.0143641585621085,-0.00129501794192101));
#21910=CARTESIAN_POINT('',(-0.00727239535854106,0.0143900242287749,-0.000298555281123069));
#21911=CARTESIAN_POINT('',(-0.00711608916534582,0.014433797014626,0.00135528773988235));
#21912=CARTESIAN_POINT('',(-0.0069551572552006,0.0144517041338108,0.00202266271856957));
#21913=CARTESIAN_POINT('',(-0.00670522738902937,0.0144696112529955,0.00265478732867433));
#21914=CARTESIAN_POINT('',(-0.00648434505370619,0.0131986176053628,0.00256733885978718));
#21915=CARTESIAN_POINT('',(-0.00624206996220368,0.0132165246820437,0.00317840965831116));
#21916=CARTESIAN_POINT('',(-0.00591372008854949,0.0132344317587247,0.00375541411016327));
#21917=CARTESIAN_POINT('',(-0.00492907070058216,0.013278204502072,0.00502477246815869));
#21918=CARTESIAN_POINT('',(-0.00419187524792228,0.0133040701687384,0.00565441906934018));
#21919=CARTESIAN_POINT('',(-0.00252807239237249,0.0133558015020713,0.00656912031052029));
#21920=CARTESIAN_POINT('',(-0.00160146498948258,0.0133816671687379,0.0068541749505189));
#21921=CARTESIAN_POINT('',(0.0002887548390605,0.0134333985020711,0.00703284788809851));
#21922=CARTESIAN_POINT('',(0.00125236726471367,0.0134592641687377,0.0069264661856795));
#21923=CARTESIAN_POINT('',(0.00305808875011229,0.0135109955020711,0.00633975332869436));
#21924=CARTESIAN_POINT('',(0.00390019780985773,0.0135368611687379,0.00585942217412824));
#21925=CARTESIAN_POINT('',(0.00532439423338749,0.0135885925020715,0.00460382363656549));
#21926=CARTESIAN_POINT('',(0.0059064815971718,0.0136144581687383,0.00382855625356888));
#21927=CARTESIAN_POINT('',(0.00671488642347269,0.013666189502072,0.00211060871692618));
#21928=CARTESIAN_POINT('',(0.00694120388598927,0.0136920551687389,0.00116792856328009));
#21929=CARTESIAN_POINT('',(0.00700084183758095,0.0137437865020727,-0.000729782125225456));
#21930=CARTESIAN_POINT('',(0.00683416232665604,0.0137696521687396,-0.00168481266008492));
#21931=CARTESIAN_POINT('',(0.00613522356131386,0.0138213835020734,-0.00345013046990492));
#21932=CARTESIAN_POINT('',(0.0056029643068966,0.0138472491687403,-0.00426041774486545));
#21933=CARTESIAN_POINT('',(0.00426041775147022,0.0138989805020741,-0.00560296431353573));
#21934=CARTESIAN_POINT('',(0.00345013045046111,0.0139248461687409,-0.00613522360724548));
#21935=CARTESIAN_POINT('',(0.00168481267948375,0.0139765775020746,-0.00683416228074223));
#21936=CARTESIAN_POINT('',(0.000729782209515497,0.0140024431687415,-0.00700084166052923));
#21937=CARTESIAN_POINT('',(-0.00116792864761797,0.0140541745020751,-0.00694120406303949));
#21938=CARTESIAN_POINT('',(-0.00211060903478319,0.0140800401687418,-0.00671488708576275));
#21939=CARTESIAN_POINT('',(-0.00382855593575437,0.0141317715020752,-0.00590648093486174));
#21940=CARTESIAN_POINT('',(-0.00460382244956033,0.0141576371687419,-0.00532439176123747));
#21941=CARTESIAN_POINT('',(-0.00585942336116364,0.0142093685020751,-0.00390020028197345));
#21942=CARTESIAN_POINT('',(-0.00633975775896097,0.0142352341687416,-0.0030580979763337));
#21943=CARTESIAN_POINT('',(-0.00692646175542652,0.0142869655020746,-0.00125235803845027));
#21944=CARTESIAN_POINT('',(-0.00703283135409474,0.014312831168741,-0.000288720406206587));
#21945=CARTESIAN_POINT('',(-0.0068816741298039,0.0143566039545921,0.00131064245560722));
#21946=CARTESIAN_POINT('',(-0.00672604356686779,0.0143745110737768,0.00195603306539268));
#21947=CARTESIAN_POINT('',(-0.00648434677888041,0.0143924181929616,0.00256733450851603));
#21948=CARTESIAN_POINT('',(-0.00636224528788308,0.0131986176053628,0.00251899604783435));
#21949=CARTESIAN_POINT('',(-0.0061245322194827,0.0132165246820437,0.00311856042577412));
#21950=CARTESIAN_POINT('',(-0.00580236515108474,0.0132344317587247,0.00368469992397763));
#21951=CARTESIAN_POINT('',(-0.00483625664252665,0.013278204502072,0.00493015635248392));
#21952=CARTESIAN_POINT('',(-0.00411294252890567,0.0133040701687384,0.00554794675201068));
#21953=CARTESIAN_POINT('',(-0.00248046896526676,0.0133558015020713,0.0064454242325147));
#21954=CARTESIAN_POINT('',(-0.00157130951524884,0.0133816671687378,0.00672511131349196));
#21955=CARTESIAN_POINT('',(0.000283317605548472,0.013433398502071,0.00690041985209886));
#21956=CARTESIAN_POINT('',(0.00122878527632786,0.0134592641687377,0.00679604130972849));
#21957=CARTESIAN_POINT('',(0.00300050515189806,0.0135109955020711,0.00622037621498456));
#21958=CARTESIAN_POINT('',(0.00382675735668888,0.0135368611687379,0.00574908966261099));
#21959=CARTESIAN_POINT('',(0.00522413626073766,0.0135885925020715,0.0045171339580768));
#21960=CARTESIAN_POINT('',(0.00579526295999564,0.0136144581687383,0.00375646480591617));
#21961=CARTESIAN_POINT('',(0.00658844557971066,0.013666189502072,0.00207086610175896));
#21962=CARTESIAN_POINT('',(0.0068105015001677,0.0136920551687389,0.00114593654976238));
#21963=CARTESIAN_POINT('',(0.0068690164732838,0.0137437865020727,-0.000716040378625932));
#21964=CARTESIAN_POINT('',(0.00670547552594286,0.0137696521687396,-0.00165308775501766));
#21965=CARTESIAN_POINT('',(0.00601969772888139,0.0138213835020734,-0.00338516475340688));
#21966=CARTESIAN_POINT('',(0.00549746087916086,0.0138472491687403,-0.00418019437540436));
#21967=CARTESIAN_POINT('',(0.00418019438188476,0.0138989805020741,-0.00549746088567498));
#21968=CARTESIAN_POINT('',(0.00338516473432919,0.0139248461687409,-0.00601969777394812));
#21969=CARTESIAN_POINT('',(0.0016530877740512,0.0139765775020746,-0.0067054754808936));
#21970=CARTESIAN_POINT('',(0.000716040461328796,0.0140024431687415,-0.00686901629956595));
#21971=CARTESIAN_POINT('',(-0.00114593663251218,0.0140541745020751,-0.00681050167388407));
#21972=CARTESIAN_POINT('',(-0.00207086641363074,0.0140800401687418,-0.00658844622952984));
#21973=CARTESIAN_POINT('',(-0.00375646449408609,0.0141317715020752,-0.00579526231015683));
#21974=CARTESIAN_POINT('',(-0.00451713279342287,0.0141576371687419,-0.00522413383513805));
#21975=CARTESIAN_POINT('',(-0.0057490908272946,0.0142093685020751,-0.00382675978225482));
#21976=CARTESIAN_POINT('',(-0.00622038056182956,0.0142352341687416,-0.00300051420439038));
#21977=CARTESIAN_POINT('',(-0.00679603696289687,0.0142869655020746,-0.00122877622379436));
#21978=CARTESIAN_POINT('',(-0.00690040362942923,0.014312831168741,-0.0002832838210628));
#21979=CARTESIAN_POINT('',(-0.00675209268514594,0.0143566039545921,0.00128596314943489));
#21980=CARTESIAN_POINT('',(-0.00659939263487256,0.0143745110737768,0.00191920109897995));
#21981=CARTESIAN_POINT('',(-0.00636224698057239,0.0143924181929616,0.00251899177849733));
#21982=CARTESIAN_POINT('',(-0.00614136473649988,0.0132758106653968,0.00243154307945581));
#21983=CARTESIAN_POINT('',(-0.00591190444542,0.0132937177420777,0.0030102921470143));
#21984=CARTESIAN_POINT('',(-0.00560092217680345,0.0133116248187586,0.00355677675942441));
#21985=CARTESIAN_POINT('',(-0.00466835443418733,0.0133553975621059,0.00475899419128651));
#21986=CARTESIAN_POINT('',(-0.00397015189879237,0.0133812632287723,0.00535533652053114));
#21987=CARTESIAN_POINT('',(-0.00239435355664199,0.0134329945621053,0.00622165592526508));
#21988=CARTESIAN_POINT('',(-0.00151675774988656,0.0134588602287718,0.00649163300075439));
#21989=CARTESIAN_POINT('',(0.000273481557722826,0.013510591562105,0.00666085528444379));
#21990=CARTESIAN_POINT('',(0.00118612505857678,0.0135364572287717,0.00656010049264387));
#21991=CARTESIAN_POINT('',(0.00289633544413128,0.0135881885621051,0.0060044209875441));
#21992=CARTESIAN_POINT('',(0.00369390232883181,0.0136140542287718,0.00554949627424424));
#21993=CARTESIAN_POINT('',(0.00504276788439255,0.0136657855621054,0.00436031085645385));
#21994=CARTESIAN_POINT('',(0.00559406655525274,0.0136916512287723,0.00362605015196332));
#21995=CARTESIAN_POINT('',(0.00635971194456203,0.013743382562106,0.00199897103552055));
#21996=CARTESIAN_POINT('',(0.00657405866301112,0.0137692482287729,0.00110615262356831));
#21997=CARTESIAN_POINT('',(0.00663054214898058,0.0138209795621066,-0.000691181325494998));
#21998=CARTESIAN_POINT('',(0.00647267891650096,0.0138468452287735,-0.00159569686260606));
#21999=CARTESIAN_POINT('',(0.00581070953472172,0.0138985765621073,-0.00326764066821018));
#22000=CARTESIAN_POINT('',(0.00530660338542209,0.0139244422287742,-0.00403506893670322));
#22001=CARTESIAN_POINT('',(0.00403506894295864,0.013976173562108,-0.00530660339171005));
#22002=CARTESIAN_POINT('',(0.00326764064979481,0.0140020392287749,-0.00581070957822385));
#22003=CARTESIAN_POINT('',(0.0015956968809788,0.0140537705621086,-0.0064726788730157));
#22004=CARTESIAN_POINT('',(0.00069118140532663,0.0140796362287754,-0.00663054198129377));
#22005=CARTESIAN_POINT('',(-0.00110615270344525,0.014131367562109,-0.00657405883069651));
#22006=CARTESIAN_POINT('',(-0.00199897133656496,0.0141572332287758,-0.00635971257182118));
#22007=CARTESIAN_POINT('',(-0.00362604985095917,0.0142089645621092,-0.00559406592797464));
#22008=CARTESIAN_POINT('',(-0.00436030973223366,0.0142348302287759,-0.00504276554300342));
#22009=CARTESIAN_POINT('',(-0.00554949739849307,0.0142865615621091,-0.00369390467018844));
#22010=CARTESIAN_POINT('',(-0.00600442518347799,0.0143124272287756,-0.00289634418234468));
#22011=CARTESIAN_POINT('',(-0.00656009629672291,0.0143641585621085,-0.00118611632032362));
#22012=CARTESIAN_POINT('',(-0.00666083962498291,0.0143900242287749,-0.00027344894614632));
#22013=CARTESIAN_POINT('',(-0.00651767764960402,0.014433797014626,0.00124131786515975));
#22014=CARTESIAN_POINT('',(-0.00637027894653976,0.0144517041338108,0.00185257144580306));
#22015=CARTESIAN_POINT('',(-0.00614136637042343,0.0144696112529955,0.00243153895833903));
#22016=CARTESIAN_POINT('',(-0.00604258395093978,0.0133530037254307,0.0023924329230301));
#22017=CARTESIAN_POINT('',(-0.00581681441407825,0.0133709108021116,0.00296187310079154));
#22018=CARTESIAN_POINT('',(-0.0055108341399869,0.0133888178787926,0.00349956778105683));
#22019=CARTESIAN_POINT('',(-0.00459326628390352,0.0134325906221399,0.00468244814576388));
#22020=CARTESIAN_POINT('',(-0.00390629398769571,0.0134584562888063,0.0052691986063811));
#22021=CARTESIAN_POINT('',(-0.00235584157512295,0.0135101876221392,0.00612158369602103));
#22022=CARTESIAN_POINT('',(-0.00149236145875803,0.0135360532888058,0.00638721832504376));
#22023=CARTESIAN_POINT('',(0.000269082743409209,0.013587784622139,0.00655371875278837));
#22024=CARTESIAN_POINT('',(0.00116704682921151,0.0136136502888056,0.00645458455151027));
#22025=CARTESIAN_POINT('',(0.00284974933457871,0.013665381622139,0.00590784287381344));
#22026=CARTESIAN_POINT('',(0.00363448775414361,0.0136912472888058,0.00546023539739472));
#22027=CARTESIAN_POINT('',(0.00496165748069726,0.0137429786221394,0.00429017743331959));
#22028=CARTESIAN_POINT('',(0.00550408878768601,0.0137688442888062,0.00356772694566319));
#22029=CARTESIAN_POINT('',(0.00625741915317544,0.0138205756221399,0.00196681858444937));
#22030=CARTESIAN_POINT('',(0.00646831821167611,0.0138464412888068,0.00108836071089196));
#22031=CARTESIAN_POINT('',(0.00652389318897452,0.0138981726221406,-0.000680064018963589));
#22032=CARTESIAN_POINT('',(0.00636856910777225,0.0139240382888075,-0.00157003087526173));
#22033=CARTESIAN_POINT('',(0.00571724717299453,0.0139757696221413,-0.00321508229951151));
#22034=CARTESIAN_POINT('',(0.00522124931941907,0.0140016352888082,-0.00397016686746317));
#22035=CARTESIAN_POINT('',(0.00397016687361797,0.014053366622142,-0.00522124932560588));
#22036=CARTESIAN_POINT('',(0.00321508228139235,0.0140792322888089,-0.00571724721579695));
#22037=CARTESIAN_POINT('',(0.00157003089333894,0.0141309636221426,-0.00636856906498643));
#22038=CARTESIAN_POINT('',(0.000680064097511164,0.0141568292888094,-0.00652389302398486));
#22039=CARTESIAN_POINT('',(-0.00108836078948412,0.014208560622143,-0.00646831837666436));
#22040=CARTESIAN_POINT('',(-0.00196681888065163,0.0142344262888097,-0.00625741977034544));
#22041=CARTESIAN_POINT('',(-0.00356772664950053,0.0142861576221432,-0.00550408817049736));
#22042=CARTESIAN_POINT('',(-0.00429017632718193,0.0143120232888098,-0.00496165517696821));
#22043=CARTESIAN_POINT('',(-0.00546023650356058,0.014363754622143,-0.00363449005784069));
#22044=CARTESIAN_POINT('',(-0.00590784700225783,0.0143896202888096,-0.00284975793224231));
#22045=CARTESIAN_POINT('',(-0.00645458042307859,0.0144413516221425,-0.00116703823150879));
#22046=CARTESIAN_POINT('',(-0.0065537033452021,0.0144672172888089,-0.000269050656373628));
#22047=CARTESIAN_POINT('',(-0.00641284405872006,0.01451099007466,0.00122135188705695));
#22048=CARTESIAN_POINT('',(-0.00626781619020218,0.0145288971938448,0.00182277375903891));
#22049=CARTESIAN_POINT('',(-0.00604258555858249,0.0145468043130295,0.00239242886819942));
#22050=CARTESIAN_POINT('',(-0.00590607226273114,0.0135550977802952,0.00233838401615509));
#22051=CARTESIAN_POINT('',(-0.00568540322275527,0.0135730048569762,0.00289495962461452));
#22052=CARTESIAN_POINT('',(-0.0053863355350862,0.0135909119336571,0.00342050691741449));
#22053=CARTESIAN_POINT('',(-0.00448949701236366,0.0136346846770044,0.004576664112556));
#22054=CARTESIAN_POINT('',(-0.00381804452501068,0.0136605503436708,0.00515015893674575));
#22055=CARTESIAN_POINT('',(-0.00230261932563777,0.0137122816770038,0.00598328727653573));
#22056=CARTESIAN_POINT('',(-0.00145864661361783,0.0137381473436703,0.00624292079213596));
#22057=CARTESIAN_POINT('',(0.000263003731537994,0.0137898786770035,0.00640565970747737));
#22058=CARTESIAN_POINT('',(0.00114068136467388,0.0138157443436702,0.00630876510721855));
#22059=CARTESIAN_POINT('',(0.0027853689145807,0.0138674756770036,0.00577437520320703));
#22060=CARTESIAN_POINT('',(0.00355237883135163,0.0138933413436703,0.00533687989945431));
#22061=CARTESIAN_POINT('',(0.00484956565963159,0.0139450726770039,0.00419325542629543));
#22062=CARTESIAN_POINT('',(0.00537974257114062,0.0139709383436707,0.00348712625688928));
#22063=CARTESIAN_POINT('',(0.00611605399228327,0.0140226696770045,0.00192238498989061));
#22064=CARTESIAN_POINT('',(0.00632218850191688,0.0140485353436713,0.0010637728922981));
#22065=CARTESIAN_POINT('',(0.00637650795111096,0.0141002666770051,-0.000664700279200532));
#22066=CARTESIAN_POINT('',(0.00622469289067143,0.014126132343672,-0.00153456135310666));
#22067=CARTESIAN_POINT('',(0.00558808536575639,0.0141778636770058,-0.00314244842036322));
#22068=CARTESIAN_POINT('',(0.00510329290128088,0.0142037293436727,-0.00388047441371363));
#22069=CARTESIAN_POINT('',(0.00388047441972938,0.0142554606770065,-0.00510329290732795));
#22070=CARTESIAN_POINT('',(0.00314244840265338,0.0142813263436734,-0.00558808540759184));
#22071=CARTESIAN_POINT('',(0.00153456137077549,0.0143330576770071,-0.00622469284885221));
#22072=CARTESIAN_POINT('',(0.000664700355973588,0.0143589233436739,-0.00637650778984869));
#22073=CARTESIAN_POINT('',(-0.00106377296911475,0.0144106546770075,-0.00632218866317778));
#22074=CARTESIAN_POINT('',(-0.00192238527940119,0.0144365203436743,-0.00611605459551041));
#22075=CARTESIAN_POINT('',(-0.00348712596741742,0.0144882516770077,-0.00537974196789526));
#22076=CARTESIAN_POINT('',(-0.0041932543451472,0.0145141173436743,-0.00484956340794749));
#22077=CARTESIAN_POINT('',(-0.0053368809806301,0.0145658486770075,-0.00355238108300448));
#22078=CARTESIAN_POINT('',(-0.00577437923838321,0.0145917143436741,-0.00278537731800925));
#22079=CARTESIAN_POINT('',(-0.00630876107205479,0.014643445677007,-0.00114067296120708));
#22080=CARTESIAN_POINT('',(-0.00640564464797325,0.0146693113436734,-0.00026297236940014));
#22081=CARTESIAN_POINT('',(-0.00626796759928114,0.0147130841295245,0.00119375958393752));
#22082=CARTESIAN_POINT('',(-0.00612621614352466,0.0147309912487093,0.00178159436871697));
#22083=CARTESIAN_POINT('',(-0.00590607383405462,0.014748898367894,0.00233838005292956));
#22084=CARTESIAN_POINT('',(-0.00586834136008259,0.0136799987751258,0.00232344526570579));
#22085=CARTESIAN_POINT('',(-0.00564908206277401,0.0136979058518067,0.00287646519466028));
#22086=CARTESIAN_POINT('',(-0.00535192496700203,0.0137158129284877,0.00339865503213973));
#22087=CARTESIAN_POINT('',(-0.00446081589110761,0.013759585671835,0.00454742612487075));
#22088=CARTESIAN_POINT('',(-0.00379365297342232,0.0137854513385014,0.00511725718126046));
#22089=CARTESIAN_POINT('',(-0.00228790905767161,0.0138371826718343,0.00594506308629448));
#22090=CARTESIAN_POINT('',(-0.00144932805960617,0.0138630483385009,0.00620303793493879));
#22091=CARTESIAN_POINT('',(0.000261323533980394,0.0139147796718341,0.00636473719382177));
#22092=CARTESIAN_POINT('',(0.00113339412950152,0.0139406453385007,0.00626846160406045));
#22093=CARTESIAN_POINT('',(0.00276757460413525,0.0139923766718341,0.00573748564633127));
#22094=CARTESIAN_POINT('',(0.00352968448324786,0.0140182423385009,0.00530278527836341));
#22095=CARTESIAN_POINT('',(0.00481858424226123,0.0140699736718345,0.00416646684240553));
#22096=CARTESIAN_POINT('',(0.00534537412216198,0.0140958393385013,0.0034648487744155));
#22097=CARTESIAN_POINT('',(0.00607698162277769,0.014147570671835,0.00191010384640304));
#22098=CARTESIAN_POINT('',(0.00628179924349266,0.0141734363385019,0.00105697698638061));
#22099=CARTESIAN_POINT('',(0.00633577167325347,0.0142251676718357,-0.000660453845968885));
#22100=CARTESIAN_POINT('',(0.00618492648229931,0.0142510333385026,-0.00152475781829594));
#22101=CARTESIAN_POINT('',(0.00555238592024544,0.0143027646718364,-0.00312237290991358));
#22102=CARTESIAN_POINT('',(0.00507069054914573,0.0143286303385033,-0.00385568402920415));
#22103=CARTESIAN_POINT('',(0.00385568403518145,0.0143803616718371,-0.00507069055515418));
#22104=CARTESIAN_POINT('',(0.00312237289231687,0.014406227338504,-0.00555238596181364));
#22105=CARTESIAN_POINT('',(0.00152475783585189,0.0144579586718377,-0.00618492644074726));
#22106=CARTESIAN_POINT('',(0.000660453922251477,0.0144838243385045,-0.00633577151302142));
#22107=CARTESIAN_POINT('',(-0.00105697706270651,0.0145355556718381,-0.00628179940372335));
#22108=CARTESIAN_POINT('',(-0.00191010413406409,0.0145614213385048,-0.00607698222215112));
#22109=CARTESIAN_POINT('',(-0.00346484848679293,0.0146131526718383,-0.00534537352277043));
#22110=CARTESIAN_POINT('',(-0.0041664657681642,0.0146390183385049,-0.00481858200496197));
#22111=CARTESIAN_POINT('',(-0.00530278635263212,0.0146907496718381,-0.00352968672051604));
#22112=CARTESIAN_POINT('',(-0.00573748965572876,0.0147166153385046,-0.00276758295387855));
#22113=CARTESIAN_POINT('',(-0.0062684575946753,0.0147683466718376,-0.00113338577972021));
#22114=CARTESIAN_POINT('',(-0.0063647222305252,0.014794212338504,-0.000261292372199345));
#22115=CARTESIAN_POINT('',(-0.00622792473072616,0.0148379851243551,0.00118613325892089));
#22116=CARTESIAN_POINT('',(-0.0060870788531847,0.0148558922435399,0.00177021266515919));
#22117=CARTESIAN_POINT('',(-0.00586834292136768,0.0148737993627246,0.0023234413277993));
#22118=CARTESIAN_POINT('',(-0.00586834136008259,0.0138052138913639,0.00232344526570579));
#22119=CARTESIAN_POINT('',(-0.00564908206277401,0.0138231209680448,0.00287646519466028));
#22120=CARTESIAN_POINT('',(-0.00535192496700203,0.0138410280447258,0.00339865503213973));
#22121=CARTESIAN_POINT('',(-0.00446081589110761,0.0138848007880731,0.00454742612487075));
#22122=CARTESIAN_POINT('',(-0.00379365297342232,0.0139106664547395,0.00511725718126046));
#22123=CARTESIAN_POINT('',(-0.00228790905767161,0.0139623977880724,0.00594506308629448));
#22124=CARTESIAN_POINT('',(-0.00144932805960617,0.013988263454739,0.00620303793493879));
#22125=CARTESIAN_POINT('',(0.000261323533980394,0.0140399947880722,0.00636473719382177));
#22126=CARTESIAN_POINT('',(0.00113339412950152,0.0140658604547388,0.00626846160406045));
#22127=CARTESIAN_POINT('',(0.00276757460413525,0.0141175917880722,0.00573748564633127));
#22128=CARTESIAN_POINT('',(0.00352968448324786,0.014143457454739,0.00530278527836341));
#22129=CARTESIAN_POINT('',(0.00481858424226122,0.0141951887880726,0.00416646684240553));
#22130=CARTESIAN_POINT('',(0.00534537412216197,0.0142210544547394,0.0034648487744155));
#22131=CARTESIAN_POINT('',(0.00607698162277769,0.0142727857880731,0.00191010384640304));
#22132=CARTESIAN_POINT('',(0.00628179924349266,0.01429865145474,0.00105697698638061));
#22133=CARTESIAN_POINT('',(0.00633577167325347,0.0143503827880738,-0.000660453845968886));
#22134=CARTESIAN_POINT('',(0.00618492648229931,0.0143762484547407,-0.00152475781829595));
#22135=CARTESIAN_POINT('',(0.00555238592024544,0.0144279797880745,-0.00312237290991358));
#22136=CARTESIAN_POINT('',(0.00507069054914573,0.0144538454547414,-0.00385568402920414));
#22137=CARTESIAN_POINT('',(0.00385568403518145,0.0145055767880752,-0.00507069055515416));
#22138=CARTESIAN_POINT('',(0.00312237289231689,0.014531442454742,-0.00555238596181362));
#22139=CARTESIAN_POINT('',(0.0015247578358519,0.0145831737880757,-0.00618492644074725));
#22140=CARTESIAN_POINT('',(0.000660453922251479,0.0146090394547426,-0.00633577151302142));
#22141=CARTESIAN_POINT('',(-0.00105697706270651,0.0146607707880762,-0.00628179940372335));
#22142=CARTESIAN_POINT('',(-0.00191010413406409,0.0146866364547429,-0.00607698222215112));
#22143=CARTESIAN_POINT('',(-0.00346484848679293,0.0147383677880763,-0.00534537352277043));
#22144=CARTESIAN_POINT('',(-0.0041664657681642,0.014764233454743,-0.00481858200496198));
#22145=CARTESIAN_POINT('',(-0.00530278635263212,0.0148159647880762,-0.00352968672051604));
#22146=CARTESIAN_POINT('',(-0.00573748965572876,0.0148418304547427,-0.00276758295387855));
#22147=CARTESIAN_POINT('',(-0.0062684575946753,0.0148935617880757,-0.0011333857797202));
#22148=CARTESIAN_POINT('',(-0.0063647222305252,0.0149194274547421,-0.000261292372199344));
#22149=CARTESIAN_POINT('',(-0.00622792473072616,0.0149632002405932,0.00118613325892089));
#22150=CARTESIAN_POINT('',(-0.0060870788531847,0.014981107359778,0.00177021266515919));
#22151=CARTESIAN_POINT('',(-0.00586834292136768,0.0149990144789627,0.0023234413277993));
#22152=CARTESIAN_POINT('',(-0.00586834159873206,0.0138055280127714,0.00232344536019399));
#22153=CARTESIAN_POINT('',(-0.0056490822925068,0.0138234350894524,0.00287646531163829));
#22154=CARTESIAN_POINT('',(-0.00535192518465025,0.0138413421661333,0.00339865517035378));
#22155=CARTESIAN_POINT('',(-0.00446081607251684,0.0138851149094806,0.00454742630980219));
#22156=CARTESIAN_POINT('',(-0.00379365312769986,0.0139109805761471,0.00511725738936538));
#22157=CARTESIAN_POINT('',(-0.00228790915071464,0.01396271190948,0.00594506332806401));
#22158=CARTESIAN_POINT('',(-0.00144932811854639,0.0139885775761465,0.00620303818719946));
#22159=CARTESIAN_POINT('',(0.00026132354460771,0.0140403089094797,0.00636473745265831));
#22160=CARTESIAN_POINT('',(0.00113339417559357,0.0140661745761464,0.00626846185898172));
#22161=CARTESIAN_POINT('',(0.00276757471668497,0.0141179059094798,0.00573748587965919));
#22162=CARTESIAN_POINT('',(0.00352968462679052,0.0141437715761466,0.00530278549401325));
#22163=CARTESIAN_POINT('',(0.00481858443821992,0.0141955029094801,0.00416646701184439));
#22164=CARTESIAN_POINT('',(0.00534537433954379,0.014221368576147,0.00346484891532146));
#22165=CARTESIAN_POINT('',(0.00607698186991199,0.0142730999094807,0.00191010392408176));
#22166=CARTESIAN_POINT('',(0.00628179949895633,0.0142989655761476,0.00105697702936498));
#22167=CARTESIAN_POINT('',(0.00633577193091206,0.0143506969094813,-0.000660453872827746));
#22168=CARTESIAN_POINT('',(0.00618492673382343,0.0143765625761482,-0.0015247578803037));
#22169=CARTESIAN_POINT('',(0.00555238614604586,0.014428293909482,-0.00312237303689198));
#22170=CARTESIAN_POINT('',(0.00507069075535691,0.0144541595761489,-0.00385568418600431));
#22171=CARTESIAN_POINT('',(0.00385568419198163,0.0145058909094827,-0.00507069076136534));
#22172=CARTESIAN_POINT('',(0.00312237301929529,0.0145317565761496,-0.00555238618761404));
#22173=CARTESIAN_POINT('',(0.00152475789785965,0.0145834879094833,-0.00618492669227137));
#22174=CARTESIAN_POINT('',(0.000660453949110342,0.0146093535761501,-0.00633577177068));
#22175=CARTESIAN_POINT('',(-0.00105697710569089,0.0146610849094837,-0.00628179965918703));
#22176=CARTESIAN_POINT('',(-0.00191010421174282,0.0146869505761505,-0.00607698246928544));
#22177=CARTESIAN_POINT('',(-0.00346484862769889,0.0147386819094839,-0.00534537374015222));
#22178=CARTESIAN_POINT('',(-0.00416646593760302,0.0147645475761506,-0.00481858220092059));
#22179=CARTESIAN_POINT('',(-0.00530278656828201,0.0148162789094838,-0.00352968686405879));
#22180=CARTESIAN_POINT('',(-0.00573748988905685,0.0148421445761503,-0.00276758306642861));
#22181=CARTESIAN_POINT('',(-0.00626845784959641,0.0148938759094832,-0.00113338582581192));
#22182=CARTESIAN_POINT('',(-0.00636472248936113,0.0149197415761496,-0.000261292382825393));
#22183=CARTESIAN_POINT('',(-0.00622792498399891,0.0149635143620007,0.0011861333071577));
#22184=CARTESIAN_POINT('',(-0.00608707910072962,0.0149814214811855,0.00177021273714892));
#22185=CARTESIAN_POINT('',(-0.00586834316001721,0.0149993286003702,0.00232344142228734));
#22186=CARTESIAN_POINT('',(-0.00586834207591637,0.0138058421337995,0.00232344554912499));
#22187=CARTESIAN_POINT('',(-0.00564908275186204,0.0138237492104805,0.00287646554553812));
#22188=CARTESIAN_POINT('',(-0.00535192561984214,0.0138416562871614,0.00339865544671549));
#22189=CARTESIAN_POINT('',(-0.00446081643524819,0.0138854290305087,0.00454742667957625));
#22190=CARTESIAN_POINT('',(-0.00379365343618084,0.0139112946971751,0.00511725780547526));
#22191=CARTESIAN_POINT('',(-0.00228790933675601,0.0139630260305081,0.00594506381148695));
#22192=CARTESIAN_POINT('',(-0.00144932823639854,0.0139888916971746,0.00620303869159962));
#22193=CARTESIAN_POINT('',(0.000261323565857239,0.0140406230305078,0.00636473797020705));
#22194=CARTESIAN_POINT('',(0.00113339426775554,0.0140664886971744,0.00626846236870181));
#22195=CARTESIAN_POINT('',(0.00276757494173037,0.0141182200305079,0.00573748634620296));
#22196=CARTESIAN_POINT('',(0.00352968491380689,0.0141440856971746,0.00530278592520935));
#22197=CARTESIAN_POINT('',(0.00481858483004321,0.0141958170305082,0.00416646735064073));
#22198=CARTESIAN_POINT('',(0.005345374774203,0.014221682697175,0.00346484919706572));
#22199=CARTESIAN_POINT('',(0.00607698236406188,0.0142734140305088,0.0019101040794019));
#22200=CARTESIAN_POINT('',(0.00628180000976098,0.0142992796971756,0.00105697711531309));
#22201=CARTESIAN_POINT('',(0.00633577244610547,0.0143510110305094,-0.000660453926532565));
#22202=CARTESIAN_POINT('',(0.00618492723675087,0.0143768766971763,-0.00152475800428941));
#22203=CARTESIAN_POINT('',(0.00555238659753824,0.0144286080305101,-0.0031223732907878));
#22204=CARTESIAN_POINT('',(0.00507069116768023,0.014454473697177,-0.00385568449952934));
#22205=CARTESIAN_POINT('',(0.00385568450550666,0.0145062050305108,-0.00507069117368866));
#22206=CARTESIAN_POINT('',(0.00312237327319112,0.0145320706971777,-0.00555238663910643));
#22207=CARTESIAN_POINT('',(0.00152475802184537,0.0145838020305114,-0.0061849271951988));
#22208=CARTESIAN_POINT('',(0.000660454002815167,0.0146096676971782,-0.0063357722858734));
#22209=CARTESIAN_POINT('',(-0.00105697719163901,0.0146613990305118,-0.00628180016999169));
#22210=CARTESIAN_POINT('',(-0.00191010436706298,0.0146872646971786,-0.00607698296343539));
#22211=CARTESIAN_POINT('',(-0.00346484890944312,0.014738996030512,-0.00534537417481139));
#22212=CARTESIAN_POINT('',(-0.00416646627639928,0.0147648616971786,-0.00481858259274369));
#22213=CARTESIAN_POINT('',(-0.0053027869994782,0.0148165930305118,-0.00352968715107534));
#22214=CARTESIAN_POINT('',(-0.00573749035560094,0.0148424586971784,-0.00276758329147468));
#22215=CARTESIAN_POINT('',(-0.00626845835931617,0.0148941900305113,-0.00113338591797321));
#22216=CARTESIAN_POINT('',(-0.00636472300690866,0.0149200556971777,-0.000261292404072388));
#22217=CARTESIAN_POINT('',(-0.00622792549042275,0.0149638284830288,0.00118613340360815));
#22218=CARTESIAN_POINT('',(-0.00608707959570058,0.0149817356022136,0.0017702128810938));
#22219=CARTESIAN_POINT('',(-0.00586834363720165,0.0149996427213983,0.00232344161121802));
#22220=CARTESIAN_POINT('',(-0.00697824898150658,0.0138049000959188,0.00276288964191571));
#22221=CARTESIAN_POINT('',(-0.00697824906356397,0.0136487737981127,0.00276288967440459));
#22222=CARTESIAN_POINT('',(-0.00685805201880862,0.013337416869826,0.00271530020449264));
#22223=CARTESIAN_POINT('',(-0.00642329517116088,0.0131436916720262,0.00254316745395578));
#22224=CARTESIAN_POINT('',(-0.00598853832329639,0.0133374168692714,0.00237103470333308));
#22225=CARTESIAN_POINT('',(-0.00586834127820382,0.0136487737974034,0.00232344523328764));
#22226=CARTESIAN_POINT('',(-0.00586834136008268,0.0138049000952095,0.00232344526570583));
#22227=CARTESIAN_POINT('',(-0.00586849431301164,0.0138048999661087,0.00232350129736579));
#22228=CARTESIAN_POINT('',(-0.00697843088154052,0.0138048999657524,0.00276295622455691));
#22229=CARTESIAN_POINT('',(-0.00586834293970373,0.0138048997127905,0.00232344128155169));
#22230=CARTESIAN_POINT('',(-0.00525929270757257,0.0138546414019838,0.00385960227976077));
#22231=CARTESIAN_POINT('',(-0.00277900226167641,0.013954124780371,0.00641767178053703));
#22232=CARTESIAN_POINT('',(0.00257509559256523,0.0141033498479532,0.00650393974269634));
#22233=CARTESIAN_POINT('',(0.00641940303122683,0.0142525749155366,0.00277792062510722));
#22234=CARTESIAN_POINT('',(0.00650365220007484,0.0144017999831204,-0.0025749745534683));
#22235=CARTESIAN_POINT('',(0.00277793188520664,0.0145510250507043,-0.00641939815574492));
#22236=CARTESIAN_POINT('',(-0.00257508315426317,0.0147002501182876,-0.00650394466354535));
#22237=CARTESIAN_POINT('',(-0.00641900150925783,0.0148494751858699,-0.00277592942708743));
#22238=CARTESIAN_POINT('',(-0.0064759396950849,0.0149489585642571,0.000786698577753388));
#22239=CARTESIAN_POINT('',(-0.00586834507057426,0.0149987002534503,0.00232343589200159));
#22240=CARTESIAN_POINT('',(-0.00697825340504447,0.0149987003172936,0.00276287846683115));
#22241=CARTESIAN_POINT('',(-0.00770076531559239,0.0149489586280798,0.000935490630701186));
#22242=CARTESIAN_POINT('',(-0.00763305811880626,0.0148494752496517,-0.00330095434255674));
#22243=CARTESIAN_POINT('',(-0.00306212097811945,0.014700250182008,-0.00773406700938429));
#22244=CARTESIAN_POINT('',(0.0033033355401448,0.0145510251143632,-0.00763352978283033));
#22245=CARTESIAN_POINT('',(0.00773371923288734,0.0144018000467179,-0.00306199183214668));
#22246=CARTESIAN_POINT('',(0.00763353557833258,0.0142525749790727,0.00330332215531694));
#22247=CARTESIAN_POINT('',(0.00306213575895693,0.0141033499114279,0.00773406116183527));
#22248=CARTESIAN_POINT('',(-0.00330460837197012,0.0139541248437842,0.00763147688575125));
#22249=CARTESIAN_POINT('',(-0.00625400805880451,0.0138546414653561,0.00458958737822419));
#22250=CARTESIAN_POINT('',(-0.00697825087833439,0.0138048997761423,0.00276288485769634));
#22251=CARTESIAN_POINT('',(-0.0060046989412083,-0.00989161587683944,-0.00195124705900381));
#22252=CARTESIAN_POINT('',(-0.00574417341912455,-0.0100289714560031,-0.00275297912024915));
#22253=CARTESIAN_POINT('',(-0.00532098773851402,-0.0101627927695994,-0.00350163042607414));
#22254=CARTESIAN_POINT('',(-0.00421612753807775,-0.0104233668656572,-0.00477475344855832));
#22255=CARTESIAN_POINT('',(-0.00353445301825201,-0.0105501196481187,-0.00529922516521753));
#22256=CARTESIAN_POINT('',(-0.00202057350610914,-0.0107965566819069,-0.00604082678144128));
#22257=CARTESIAN_POINT('',(-0.00118836851379201,-0.0109162409332336,-0.00625795668100582));
#22258=CARTESIAN_POINT('',(0.000494838502468597,-0.0111485409047524,-0.00635053704198387));
#22259=CARTESIAN_POINT('',(0.00134584052641207,-0.0112611566249443,-0.00622598750339738));
#22260=CARTESIAN_POINT('',(0.0029319176516602,-0.0114793195341935,-0.00565491662083544));
#22261=CARTESIAN_POINT('',(0.00366699275296484,-0.0115848667232507,-0.00520839527685999));
#22262=CARTESIAN_POINT('',(0.00490484825389108,-0.0117888925702303,-0.00406407147112351));
#22263=CARTESIAN_POINT('',(0.00540762865351265,-0.0118873712281527,-0.00336626900936249));
#22264=CARTESIAN_POINT('',(0.0061013001303894,-0.0120772600128628,-0.00182985032013212));
#22265=CARTESIAN_POINT('',(0.00629219120764457,-0.0121686701396505,-0.000991234092662768));
#22266=CARTESIAN_POINT('',(0.00633186442354634,-0.012344421862091,0.000694051892870558));
#22267=CARTESIAN_POINT('',(0.00618064656219294,-0.0124287634577439,0.00154072165093454));
#22268=CARTESIAN_POINT('',(0.00556004095928272,-0.0125903781179149,0.00310807973892309));
#22269=CARTESIAN_POINT('',(0.00509065321772592,-0.012667651182433,0.00382876806884765));
#22270=CARTESIAN_POINT('',(0.00390801589266107,-0.0128151287803345,0.00503007226615351));
#22271=CARTESIAN_POINT('',(0.00319476630915303,-0.0128853333137179,0.00551068813353479));
#22272=CARTESIAN_POINT('',(0.0016373188335356,-0.0130186738493498,0.00615576166977231));
#22273=CARTESIAN_POINT('',(0.000793120941426222,-0.0130818098515984,0.00632021933862854));
#22274=CARTESIAN_POINT('',(-0.000892579781795836,-0.0132010133249608,0.0063069420913346));
#22275=CARTESIAN_POINT('',(-0.00173408261290851,-0.0132570807960746,0.00612920717518441));
#22276=CARTESIAN_POINT('',(-0.00328117503347942,-0.0133621472071675,0.00545967925016396));
#22277=CARTESIAN_POINT('',(-0.00398676462293764,-0.0134111461471466,0.0049678862412937));
#22278=CARTESIAN_POINT('',(-0.00515033405494463,-0.0135020754959699,0.00374810627762913));
#22279=CARTESIAN_POINT('',(-0.00560831389749338,-0.0135440059048142,0.00302011932283482));
#22280=CARTESIAN_POINT('',(-0.00620414568196542,-0.013620798191368,0.00144316383230204));
#22281=CARTESIAN_POINT('',(-0.00634199762388869,-0.0136556600690776,0.000594195296563549));
#22282=CARTESIAN_POINT('',(-0.0062758104309332,-0.0137183152933619,-0.00109019704146796));
#22283=CARTESIAN_POINT('',(-0.00607177129605443,-0.0137461086399366,-0.00192562084376098));
#22284=CARTESIAN_POINT('',(-0.00571282530871555,-0.013770367720944,-0.00268838268330946));
#22285=CARTESIAN_POINT('',(-0.00600351494261159,-0.00990699069817707,-0.00195086231468902));
#22286=CARTESIAN_POINT('',(-0.00574304079060577,-0.0100443462773407,-0.00275243629146672));
#22287=CARTESIAN_POINT('',(-0.00531993855318813,-0.010178167590937,-0.00350093997921721));
#22288=CARTESIAN_POINT('',(-0.00421529620762514,-0.0104387416869948,-0.00477381196898739));
#22289=CARTESIAN_POINT('',(-0.00353375609947977,-0.0105654944694563,-0.00529818027100706));
#22290=CARTESIAN_POINT('',(-0.00202017509209718,-0.0108119315032446,-0.0060396356592048));
#22291=CARTESIAN_POINT('',(-0.00118813419285994,-0.0109316157545713,-0.00625672274538287));
#22292=CARTESIAN_POINT('',(0.000494740930867046,-0.0111639157260901,-0.00634928485148777));
#22293=CARTESIAN_POINT('',(0.00134557515535679,-0.011276531446282,-0.0062247598714146));
#22294=CARTESIAN_POINT('',(0.00293133954001475,-0.0114946943555312,-0.00565380159185411));
#22295=CARTESIAN_POINT('',(0.00366626970018299,-0.0116002415445884,-0.00520736829236679));
#22296=CARTESIAN_POINT('',(0.00490388112239846,-0.0118042673915681,-0.0040632701228851));
#22297=CARTESIAN_POINT('',(0.00540656238444571,-0.0119027460494905,-0.00336560525289072));
#22298=CARTESIAN_POINT('',(0.00610009708409794,-0.0120926348342006,-0.00182948951266575));
#22299=CARTESIAN_POINT('',(0.00629095052170294,-0.0121840449609883,-0.000991038642435168));
#22300=CARTESIAN_POINT('',(0.00633061591489246,-0.0123597966834289,0.000693915040636124));
#22301=CARTESIAN_POINT('',(0.00617942787047698,-0.0124441382790818,0.00154041785347683));
#22302=CARTESIAN_POINT('',(0.00555894463775888,-0.0126057529392528,0.00310746689187024));
#22303=CARTESIAN_POINT('',(0.00508964944945624,-0.0126830260037709,0.00382801311742294));
#22304=CARTESIAN_POINT('',(0.00390724531525524,-0.0128305036016724,0.00502908044315575));
#22305=CARTESIAN_POINT('',(0.0031941363693569,-0.0129007081350558,0.00550960154333586));
#22306=CARTESIAN_POINT('',(0.00163699598917317,-0.0130340486706877,0.00615454788482654));
#22307=CARTESIAN_POINT('',(0.000792964554887801,-0.0130971846729363,0.0063189731261371));
#22308=CARTESIAN_POINT('',(-0.000892403784094794,-0.0132163881462987,0.00630569849683322));
#22309=CARTESIAN_POINT('',(-0.00173374068879202,-0.0132724556174126,0.00612799862621877));
#22310=CARTESIAN_POINT('',(-0.00328052805572528,-0.0133775220285054,0.0054586027178292));
#22311=CARTESIAN_POINT('',(-0.00398597851796133,-0.0134265209684845,0.00496690668005409));
#22312=CARTESIAN_POINT('',(-0.00514931851888639,-0.0135174503173078,0.00374736723098974));
#22313=CARTESIAN_POINT('',(-0.00560720805757541,-0.0135593807261521,0.0030195238197005));
#22314=CARTESIAN_POINT('',(-0.0062029223567241,-0.0136361730127058,0.001442879271166));
#22315=CARTESIAN_POINT('',(-0.00634074711718376,-0.0136710348904153,0.000594078133920726));
#22316=CARTESIAN_POINT('',(-0.00627457297493145,-0.0137336901146996,-0.00108998207785698));
#22317=CARTESIAN_POINT('',(-0.00607057407221948,-0.0137614834612743,-0.00192524115238941));
#22318=CARTESIAN_POINT('',(-0.00571169886137573,-0.0137857425422816,-0.00268785259156703));
#22319=CARTESIAN_POINT('',(-0.00600291424347733,-0.00992240968822442,-0.00195066711549076));
#22320=CARTESIAN_POINT('',(-0.00574246615396974,-0.0100597652673881,-0.00275216088845478));
#22321=CARTESIAN_POINT('',(-0.00531940625127604,-0.0101935865809844,-0.0035005896824936));
#22322=CARTESIAN_POINT('',(-0.00421487443391311,-0.0104541606770422,-0.00477333431135777));
#22323=CARTESIAN_POINT('',(-0.00353340251924388,-0.0105809134595037,-0.00529765014618313));
#22324=CARTESIAN_POINT('',(-0.00201997295760755,-0.010827350493292,-0.00603903134590728));
#22325=CARTESIAN_POINT('',(-0.00118801531064046,-0.0109470347446187,-0.00625609671080606));
#22326=CARTESIAN_POINT('',(0.000494691428125452,-0.0111793347161375,-0.00634864955534044));
#22327=CARTESIAN_POINT('',(0.00134544051992427,-0.0112919504363294,-0.00622413703497603));
#22328=CARTESIAN_POINT('',(0.00293104623631838,-0.0115101133455787,-0.00565323588430545));
#22329=CARTESIAN_POINT('',(0.00366590286091367,-0.0116156605346359,-0.00520684725399928));
#22330=CARTESIAN_POINT('',(0.0049033904503217,-0.0118196863816156,-0.00406286356058477));
#22331=CARTESIAN_POINT('',(0.00540602141513444,-0.011918165039538,-0.00336526849747643));
#22332=CARTESIAN_POINT('',(0.00609948672115684,-0.0121080538242481,-0.00182930645777592));
#22333=CARTESIAN_POINT('',(0.0062903210623665,-0.0121994639510358,-0.000990939481183764));
#22334=CARTESIAN_POINT('',(0.00632998248671984,-0.0123752156734764,0.000693845608950162));
#22335=CARTESIAN_POINT('',(0.00617880956986351,-0.0124595572691293,0.00154026372249193));
#22336=CARTESIAN_POINT('',(0.00555838842139842,-0.0126211719293004,0.00310715596523984));
#22337=CARTESIAN_POINT('',(0.00508914018978966,-0.0126984449938185,0.00382763009444597));
#22338=CARTESIAN_POINT('',(0.00390685436447048,-0.01284592259172,0.00502857724389711));
#22339=CARTESIAN_POINT('',(0.00319381677076005,-0.0129161271251034,0.00550905026414212));
#22340=CARTESIAN_POINT('',(0.00163683219478224,-0.0130494676607354,0.00615393207365233));
#22341=CARTESIAN_POINT('',(0.000792885212514845,-0.0131126036629839,0.00631834086291754));
#22342=CARTESIAN_POINT('',(-0.000892314492040781,-0.0132318071363464,0.00630506756184527));
#22343=CARTESIAN_POINT('',(-0.00173356721432902,-0.0132878746074602,0.00612738547150779));
#22344=CARTESIAN_POINT('',(-0.0032801998129572,-0.013392941018553,0.00545805654147115));
#22345=CARTESIAN_POINT('',(-0.00398557968929714,-0.013441939958532,0.004966409701772));
#22346=CARTESIAN_POINT('',(-0.00514880328885766,-0.0135328693073553,0.0037469922772713));
#22347=CARTESIAN_POINT('',(-0.00560664701207823,-0.0135747997161996,0.00301922169246975));
#22348=CARTESIAN_POINT('',(-0.00620230170530153,-0.0136515920027533,0.0014427348996874));
#22349=CARTESIAN_POINT('',(-0.00634011267530426,-0.0136864538804628,0.0005940186917066));
#22350=CARTESIAN_POINT('',(-0.00627394515429805,-0.013749109104747,-0.0010898730165326));
#22351=CARTESIAN_POINT('',(-0.00606996666328913,-0.0137769024513216,-0.00192504851679101));
#22352=CARTESIAN_POINT('',(-0.00571112736074751,-0.0138011615323289,-0.00268758365066487));
#22353=CARTESIAN_POINT('',(-0.00600291424347732,-0.0100937412712376,-0.00195066711549076));
#22354=CARTESIAN_POINT('',(-0.00574246615396973,-0.0102310968504013,-0.00275216088845478));
#22355=CARTESIAN_POINT('',(-0.00531940625127603,-0.0103649181639975,-0.00350058968249358));
#22356=CARTESIAN_POINT('',(-0.0042148744339131,-0.0106254922600554,-0.00477333431135776));
#22357=CARTESIAN_POINT('',(-0.00353340251924387,-0.010752245042517,-0.00529765014618313));
#22358=CARTESIAN_POINT('',(-0.00201997295760755,-0.0109986820763054,-0.00603903134590728));
#22359=CARTESIAN_POINT('',(-0.00118801531064047,-0.0111183663276323,-0.00625609671080605));
#22360=CARTESIAN_POINT('',(0.000494691428125445,-0.0113506662991512,-0.00634864955534043));
#22361=CARTESIAN_POINT('',(0.00134544051992427,-0.0114632820193433,-0.00622413703497602));
#22362=CARTESIAN_POINT('',(0.00293104623631838,-0.0116814449285928,-0.00565323588430546));
#22363=CARTESIAN_POINT('',(0.00366590286091366,-0.0117869921176501,-0.00520684725399929));
#22364=CARTESIAN_POINT('',(0.00490339045032169,-0.0119910179646301,-0.00406286356058478));
#22365=CARTESIAN_POINT('',(0.00540602141513444,-0.0120894966225526,-0.00336526849747642));
#22366=CARTESIAN_POINT('',(0.00609948672115685,-0.012279385407263,-0.00182930645777591));
#22367=CARTESIAN_POINT('',(0.0062903210623665,-0.0123707955340508,-0.000990939481183761));
#22368=CARTESIAN_POINT('',(0.00632998248671984,-0.0125465472564916,0.000693845608950159));
#22369=CARTESIAN_POINT('',(0.00617880956986352,-0.0126308888521447,0.00154026372249192));
#22370=CARTESIAN_POINT('',(0.00555838842139841,-0.0127925035123159,0.00310715596523981));
#22371=CARTESIAN_POINT('',(0.00508914018978966,-0.0128697765768341,0.00382763009444594));
#22372=CARTESIAN_POINT('',(0.00390685436447047,-0.0130172541747358,0.0050285772438971));
#22373=CARTESIAN_POINT('',(0.00319381677076006,-0.0130874587081192,0.0055090502641421));
#22374=CARTESIAN_POINT('',(0.00163683219478224,-0.0132207992437512,0.00615393207365233));
#22375=CARTESIAN_POINT('',(0.000792885212514844,-0.0132839352459997,0.00631834086291754));
#22376=CARTESIAN_POINT('',(-0.000892314492040773,-0.0134031387193621,0.00630506756184528));
#22377=CARTESIAN_POINT('',(-0.00173356721432899,-0.0134592061904759,0.00612738547150781));
#22378=CARTESIAN_POINT('',(-0.00328019981295716,-0.0135642726015686,0.00545805654147116));
#22379=CARTESIAN_POINT('',(-0.00398557968929713,-0.0136132715415475,0.004966409701772));
#22380=CARTESIAN_POINT('',(-0.00514880328885766,-0.0137042008903706,0.00374699227727129));
#22381=CARTESIAN_POINT('',(-0.00560664701207822,-0.0137461312992146,0.00301922169246975));
#22382=CARTESIAN_POINT('',(-0.00620230170530152,-0.0138229235857679,0.0014427348996874));
#22383=CARTESIAN_POINT('',(-0.00634011267530425,-0.0138577854634772,0.000594018691706603));
#22384=CARTESIAN_POINT('',(-0.00627394515429805,-0.0139204406877607,-0.0010898730165326));
#22385=CARTESIAN_POINT('',(-0.00606996666328912,-0.0139482340343351,-0.001925048516791));
#22386=CARTESIAN_POINT('',(-0.0057111273607475,-0.013972493115342,-0.00268758365066487));
#22387=CARTESIAN_POINT('',(-0.00606433392192398,-0.0102496538642035,-0.0019706256459862));
#22388=CARTESIAN_POINT('',(-0.00580122102041663,-0.0103870094433671,-0.00278032001749549));
#22389=CARTESIAN_POINT('',(-0.0053738325196232,-0.0105208307569634,-0.00353640646813335));
#22390=CARTESIAN_POINT('',(-0.00425799952648047,-0.0107814048530212,-0.00482217336629522));
#22391=CARTESIAN_POINT('',(-0.00356955503413119,-0.0109081576354828,-0.00535185381381923));
#22392=CARTESIAN_POINT('',(-0.00204064060077138,-0.0111545946692711,-0.00610082056166993));
#22393=CARTESIAN_POINT('',(-0.00120017065976085,-0.0112742789205979,-0.00632010686199661));
#22394=CARTESIAN_POINT('',(0.000499752934456115,-0.0115065788921167,-0.00641360667424035));
#22395=CARTESIAN_POINT('',(0.00135920658766256,-0.0116191946123087,-0.0062878201861574));
#22396=CARTESIAN_POINT('',(0.0029610356564642,-0.011837357521558,-0.00571107777844453));
#22397=CARTESIAN_POINT('',(0.00370341107205939,-0.0119429047106153,-0.0052601218588146));
#22398=CARTESIAN_POINT('',(0.00495356019330685,-0.012146930557595,-0.00410443333208948));
#22399=CARTESIAN_POINT('',(0.00546133389895912,-0.0122454092155175,-0.00339970072499429));
#22400=CARTESIAN_POINT('',(0.00616189449476616,-0.0124352980002277,-0.00184802326928778));
#22401=CARTESIAN_POINT('',(0.00635468138492093,-0.0125267081270155,-0.00100107842067645));
#22402=CARTESIAN_POINT('',(0.0063947486108286,-0.0127024598494561,0.000700944789858774));
#22403=CARTESIAN_POINT('',(0.0062420289465815,-0.0127868014451091,0.00155602315178267));
#22404=CARTESIAN_POINT('',(0.005615259870111,-0.0129484161052802,0.00313894727734728));
#22405=CARTESIAN_POINT('',(0.00514121045788761,-0.0130256891697984,0.00386679304098799));
#22406=CARTESIAN_POINT('',(0.00394682790549922,-0.0131731667676999,0.00508002785352392));
#22407=CARTESIAN_POINT('',(0.00322649476533423,-0.0132433713010833,0.00556541690241914));
#22408=CARTESIAN_POINT('',(0.00165357967825393,-0.0133767118367152,0.00621689691269813));
#22409=CARTESIAN_POINT('',(0.00080099773133863,-0.0134398478389638,0.0063829878740819));
#22410=CARTESIAN_POINT('',(-0.000901444335805242,-0.0135590513123262,0.00636957876532512));
#22411=CARTESIAN_POINT('',(-0.00175130445603381,-0.01361511878344,0.00619007869518455));
#22412=CARTESIAN_POINT('',(-0.0033137616480228,-0.0137201851945328,0.00551390143015753));
#22413=CARTESIAN_POINT('',(-0.00402635871978323,-0.0137691841345118,0.00501722423527106));
#22414=CARTESIAN_POINT('',(-0.00520148400851484,-0.013860113483335,0.00378533016641609));
#22415=CARTESIAN_POINT('',(-0.00566401222548603,-0.0139020438921792,0.00305011329244757));
#22416=CARTESIAN_POINT('',(-0.00626576144517416,-0.0139788361787328,0.00145749644883311));
#22417=CARTESIAN_POINT('',(-0.00640498244789111,-0.0140136980564422,0.000600096479187168));
#22418=CARTESIAN_POINT('',(-0.00633813792439929,-0.0140763532807262,-0.00110102420868829));
#22419=CARTESIAN_POINT('',(-0.00613207239819051,-0.0141041466273008,-0.0019447449269178));
#22420=CARTESIAN_POINT('',(-0.00576956157983471,-0.0141284057083079,-0.00271508204843087));
#22421=CARTESIAN_POINT('',(-0.00627403382107316,-0.0104701475677205,-0.00203876833148874));
#22422=CARTESIAN_POINT('',(-0.00600182268229503,-0.0106075031468842,-0.00287646129777087));
#22423=CARTESIAN_POINT('',(-0.00555965542316345,-0.0107413244604805,-0.0036586926234252));
#22424=CARTESIAN_POINT('',(-0.00440523780240261,-0.0110018985565383,-0.00498892033003615));
#22425=CARTESIAN_POINT('',(-0.00369298744077334,-0.0111286513389998,-0.00553691671099277));
#22426=CARTESIAN_POINT('',(-0.00211120434836357,-0.011375088372788,-0.00631178214013517));
#22427=CARTESIAN_POINT('',(-0.00124167161758307,-0.0114947726241148,-0.00653865118832096));
#22428=CARTESIAN_POINT('',(0.00051703399801631,-0.0117270725956335,-0.00663538415056112));
#22429=CARTESIAN_POINT('',(0.00140620688283519,-0.0118396883158255,-0.00650524806461549));
#22430=CARTESIAN_POINT('',(0.00306342594145377,-0.0120578512250747,-0.00590856235788749));
#22431=CARTESIAN_POINT('',(0.00383147211525347,-0.0121633984141319,-0.00544201273710512));
#22432=CARTESIAN_POINT('',(0.00512485041022755,-0.0123674242611115,-0.00424636140974563));
#22433=CARTESIAN_POINT('',(0.00565018253140191,-0.0124659029190339,-0.00351725970316851));
#22434=CARTESIAN_POINT('',(0.00637496796182063,-0.0126557917037441,-0.00191192646099593));
#22435=CARTESIAN_POINT('',(0.00657442127106498,-0.0127472018305317,-0.00103569492540046));
#22436=CARTESIAN_POINT('',(0.00661587399014308,-0.0129229535529723,0.000725182909598715));
#22437=CARTESIAN_POINT('',(0.00645787339997682,-0.0130072951486252,0.00160982920900241));
#22438=CARTESIAN_POINT('',(0.00580943114161729,-0.0131689098087962,0.00324748960631019));
#22439=CARTESIAN_POINT('',(0.00531898947342402,-0.0132461828733143,0.00400050370421426));
#22440=CARTESIAN_POINT('',(0.00408330611141565,-0.0133936604712158,0.00525569122270414));
#22441=CARTESIAN_POINT('',(0.00333806441760055,-0.0134638650045992,0.00575786464328995));
#22442=CARTESIAN_POINT('',(0.00171075916345863,-0.0135972055402311,0.00643187232012095));
#22443=CARTESIAN_POINT('',(0.000828695603131797,-0.0136603415424797,0.00660370657636615));
#22444=CARTESIAN_POINT('',(-0.00093261557220824,-0.0137795450158421,0.00658983379117099));
#22445=CARTESIAN_POINT('',(-0.00181186318722145,-0.0138356124869559,0.00640412674973063));
#22446=CARTESIAN_POINT('',(-0.00342834892048198,-0.0139406788980488,0.00570456780649976));
#22447=CARTESIAN_POINT('',(-0.00416558703872929,-0.0139896778380279,0.00519071590470924));
#22448=CARTESIAN_POINT('',(-0.00538134723604398,-0.0140806071868512,0.00391622390748699));
#22449=CARTESIAN_POINT('',(-0.00585986931511135,-0.0141225375956955,0.00315558381205526));
#22450=CARTESIAN_POINT('',(-0.00648242654971197,-0.0141993298822493,0.00150789553012803));
#22451=CARTESIAN_POINT('',(-0.00662646170524521,-0.0142341917599588,0.000620847343632541));
#22452=CARTESIAN_POINT('',(-0.00655730575068522,-0.014296846984243,-0.00113909676018287));
#22453=CARTESIAN_POINT('',(-0.00634411464059197,-0.0143246403308177,-0.00201199267750278));
#22454=CARTESIAN_POINT('',(-0.00596906848314891,-0.0143488994118251,-0.00280896745102709));
#22455=CARTESIAN_POINT('',(-0.00642231404177568,-0.0105347286782718,-0.00208695248649585));
#22456=CARTESIAN_POINT('',(-0.00614366947772652,-0.0106720842574354,-0.00294444344900556));
#22457=CARTESIAN_POINT('',(-0.00569105205835654,-0.0108059055710317,-0.0037451619930773));
#22458=CARTESIAN_POINT('',(-0.00450935098575737,-0.0110664796670895,-0.00510682823883964));
#22459=CARTESIAN_POINT('',(-0.00378026733252819,-0.011193232449551,-0.00566777594053021));
#22460=CARTESIAN_POINT('',(-0.00216110045279195,-0.0114396694833393,-0.00646095450283777));
#22461=CARTESIAN_POINT('',(-0.0012710172262849,-0.0115593537346661,-0.00669318536345474));
#22462=CARTESIAN_POINT('',(0.000529253555245836,-0.0117916537061849,-0.00679220450798196));
#22463=CARTESIAN_POINT('',(0.00143944111026952,-0.0119042694263769,-0.00665899279189221));
#22464=CARTESIAN_POINT('',(0.00313582680629751,-0.0121224323356261,-0.00604820504319139));
#22465=CARTESIAN_POINT('',(0.00392202494730184,-0.0122279795246833,-0.00557062901058033));
#22466=CARTESIAN_POINT('',(0.00524597088416309,-0.012432005371663,-0.00434671971589707));
#22467=CARTESIAN_POINT('',(0.00578371868002001,-0.0125304840295855,-0.00360038645382486));
#22468=CARTESIAN_POINT('',(0.00652563365526577,-0.0127203728142956,-0.00195711284119222));
#22469=CARTESIAN_POINT('',(0.0067298008346546,-0.0128117829410833,-0.00106017249063177));
#22470=CARTESIAN_POINT('',(0.00677223324534879,-0.012987534663524,0.00074232184843004));
#22471=CARTESIAN_POINT('',(0.00661049847665415,-0.0130718762591769,0.0016478758369314));
#22472=CARTESIAN_POINT('',(0.005946730964411,-0.0132334909193479,0.00332424062316563));
#22473=CARTESIAN_POINT('',(0.00544469822086248,-0.0133107639838661,0.00409505142089849));
#22474=CARTESIAN_POINT('',(0.00417981077630333,-0.0134582415817676,0.00537990398225753));
#22475=CARTESIAN_POINT('',(0.00341695607529269,-0.013528446115151,0.00589394574588372));
#22476=CARTESIAN_POINT('',(0.00175119116519162,-0.0136617866507829,0.00658388288849797));
#22477=CARTESIAN_POINT('',(0.000848280956101178,-0.0137249226530315,0.00675977826748603));
#22478=CARTESIAN_POINT('',(-0.000954656964846768,-0.0138441261263939,0.00674557761353703));
#22479=CARTESIAN_POINT('',(-0.00185468467670427,-0.0139001935975077,0.00655548158059996));
#22480=CARTESIAN_POINT('',(-0.00350937435787551,-0.0140052600086006,0.00583938929415562));
#22481=CARTESIAN_POINT('',(-0.00426403632718924,-0.0140542589485796,0.00531339304064835));
#22482=CARTESIAN_POINT('',(-0.00550852974391592,-0.0141451882974029,0.0040087797594131));
#22483=CARTESIAN_POINT('',(-0.00599836119132887,-0.0141871187062471,0.00323016273168512));
#22484=CARTESIAN_POINT('',(-0.00663563191437714,-0.0142639109928008,0.00154353306227724));
#22485=CARTESIAN_POINT('',(-0.00678307119001246,-0.0142987728705102,0.000635520420597347));
#22486=CARTESIAN_POINT('',(-0.00671228080686991,-0.0143614280947944,-0.00116601811952175));
#22487=CARTESIAN_POINT('',(-0.00649405114809204,-0.014389221441369,-0.00205954401796095));
#22488=CARTESIAN_POINT('',(-0.00611014116737591,-0.0144134805223763,-0.0028753544558573));
#22489=CARTESIAN_POINT('',(-0.00671887448318071,-0.0105347286782718,-0.00218332079651008));
#22490=CARTESIAN_POINT('',(-0.00642736306858952,-0.0106720842574354,-0.00308040775147493));
#22491=CARTESIAN_POINT('',(-0.0059538453287427,-0.0108059055710317,-0.00391810073238151));
#22492=CARTESIAN_POINT('',(-0.00471757735246687,-0.0110664796670895,-0.0053426440564466));
#22493=CARTESIAN_POINT('',(-0.00395482711603786,-0.011193232449551,-0.00592949439960509));
#22494=CARTESIAN_POINT('',(-0.00226089266164871,-0.0114396694833393,-0.00675929922824295));
#22495=CARTESIAN_POINT('',(-0.00132970844368856,-0.0115593537346661,-0.00700225371372231));
#22496=CARTESIAN_POINT('',(0.000553692669704887,-0.0117916537061849,-0.00710584522282366));
#22497=CARTESIAN_POINT('',(0.00150590956513818,-0.0119042694263769,-0.00696648224644565));
#22498=CARTESIAN_POINT('',(0.00328062853598501,-0.0121224323356261,-0.0063274904137992));
#22499=CARTESIAN_POINT('',(0.00410313061139855,-0.0122279795246833,-0.00582786155753075));
#22500=CARTESIAN_POINT('',(0.00548821183203415,-0.012432005371663,-0.00454743632819994));
#22501=CARTESIAN_POINT('',(0.00605079097725621,-0.0125304840295855,-0.00376663995513757));
#22502=CARTESIAN_POINT('',(0.00682696504215606,-0.0127203728142956,-0.00204748560158481));
#22503=CARTESIAN_POINT('',(0.00704055996183384,-0.0128117829410833,-0.00110912762109441));
#22504=CARTESIAN_POINT('',(0.00708495175576022,-0.012987534663524,0.000776599726092681));
#22505=CARTESIAN_POINT('',(0.00691574863000881,-0.0130718762591769,0.00172396909278938));
#22506=CARTESIAN_POINT('',(0.00622133060999841,-0.0132334909193479,0.00347774265687652));
#22507=CARTESIAN_POINT('',(0.00569611571573941,-0.0133107639838661,0.00428414685426696));
#22508=CARTESIAN_POINT('',(0.00437282010607869,-0.0134582415817676,0.00562832950136433));
#22509=CARTESIAN_POINT('',(0.00357473939067698,-0.013528446115151,0.00616610795107127));
#22510=CARTESIAN_POINT('',(0.0018320551686576,-0.0136617866507829,0.006887904025252));
#22511=CARTESIAN_POINT('',(0.000887451662039945,-0.0137249226530315,0.00707192164972581));
#22512=CARTESIAN_POINT('',(-0.000998739750123817,-0.0138441261263939,0.00705706525826912));
#22513=CARTESIAN_POINT('',(-0.00194032765566992,-0.0139001935975077,0.00685819124233862));
#22514=CARTESIAN_POINT('',(-0.00367142523266258,-0.0140052600086006,0.00610903226946734));
#22515=CARTESIAN_POINT('',(-0.00446093490410914,-0.0140542589485796,0.00555874731252656));
#22516=CARTESIAN_POINT('',(-0.00576289475965981,-0.0141451882974029,0.00419389146326531));
#22517=CARTESIAN_POINT('',(-0.00627534494376392,-0.0141871187062471,0.00337932057094484));
#22518=CARTESIAN_POINT('',(-0.00694204264370749,-0.0142639109928008,0.00161480812657567));
#22519=CARTESIAN_POINT('',(-0.00709629015954695,-0.0142987728705102,0.00066486657452696));
#22520=CARTESIAN_POINT('',(-0.0070222309192393,-0.0143614280947944,-0.00121986083819952));
#22521=CARTESIAN_POINT('',(-0.00679392416309219,-0.014389221441369,-0.00215464669887731));
#22522=CARTESIAN_POINT('',(-0.00639228653582991,-0.0144134805223763,-0.00300812846551772));
#22523=CARTESIAN_POINT('',(-0.00686715470388324,-0.0104701475677205,-0.00223150495151719));
#22524=CARTESIAN_POINT('',(-0.00656920986402103,-0.0106075031468842,-0.00314838990270961));
#22525=CARTESIAN_POINT('',(-0.00608524196393579,-0.0107413244604805,-0.00400457010203361));
#22526=CARTESIAN_POINT('',(-0.00482169053582163,-0.0110018985565383,-0.00546055196525008));
#22527=CARTESIAN_POINT('',(-0.00404210700779271,-0.0111286513389998,-0.00606035362914253));
#22528=CARTESIAN_POINT('',(-0.00231078876607709,-0.011375088372788,-0.00690847159094555));
#22529=CARTESIAN_POINT('',(-0.00135905405239039,-0.0114947726241148,-0.0071567878888561));
#22530=CARTESIAN_POINT('',(0.000565912226934413,-0.0117270725956335,-0.00726266558024451));
#22531=CARTESIAN_POINT('',(0.00153914379257251,-0.0118396883158255,-0.00712022697372237));
#22532=CARTESIAN_POINT('',(0.00335302940082875,-0.0120578512250747,-0.00646713309910309));
#22533=CARTESIAN_POINT('',(0.0041936834434469,-0.0121633984141319,-0.00595647783100596));
#22534=CARTESIAN_POINT('',(0.00560933230596968,-0.0123674242611115,-0.00464779463435138));
#22535=CARTESIAN_POINT('',(0.00618432712587431,-0.0124659029190339,-0.00384976670579392));
#22536=CARTESIAN_POINT('',(0.0069776307356012,-0.012655791703744,-0.00209267198178111));
#22537=CARTESIAN_POINT('',(0.00719593952542346,-0.0127472018305317,-0.00113360518632574));
#22538=CARTESIAN_POINT('',(0.00724131101096593,-0.0129229535529723,0.000793738664923998));
#22539=CARTESIAN_POINT('',(0.00706837370668615,-0.0130072951486252,0.00176201572071837));
#22540=CARTESIAN_POINT('',(0.00635863043279212,-0.0131689098087962,0.00355449367373196));
#22541=CARTESIAN_POINT('',(0.00582182446317788,-0.0132461828733143,0.00437869457095119));
#22542=CARTESIAN_POINT('',(0.00446932477096638,-0.0133936604712158,0.00575254226091774));
#22543=CARTESIAN_POINT('',(0.00365363104836912,-0.0134638650045992,0.00630218905366504));
#22544=CARTESIAN_POINT('',(0.0018724871703906,-0.0135972055402311,0.00703991459362902));
#22545=CARTESIAN_POINT('',(0.000907037015009332,-0.0136603415424797,0.0072279933408457));
#22546=CARTESIAN_POINT('',(-0.00102078114276234,-0.0137795450158421,0.00721280908063516));
#22547=CARTESIAN_POINT('',(-0.00198314914515274,-0.0138356124869559,0.00700954607320794));
#22548=CARTESIAN_POINT('',(-0.00375245067005612,-0.0139406788980488,0.0062438537571232));
#22549=CARTESIAN_POINT('',(-0.0045593841925691,-0.0139896778380279,0.00568142444846567));
#22550=CARTESIAN_POINT('',(-0.00589007726753176,-0.0140806071868512,0.00428644731519142));
#22551=CARTESIAN_POINT('',(-0.00641383681998145,-0.0141225375956955,0.0034538994905747));
#22552=CARTESIAN_POINT('',(-0.00709524800837267,-0.0141993298822493,0.00165044565872487));
#22553=CARTESIAN_POINT('',(-0.00725289964431421,-0.0142341917599588,0.000679539651491767));
#22554=CARTESIAN_POINT('',(-0.007177205975424,-0.014296846984243,-0.00124678219753841));
#22555=CARTESIAN_POINT('',(-0.00694386067059227,-0.0143246403308177,-0.00220219803933549));
#22556=CARTESIAN_POINT('',(-0.0065333592200569,-0.0143488994118251,-0.00307451547034793));
#22557=CARTESIAN_POINT('',(-0.00707685460303241,-0.0102496538642035,-0.00229964763701973));
#22558=CARTESIAN_POINT('',(-0.00676981152589942,-0.0103870094433671,-0.003244531182985));
#22559=CARTESIAN_POINT('',(-0.00627106486747605,-0.0105208307569634,-0.00412685625732547));
#22560=CARTESIAN_POINT('',(-0.00496892881174377,-0.0107814048530212,-0.00562729892899101));
#22561=CARTESIAN_POINT('',(-0.00416553941443487,-0.0109081576354828,-0.00624541652631608));
#22562=CARTESIAN_POINT('',(-0.00238135251366929,-0.0111545946692711,-0.00711943316941079));
#22563=CARTESIAN_POINT('',(-0.00140055501021261,-0.0112742789205979,-0.00737533221518044));
#22564=CARTESIAN_POINT('',(0.000583193290494599,-0.0115065788921167,-0.00748444305656528));
#22565=CARTESIAN_POINT('',(0.00158614408774513,-0.0116191946123087,-0.00733765485218046));
#22566=CARTESIAN_POINT('',(0.00345541968581831,-0.011837357521558,-0.00666461767854607));
#22567=CARTESIAN_POINT('',(0.00432174448664098,-0.0119429047106153,-0.00613836870929649));
#22568=CARTESIAN_POINT('',(0.00578062252289037,-0.012146930557595,-0.00478972271200754));
#22569=CARTESIAN_POINT('',(0.00637317575831709,-0.0122454092155175,-0.00396732568396815));
#22570=CARTESIAN_POINT('',(0.00719070420265566,-0.0124352980002277,-0.00215657517348927));
#22571=CARTESIAN_POINT('',(0.00741567941156751,-0.0125267081270155,-0.00116822169104975));
#22572=CARTESIAN_POINT('',(0.00746243639028041,-0.0127024598494561,0.000817976784663933));
#22573=CARTESIAN_POINT('',(0.00728421816008148,-0.0127868014451091,0.0018158217779381));
#22574=CARTESIAN_POINT('',(0.00655280170429842,-0.0129484161052802,0.00366303600269487));
#22575=CARTESIAN_POINT('',(0.0059996034787143,-0.0130256891697984,0.00451240523417745));
#22576=CARTESIAN_POINT('',(0.00460580297688281,-0.0131731667676999,0.00592820563009794));
#22577=CARTESIAN_POINT('',(0.00376520070063544,-0.0132433713010833,0.00649463679453584));
#22578=CARTESIAN_POINT('',(0.00192966665559529,-0.0133767118367153,0.00725489000105184));
#22579=CARTESIAN_POINT('',(0.000934734886802505,-0.0134398478389638,0.00744871204312994));
#22580=CARTESIAN_POINT('',(-0.00105195237916532,-0.0135590513123262,0.00743306410648104));
#22581=CARTESIAN_POINT('',(-0.00204370787634037,-0.01361511878344,0.00722359412775403));
#22582=CARTESIAN_POINT('',(-0.00386703794251528,-0.0137201851945328,0.00643452013346544));
#22583=CARTESIAN_POINT('',(-0.00469861251151514,-0.0137691841345118,0.00585491611790385));
#22584=CARTESIAN_POINT('',(-0.00606994049506089,-0.013860113483335,0.00441734105626232));
#22585=CARTESIAN_POINT('',(-0.00660969390960677,-0.0139020438921792,0.00355937001018238));
#22586=CARTESIAN_POINT('',(-0.00731191311291048,-0.0139788361787328,0.00170084474001979));
#22587=CARTESIAN_POINT('',(-0.0074743789016683,-0.0140136980564422,0.000700290515937141));
#22588=CARTESIAN_POINT('',(-0.00739637380170993,-0.0140763532807262,-0.00128485474903298));
#22589=CARTESIAN_POINT('',(-0.00715590291299373,-0.0141041466273008,-0.00226944578992046));
#22590=CARTESIAN_POINT('',(-0.00673286612337111,-0.014128405708308,-0.00316840087294414));
#22591=CARTESIAN_POINT('',(-0.00713827428147907,-0.0100937412712376,-0.00231960616751517));
#22592=CARTESIAN_POINT('',(-0.00682856639234631,-0.0102310968504013,-0.00327269031202571));
#22593=CARTESIAN_POINT('',(-0.00632549113582322,-0.0103649181639976,-0.00416267304296523));
#22594=CARTESIAN_POINT('',(-0.00501205390431115,-0.0106254922600555,-0.00567613798392846));
#22595=CARTESIAN_POINT('',(-0.00420169192932218,-0.010752245042517,-0.00629962019395218));
#22596=CARTESIAN_POINT('',(-0.0024020201568331,-0.0109986820763054,-0.00718122238517345));
#22597=CARTESIAN_POINT('',(-0.001412710359333,-0.0111183663276323,-0.007439342366371));
#22598=CARTESIAN_POINT('',(0.00058825479682526,-0.0113506662991512,-0.00754940017546519));
#22599=CARTESIAN_POINT('',(0.00159991015548341,-0.0114632820193433,-0.00740133800336183));
#22600=CARTESIAN_POINT('',(0.00348540910596414,-0.0116814449285928,-0.00672245957268514));
#22601=CARTESIAN_POINT('',(0.00435925269778671,-0.0117869921176501,-0.0061916433141118));
#22602=CARTESIAN_POINT('',(0.00583079226587554,-0.0119910179646301,-0.00483129248351225));
#22603=CARTESIAN_POINT('',(0.00642848824214178,-0.0120894966225526,-0.00400175791148603));
#22604=CARTESIAN_POINT('',(0.00725311197626499,-0.012279385407263,-0.00217529198500113));
#22605=CARTESIAN_POINT('',(0.00748003973412194,-0.0123707955340508,-0.00117836063054244));
#22606=CARTESIAN_POINT('',(0.00752720251438918,-0.0125465472564916,0.000825075965572551));
#22607=CARTESIAN_POINT('',(0.00734743753679947,-0.0126308888521447,0.00183158120722885));
#22608=CARTESIAN_POINT('',(0.006609673153011,-0.0127925035123159,0.00369482731480231));
#22609=CARTESIAN_POINT('',(0.00605167374681224,-0.0128697765768341,0.00455156818071947));
#22610=CARTESIAN_POINT('',(0.00464577651791155,-0.0130172541747358,0.00597965623972474));
#22611=CARTESIAN_POINT('',(0.00379787869520962,-0.0130874587081192,0.00655100343281285));
#22612=CARTESIAN_POINT('',(0.00194641413906699,-0.0132207992437512,0.00731785484009763));
#22613=CARTESIAN_POINT('',(0.00094284740562629,-0.0132839352459998,0.0075133590542943));
#22614=CARTESIAN_POINT('',(-0.00106108222292979,-0.0134031387193622,0.00749757530996088));
#22615=CARTESIAN_POINT('',(-0.00206144511804517,-0.0134592061904759,0.00728628735143079));
#22616=CARTESIAN_POINT('',(-0.0039005997775809,-0.0135642726015686,0.00649036502215181));
#22617=CARTESIAN_POINT('',(-0.00473939154200123,-0.0136132715415475,0.00590573065140292));
#22618=CARTESIAN_POINT('',(-0.00612262121471807,-0.0137042008903706,0.00445567894540712));
#22619=CARTESIAN_POINT('',(-0.00666705912301456,-0.0137461312992147,0.00359026161016021));
#22620=CARTESIAN_POINT('',(-0.0073753728527831,-0.0138229235857679,0.00171560628916551));
#22621=CARTESIAN_POINT('',(-0.00753924867425515,-0.0138577854634772,0.000706368303417708));
#22622=CARTESIAN_POINT('',(-0.00746056657181116,-0.0139204406877607,-0.00129600594118867));
#22623=CARTESIAN_POINT('',(-0.00721800864789512,-0.0139482340343351,-0.00228914220004725));
#22624=CARTESIAN_POINT('',(-0.00679130034245832,-0.013972493115342,-0.00319589927071014));
#22625=CARTESIAN_POINT('',(-0.00713827428147907,-0.00992240968822442,-0.00231960616751517));
#22626=CARTESIAN_POINT('',(-0.00682856639234631,-0.0100597652673881,-0.00327269031202571));
#22627=CARTESIAN_POINT('',(-0.00632549113582321,-0.0101935865809844,-0.00416267304296523));
#22628=CARTESIAN_POINT('',(-0.00501205390431114,-0.0104541606770422,-0.00567613798392846));
#22629=CARTESIAN_POINT('',(-0.00420169192932218,-0.0105809134595037,-0.00629962019395218));
#22630=CARTESIAN_POINT('',(-0.00240202015683311,-0.010827350493292,-0.00718122238517345));
#22631=CARTESIAN_POINT('',(-0.001412710359333,-0.0109470347446187,-0.00743934236637099));
#22632=CARTESIAN_POINT('',(0.000588254796825264,-0.0111793347161375,-0.00754940017546519));
#22633=CARTESIAN_POINT('',(0.00159991015548341,-0.0112919504363294,-0.00740133800336183));
#22634=CARTESIAN_POINT('',(0.00348540910596414,-0.0115101133455787,-0.00672245957268514));
#22635=CARTESIAN_POINT('',(0.00435925269778671,-0.0116156605346359,-0.0061916433141118));
#22636=CARTESIAN_POINT('',(0.00583079226587553,-0.0118196863816156,-0.00483129248351225));
#22637=CARTESIAN_POINT('',(0.00642848824214178,-0.011918165039538,-0.00400175791148602));
#22638=CARTESIAN_POINT('',(0.00725311197626499,-0.0121080538242482,-0.00217529198500112));
#22639=CARTESIAN_POINT('',(0.00748003973412194,-0.0121994639510358,-0.00117836063054243));
#22640=CARTESIAN_POINT('',(0.00752720251438917,-0.0123752156734764,0.000825075965572551));
#22641=CARTESIAN_POINT('',(0.00734743753679946,-0.0124595572691293,0.00183158120722885));
#22642=CARTESIAN_POINT('',(0.00660967315301099,-0.0126211719293004,0.00369482731480231));
#22643=CARTESIAN_POINT('',(0.00605167374681224,-0.0126984449938185,0.00455156818071947));
#22644=CARTESIAN_POINT('',(0.00464577651791156,-0.01284592259172,0.00597965623972475));
#22645=CARTESIAN_POINT('',(0.00379787869520962,-0.0129161271251034,0.00655100343281287));
#22646=CARTESIAN_POINT('',(0.00194641413906699,-0.0130494676607354,0.00731785484009764));
#22647=CARTESIAN_POINT('',(0.000942847405626288,-0.0131126036629839,0.0075133590542943));
#22648=CARTESIAN_POINT('',(-0.00106108222292979,-0.0132318071363463,0.00749757530996088));
#22649=CARTESIAN_POINT('',(-0.00206144511804517,-0.0132878746074602,0.00728628735143079));
#22650=CARTESIAN_POINT('',(-0.0039005997775809,-0.013392941018553,0.00649036502215181));
#22651=CARTESIAN_POINT('',(-0.00473939154200124,-0.013441939958532,0.00590573065140291));
#22652=CARTESIAN_POINT('',(-0.00612262121471807,-0.0135328693073553,0.00445567894540711));
#22653=CARTESIAN_POINT('',(-0.00666705912301456,-0.0135747997161996,0.00359026161016021));
#22654=CARTESIAN_POINT('',(-0.00737537285278311,-0.0136515920027533,0.00171560628916551));
#22655=CARTESIAN_POINT('',(-0.00753924867425516,-0.0136864538804628,0.000706368303417708));
#22656=CARTESIAN_POINT('',(-0.00746056657181117,-0.013749109104747,-0.00129600594118867));
#22657=CARTESIAN_POINT('',(-0.00721800864789512,-0.0137769024513216,-0.00228914220004726));
#22658=CARTESIAN_POINT('',(-0.00679130034245831,-0.0138011615323289,-0.00319589927071015));
#22659=CARTESIAN_POINT('',(-0.00713767358234481,-0.00990699069817707,-0.00231941096831691));
#22660=CARTESIAN_POINT('',(-0.00682799175571029,-0.0100443462773407,-0.00327241490901377));
#22661=CARTESIAN_POINT('',(-0.00632495883391112,-0.010178167590937,-0.00416232274624161));
#22662=CARTESIAN_POINT('',(-0.00501163213059911,-0.0104387416869948,-0.00567566032629884));
#22663=CARTESIAN_POINT('',(-0.00420133834908628,-0.0105654944694563,-0.00629909006912824));
#22664=CARTESIAN_POINT('',(-0.00240181802234349,-0.0108119315032446,-0.00718061807187592));
#22665=CARTESIAN_POINT('',(-0.00141259147711352,-0.0109316157545713,-0.00743871633179419));
#22666=CARTESIAN_POINT('',(0.000588205294083671,-0.01116391572609,-0.00754876487931786));
#22667=CARTESIAN_POINT('',(0.0015997755200509,-0.011276531446282,-0.00740071516692327));
#22668=CARTESIAN_POINT('',(0.00348511580226776,-0.0114946943555312,-0.00672189386513648));
#22669=CARTESIAN_POINT('',(0.00435888585851739,-0.0116002415445884,-0.0061911222757443));
#22670=CARTESIAN_POINT('',(0.00583030159379877,-0.0118042673915681,-0.00483088592121192));
#22671=CARTESIAN_POINT('',(0.00642794727283052,-0.0119027460494905,-0.00400142115607174));
#22672=CARTESIAN_POINT('',(0.00725250161332388,-0.0120926348342006,-0.00217510893011129));
#22673=CARTESIAN_POINT('',(0.00747941027478551,-0.0121840449609883,-0.00117826146929103));
#22674=CARTESIAN_POINT('',(0.00752656908621655,-0.0123597966834289,0.00082500653388659));
#22675=CARTESIAN_POINT('',(0.00734681923618598,-0.0124441382790818,0.00183142707624395));
#22676=CARTESIAN_POINT('',(0.00660911693665054,-0.0126057529392528,0.00369451638817191));
#22677=CARTESIAN_POINT('',(0.00605116448714566,-0.0126830260037709,0.00455118515774251));
#22678=CARTESIAN_POINT('',(0.00464538556712678,-0.0128305036016724,0.00597915304046611));
#22679=CARTESIAN_POINT('',(0.00379755909661278,-0.0129007081350558,0.00655045215361912));
#22680=CARTESIAN_POINT('',(0.00194625034467605,-0.0130340486706877,0.00731723902892344));
#22681=CARTESIAN_POINT('',(0.000942768063253332,-0.0130971846729363,0.00751272679107474));
#22682=CARTESIAN_POINT('',(-0.00106099293087578,-0.0132163881462987,0.00749694437497293));
#22683=CARTESIAN_POINT('',(-0.00206127164358217,-0.0132724556174126,0.00728567419671981));
#22684=CARTESIAN_POINT('',(-0.00390027153481281,-0.0133775220285054,0.00648981884579376));
#22685=CARTESIAN_POINT('',(-0.00473899271333706,-0.0134265209684845,0.00590523367312083));
#22686=CARTESIAN_POINT('',(-0.00612210598468935,-0.0135174503173078,0.00445530399168868));
#22687=CARTESIAN_POINT('',(-0.00666649807751738,-0.013559380726152,0.00358995948292945));
#22688=CARTESIAN_POINT('',(-0.00737475220136054,-0.0136361730127058,0.00171546191768691));
#22689=CARTESIAN_POINT('',(-0.00753861423237565,-0.0136710348904153,0.000706308861203582));
#22690=CARTESIAN_POINT('',(-0.00745993875117777,-0.0137336901146995,-0.0012958968798643));
#22691=CARTESIAN_POINT('',(-0.00721740123896477,-0.0137614834612743,-0.00228894956444885));
#22692=CARTESIAN_POINT('',(-0.0067907288418301,-0.0137857425422816,-0.00319563032980799));
#22693=CARTESIAN_POINT('',(-0.0071364895837481,-0.00989161587683944,-0.00231902622400212));
#22694=CARTESIAN_POINT('',(-0.0068268591271915,-0.0100289714560031,-0.00327187208023133));
#22695=CARTESIAN_POINT('',(-0.00632390964858522,-0.0101627927695994,-0.00416163229938468));
#22696=CARTESIAN_POINT('',(-0.00501080080014649,-0.0104233668656572,-0.00567471884672791));
#22697=CARTESIAN_POINT('',(-0.00420064143031404,-0.0105501196481187,-0.00629804517491777));
#22698=CARTESIAN_POINT('',(-0.00240141960833152,-0.0107965566819069,-0.00717942694963944));
#22699=CARTESIAN_POINT('',(-0.00141235715618145,-0.0109162409332336,-0.00743748239617125));
#22700=CARTESIAN_POINT('',(0.000588107722482121,-0.0111485409047524,-0.00754751268882177));
#22701=CARTESIAN_POINT('',(0.00159951014899562,-0.0112611566249443,-0.00739948753494049));
#22702=CARTESIAN_POINT('',(0.00348453769062233,-0.0114793195341935,-0.00672077883615515));
#22703=CARTESIAN_POINT('',(0.00435816280573553,-0.0115848667232507,-0.0061900952912511));
#22704=CARTESIAN_POINT('',(0.00582933446230616,-0.0117888925702303,-0.00483008457297351));
#22705=CARTESIAN_POINT('',(0.00642688100376357,-0.0118873712281527,-0.00400075739959997));
#22706=CARTESIAN_POINT('',(0.00725129856703243,-0.0120772600128628,-0.00217474812264493));
#22707=CARTESIAN_POINT('',(0.00747816958884387,-0.0121686701396505,-0.00117806601906343));
#22708=CARTESIAN_POINT('',(0.00752532057756267,-0.012344421862091,0.000824869681652156));
#22709=CARTESIAN_POINT('',(0.00734560054447003,-0.0124287634577439,0.00183112327878624));
#22710=CARTESIAN_POINT('',(0.00660802061512669,-0.0125903781179149,0.00369390354111906));
#22711=CARTESIAN_POINT('',(0.00605016071887598,-0.012667651182433,0.00455043020631779));
#22712=CARTESIAN_POINT('',(0.00464461498972096,-0.0128151287803345,0.00597816121746836));
#22713=CARTESIAN_POINT('',(0.00379692915681664,-0.0128853333137179,0.00654936556342019));
#22714=CARTESIAN_POINT('',(0.00194592750031362,-0.0130186738493498,0.00731602524397766));
#22715=CARTESIAN_POINT('',(0.000942611676714912,-0.0130818098515984,0.0075114805785833));
#22716=CARTESIAN_POINT('',(-0.00106081693317474,-0.0132010133249608,0.00749570078047156));
#22717=CARTESIAN_POINT('',(-0.00206092971946568,-0.0132570807960746,0.00728446564775417));
#22718=CARTESIAN_POINT('',(-0.00389962455705868,-0.0133621472071675,0.006488742313459));
#22719=CARTESIAN_POINT('',(-0.00473820660836074,-0.0134111461471466,0.00590425411188122));
#22720=CARTESIAN_POINT('',(-0.00612109044863111,-0.0135020754959699,0.00445456494504928));
#22721=CARTESIAN_POINT('',(-0.00666539223759941,-0.0135440059048142,0.00358936397979514));
#22722=CARTESIAN_POINT('',(-0.00737352887611922,-0.013620798191368,0.00171517735655088));
#22723=CARTESIAN_POINT('',(-0.00753736372567072,-0.0136556600690776,0.000706191698560759));
#22724=CARTESIAN_POINT('',(-0.00745870129517602,-0.0137183152933619,-0.00129568191625332));
#22725=CARTESIAN_POINT('',(-0.00721620401512981,-0.0137461086399366,-0.00228856987307729));
#22726=CARTESIAN_POINT('',(-0.00678960239449027,-0.013770367720944,-0.00319510023806557));
#22727=CARTESIAN_POINT('',(-0.00586854477794281,-0.0138049051783931,-0.00232352128445575));
#22728=CARTESIAN_POINT('',(-0.00647608624973171,-0.0137551635056439,-0.000786833552677216));
#22729=CARTESIAN_POINT('',(-0.00641918266558093,-0.0136285038708237,0.00277611211943972));
#22730=CARTESIAN_POINT('',(-0.00257506117324275,-0.0133569855506279,0.00650403957094241));
#22731=CARTESIAN_POINT('',(0.00277796776553595,-0.0130039383624667,0.00641940533627276));
#22732=CARTESIAN_POINT('',(0.00650363167066124,-0.0125693623063402,0.00257497225928561));
#22733=CARTESIAN_POINT('',(0.00641943847793923,-0.0120532573822484,-0.00277789137493516));
#22734=CARTESIAN_POINT('',(0.00257518666651457,-0.0114556235901914,-0.0065039899999209));
#22735=CARTESIAN_POINT('',(-0.00277899926821046,-0.0107764609301692,-0.00641793340392155));
#22736=CARTESIAN_POINT('',(-0.00525948636061672,-0.0102693332448443,-0.0038596124225381));
#22737=CARTESIAN_POINT('',(-0.00586854353305237,-0.010002181257521,-0.00232352483973746));
#22738=CARTESIAN_POINT('',(-0.00586720610780115,-0.0100021881219798,-0.0023229945466064));
#22739=CARTESIAN_POINT('',(-0.00586854353315033,-0.0100021880910911,-0.00232352483977624));
#22740=CARTESIAN_POINT('',(-0.00586854666154146,-0.0101580986507601,-0.00232352603135712));
#22741=CARTESIAN_POINT('',(-0.00598863875979985,-0.0104699172300717,-0.00237107384600943));
#22742=CARTESIAN_POINT('',(-0.00642351653109598,-0.0106636552715684,-0.00254325427496914));
#22743=CARTESIAN_POINT('',(-0.00685839433219838,-0.0104699172424568,-0.00271543469247471));
#22744=CARTESIAN_POINT('',(-0.00697848647290429,-0.0101580986499977,-0.00276298249495351));
#22745=CARTESIAN_POINT('',(-0.00697848962230257,-0.0100021880761874,-0.00276298368595471));
#22746=CARTESIAN_POINT('',(-0.00697689923797853,-0.0100021880392446,-0.00276235310573588));
#22747=CARTESIAN_POINT('',(-0.00697848962239398,-0.0100021820184533,-0.00276298368599091));
#22748=CARTESIAN_POINT('',(-0.00625423868271113,-0.0102693340114975,-0.00458959897989776));
#22749=CARTESIAN_POINT('',(-0.00330460534139247,-0.0107764617076857,-0.00763178778113441));
#22750=CARTESIAN_POINT('',(0.00306224359742731,-0.0114556243822671,-0.00773412112575933));
#22751=CARTESIAN_POINT('',(0.00763357757233496,-0.0120532581871476,-0.00330328777955172));
#22752=CARTESIAN_POINT('',(0.00773369497252947,-0.0125693631223272,0.0030619887676494));
#22753=CARTESIAN_POINT('',(0.00330337849061272,-0.0130039391878057,0.00763353821745889));
#22754=CARTESIAN_POINT('',(-0.00306209462755998,-0.0133569863835833,0.00773417996973019));
#22755=CARTESIAN_POINT('',(-0.0076332734872252,-0.0136285047096598,0.00330117174949463));
#22756=CARTESIAN_POINT('',(-0.00770093960740274,-0.0137551643472433,-0.000935651021456268));
#22757=CARTESIAN_POINT('',(-0.00697849091759819,-0.0138049060210849,-0.00276297992488766));
#22758=CARTESIAN_POINT('',(-0.0071364895837481,-0.00998404147970407,-0.00231902622400212));
#22759=CARTESIAN_POINT('',(-0.0068268591271915,-0.0101213970588677,-0.00327187208023133));
#22760=CARTESIAN_POINT('',(-0.00632390964858522,-0.010255218372464,-0.00416163229938468));
#22761=CARTESIAN_POINT('',(-0.00501080080014649,-0.0105157924685218,-0.00567471884672791));
#22762=CARTESIAN_POINT('',(-0.00420064143031404,-0.0106425452509834,-0.00629804517491777));
#22763=CARTESIAN_POINT('',(-0.00240141960833152,-0.0108889822847717,-0.00717942694963944));
#22764=CARTESIAN_POINT('',(-0.00141235715618145,-0.0110086665360985,-0.00743748239617125));
#22765=CARTESIAN_POINT('',(0.000588107722482121,-0.0112409665076173,-0.00754751268882177));
#22766=CARTESIAN_POINT('',(0.00159951014899562,-0.0113535822278093,-0.00739948753494049));
#22767=CARTESIAN_POINT('',(0.00348453769062233,-0.0115717451370586,-0.00672077883615515));
#22768=CARTESIAN_POINT('',(0.00435816280573553,-0.0116772923261159,-0.0061900952912511));
#22769=CARTESIAN_POINT('',(0.00582933446230616,-0.0118813181730956,-0.00483008457297351));
#22770=CARTESIAN_POINT('',(0.00642688100376358,-0.0119797968310181,-0.00400075739959997));
#22771=CARTESIAN_POINT('',(0.00725129856703243,-0.0121696856157283,-0.00217474812264493));
#22772=CARTESIAN_POINT('',(0.00747816958884387,-0.0122610957425161,-0.00117806601906343));
#22773=CARTESIAN_POINT('',(0.00752532057756267,-0.0124368474649567,0.000824869681652156));
#22774=CARTESIAN_POINT('',(0.00734560054447003,-0.0125211890606097,0.00183112327878624));
#22775=CARTESIAN_POINT('',(0.00660802061512669,-0.0126828037207808,0.00369390354111907));
#22776=CARTESIAN_POINT('',(0.00605016071887599,-0.0127600767852989,0.00455043020631779));
#22777=CARTESIAN_POINT('',(0.00464461498972096,-0.0129075543832005,0.00597816121746836));
#22778=CARTESIAN_POINT('',(0.00379692915681664,-0.0129777589165839,0.00654936556342019));
#22779=CARTESIAN_POINT('',(0.00194592750031363,-0.0131110994522158,0.00731602524397766));
#22780=CARTESIAN_POINT('',(0.000942611676714919,-0.0131742354544644,0.00751148057858331));
#22781=CARTESIAN_POINT('',(-0.00106081693317473,-0.0132934389278268,0.00749570078047156));
#22782=CARTESIAN_POINT('',(-0.00206092971946568,-0.0133495063989406,0.00728446564775417));
#22783=CARTESIAN_POINT('',(-0.00389962455705868,-0.0134545728100334,0.006488742313459));
#22784=CARTESIAN_POINT('',(-0.00473820660836074,-0.0135035717500124,0.00590425411188122));
#22785=CARTESIAN_POINT('',(-0.00612109044863111,-0.0135945010988356,0.00445456494504928));
#22786=CARTESIAN_POINT('',(-0.00666539223759941,-0.0136364315076798,0.00358936397979514));
#22787=CARTESIAN_POINT('',(-0.00737352887611922,-0.0137132237942334,0.00171517735655088));
#22788=CARTESIAN_POINT('',(-0.00753736372567072,-0.0137480856719428,0.000706191698560759));
#22789=CARTESIAN_POINT('',(-0.00745870129517602,-0.0138107408962268,-0.00129568191625332));
#22790=CARTESIAN_POINT('',(-0.00721620401512982,-0.0138385342428014,-0.00228856987307729));
#22791=CARTESIAN_POINT('',(-0.00678960239449027,-0.0138627933238085,-0.00319510023806557));
#22792=CARTESIAN_POINT('',(-0.00713767358234481,-0.00996866665836644,-0.00231941096831692));
#22793=CARTESIAN_POINT('',(-0.00682799175571029,-0.0101060222375301,-0.00327241490901377));
#22794=CARTESIAN_POINT('',(-0.00632495883391112,-0.0102398435511264,-0.00416232274624161));
#22795=CARTESIAN_POINT('',(-0.00501163213059911,-0.0105004176471842,-0.00567566032629884));
#22796=CARTESIAN_POINT('',(-0.00420133834908628,-0.0106271704296457,-0.00629909006912824));
#22797=CARTESIAN_POINT('',(-0.00240181802234349,-0.0108736074634341,-0.00718061807187592));
#22798=CARTESIAN_POINT('',(-0.00141259147711352,-0.0109932917147608,-0.00743871633179419));
#22799=CARTESIAN_POINT('',(0.000588205294083671,-0.0112255916862796,-0.00754876487931786));
#22800=CARTESIAN_POINT('',(0.00159977552005091,-0.0113382074064716,-0.00740071516692327));
#22801=CARTESIAN_POINT('',(0.00348511580226776,-0.0115563703157209,-0.00672189386513648));
#22802=CARTESIAN_POINT('',(0.00435888585851739,-0.0116619175047782,-0.0061911222757443));
#22803=CARTESIAN_POINT('',(0.00583030159379877,-0.0118659433517579,-0.00483088592121192));
#22804=CARTESIAN_POINT('',(0.00642794727283052,-0.0119644220096804,-0.00400142115607174));
#22805=CARTESIAN_POINT('',(0.00725250161332388,-0.0121543107943906,-0.00217510893011129));
#22806=CARTESIAN_POINT('',(0.0074794102747855,-0.0122457209211783,-0.00117826146929103));
#22807=CARTESIAN_POINT('',(0.00752656908621655,-0.012421472643619,0.000825006533886589));
#22808=CARTESIAN_POINT('',(0.00734681923618598,-0.0125058142392719,0.00183142707624395));
#22809=CARTESIAN_POINT('',(0.00660911693665054,-0.012667428899443,0.00369451638817191));
#22810=CARTESIAN_POINT('',(0.00605116448714566,-0.0127447019639612,0.00455118515774251));
#22811=CARTESIAN_POINT('',(0.00464538556712678,-0.0128921795618627,0.00597915304046612));
#22812=CARTESIAN_POINT('',(0.00379755909661278,-0.0129623840952461,0.00655045215361912));
#22813=CARTESIAN_POINT('',(0.00194625034467606,-0.0130957246308781,0.00731723902892344));
#22814=CARTESIAN_POINT('',(0.00094276806325334,-0.0131588606331266,0.00751272679107474));
#22815=CARTESIAN_POINT('',(-0.00106099293087577,-0.013278064106489,0.00749694437497293));
#22816=CARTESIAN_POINT('',(-0.00206127164358217,-0.0133341315776028,0.00728567419671981));
#22817=CARTESIAN_POINT('',(-0.00390027153481281,-0.0134391979886957,0.00648981884579376));
#22818=CARTESIAN_POINT('',(-0.00473899271333706,-0.0134881969286747,0.00590523367312083));
#22819=CARTESIAN_POINT('',(-0.00612210598468935,-0.0135791262774979,0.00445530399168868));
#22820=CARTESIAN_POINT('',(-0.00666649807751738,-0.0136210566863421,0.00358995948292946));
#22821=CARTESIAN_POINT('',(-0.00737475220136054,-0.0136978489728957,0.00171546191768691));
#22822=CARTESIAN_POINT('',(-0.00753861423237565,-0.0137327108506051,0.000706308861203582));
#22823=CARTESIAN_POINT('',(-0.00745993875117777,-0.0137953660748891,-0.0012958968798643));
#22824=CARTESIAN_POINT('',(-0.00721740123896477,-0.0138231594214637,-0.00228894956444885));
#22825=CARTESIAN_POINT('',(-0.0067907288418301,-0.0138474185024709,-0.00319563032980799));
#22826=CARTESIAN_POINT('',(-0.00713827428147907,-0.0099532476683191,-0.00231960616751517));
#22827=CARTESIAN_POINT('',(-0.00682856639234631,-0.0100906032474828,-0.00327269031202571));
#22828=CARTESIAN_POINT('',(-0.00632549113582321,-0.010224424561079,-0.00416267304296523));
#22829=CARTESIAN_POINT('',(-0.00501205390431114,-0.0104849986571369,-0.00567613798392846));
#22830=CARTESIAN_POINT('',(-0.00420169192932218,-0.0106117514395984,-0.00629962019395218));
#22831=CARTESIAN_POINT('',(-0.00240202015683311,-0.0108581884733867,-0.00718122238517345));
#22832=CARTESIAN_POINT('',(-0.001412710359333,-0.0109778727247135,-0.007439342366371));
#22833=CARTESIAN_POINT('',(0.000588254796825264,-0.0112101726962322,-0.00754940017546519));
#22834=CARTESIAN_POINT('',(0.00159991015548341,-0.0113227884164243,-0.00740133800336183));
#22835=CARTESIAN_POINT('',(0.00348540910596414,-0.0115409513256735,-0.00672245957268514));
#22836=CARTESIAN_POINT('',(0.00435925269778671,-0.0116464985147308,-0.0061916433141118));
#22837=CARTESIAN_POINT('',(0.00583079226587553,-0.0118505243617105,-0.00483129248351225));
#22838=CARTESIAN_POINT('',(0.00642848824214178,-0.011949003019633,-0.00400175791148602));
#22839=CARTESIAN_POINT('',(0.00725311197626499,-0.0121388918043431,-0.00217529198500112));
#22840=CARTESIAN_POINT('',(0.00748003973412194,-0.0122303019311308,-0.00117836063054243));
#22841=CARTESIAN_POINT('',(0.00752720251438918,-0.0124060536535715,0.000825075965572551));
#22842=CARTESIAN_POINT('',(0.00734743753679946,-0.0124903952492244,0.00183158120722885));
#22843=CARTESIAN_POINT('',(0.00660967315301099,-0.0126520099093955,0.00369482731480231));
#22844=CARTESIAN_POINT('',(0.00605167374681224,-0.0127292829739137,0.00455156818071947));
#22845=CARTESIAN_POINT('',(0.00464577651791156,-0.0128767605718152,0.00597965623972475));
#22846=CARTESIAN_POINT('',(0.00379787869520962,-0.0129469651051986,0.00655100343281287));
#22847=CARTESIAN_POINT('',(0.00194641413906699,-0.0130803056408305,0.00731785484009764));
#22848=CARTESIAN_POINT('',(0.000942847405626291,-0.0131434416430791,0.0075133590542943));
#22849=CARTESIAN_POINT('',(-0.00106108222292979,-0.0132626451164415,0.00749757530996088));
#22850=CARTESIAN_POINT('',(-0.00206144511804517,-0.0133187125875553,0.00728628735143079));
#22851=CARTESIAN_POINT('',(-0.0039005997775809,-0.0134237789986481,0.00649036502215181));
#22852=CARTESIAN_POINT('',(-0.00473939154200124,-0.0134727779386271,0.00590573065140291));
#22853=CARTESIAN_POINT('',(-0.00612262121471807,-0.0135637072874504,0.00445567894540711));
#22854=CARTESIAN_POINT('',(-0.00666705912301456,-0.0136056376962946,0.00359026161016021));
#22855=CARTESIAN_POINT('',(-0.00737537285278311,-0.0136824299828483,0.00171560628916551));
#22856=CARTESIAN_POINT('',(-0.00753924867425516,-0.0137172918605577,0.000706368303417708));
#22857=CARTESIAN_POINT('',(-0.00746056657181117,-0.0137799470848417,-0.00129600594118867));
#22858=CARTESIAN_POINT('',(-0.00721800864789512,-0.0138077404314164,-0.00228914220004726));
#22859=CARTESIAN_POINT('',(-0.00679130034245831,-0.0138319995124236,-0.00319589927071015));
#22860=CARTESIAN_POINT('',(-0.00713827428147908,-0.00978191608530591,-0.00231960616751517));
#22861=CARTESIAN_POINT('',(-0.00682856639234631,-0.00991927166446956,-0.0032726903120257));
#22862=CARTESIAN_POINT('',(-0.00632549113582322,-0.0100530929780658,-0.00416267304296523));
#22863=CARTESIAN_POINT('',(-0.00501205390431114,-0.0103136670741236,-0.00567613798392846));
#22864=CARTESIAN_POINT('',(-0.00420169192932218,-0.0104404198565851,-0.00629962019395217));
#22865=CARTESIAN_POINT('',(-0.0024020201568331,-0.0106868568903732,-0.00718122238517344));
#22866=CARTESIAN_POINT('',(-0.001412710359333,-0.0108065411416999,-0.007439342366371));
#22867=CARTESIAN_POINT('',(0.000588254796825258,-0.0110388411132185,-0.0075494001754652));
#22868=CARTESIAN_POINT('',(0.00159991015548341,-0.0111514568334104,-0.00740133800336183));
#22869=CARTESIAN_POINT('',(0.00348540910596413,-0.0113696197426594,-0.00672245957268514));
#22870=CARTESIAN_POINT('',(0.00435925269778671,-0.0114751669317165,-0.00619164331411181));
#22871=CARTESIAN_POINT('',(0.00583079226587553,-0.011679192778696,-0.00483129248351226));
#22872=CARTESIAN_POINT('',(0.00642848824214178,-0.0117776714366183,-0.00400175791148603));
#22873=CARTESIAN_POINT('',(0.00725311197626498,-0.0119675602213283,-0.00217529198500112));
#22874=CARTESIAN_POINT('',(0.00748003973412194,-0.0120589703481159,-0.00117836063054244));
#22875=CARTESIAN_POINT('',(0.00752720251438918,-0.0122347220705563,0.000825075965572557));
#22876=CARTESIAN_POINT('',(0.00734743753679946,-0.0123190636662091,0.00183158120722885));
#22877=CARTESIAN_POINT('',(0.00660967315301099,-0.01248067832638,0.00369482731480231));
#22878=CARTESIAN_POINT('',(0.00605167374681224,-0.0125579513908981,0.00455156818071948));
#22879=CARTESIAN_POINT('',(0.00464577651791155,-0.0127054289887995,0.00597965623972473));
#22880=CARTESIAN_POINT('',(0.00379787869520963,-0.0127756335221828,0.00655100343281285));
#22881=CARTESIAN_POINT('',(0.00194641413906698,-0.0129089740578147,0.00731785484009762));
#22882=CARTESIAN_POINT('',(0.00094284740562626,-0.0129721100600632,0.0075133590542943));
#22883=CARTESIAN_POINT('',(-0.00106108222292982,-0.0130913135334257,0.00749757530996088));
#22884=CARTESIAN_POINT('',(-0.00206144511804518,-0.0131473810045395,0.00728628735143079));
#22885=CARTESIAN_POINT('',(-0.00390059977758088,-0.0132524474156325,0.00649036502215181));
#22886=CARTESIAN_POINT('',(-0.00473939154200123,-0.0133014463556117,0.00590573065140293));
#22887=CARTESIAN_POINT('',(-0.00612262121471807,-0.0133923757044352,0.00445567894540711));
#22888=CARTESIAN_POINT('',(-0.00666705912301456,-0.0134343061132796,0.0035902616101602));
#22889=CARTESIAN_POINT('',(-0.0073753728527831,-0.0135110983998337,0.00171560628916551));
#22890=CARTESIAN_POINT('',(-0.00753924867425516,-0.0135459602775433,0.000706368303417707));
#22891=CARTESIAN_POINT('',(-0.00746056657181116,-0.013608615501828,-0.00129600594118867));
#22892=CARTESIAN_POINT('',(-0.00721800864789512,-0.013636408848403,-0.00228914220004726));
#22893=CARTESIAN_POINT('',(-0.00679130034245831,-0.0136606679294106,-0.00319589927071014));
#22894=CARTESIAN_POINT('',(-0.00707685460303241,-0.00962600349234004,-0.00229964763701973));
#22895=CARTESIAN_POINT('',(-0.00676981152589942,-0.00976335907150373,-0.00324453118298499));
#22896=CARTESIAN_POINT('',(-0.00627106486747605,-0.00989718038509995,-0.00412685625732547));
#22897=CARTESIAN_POINT('',(-0.00496892881174377,-0.0101577544811575,-0.00562729892899101));
#22898=CARTESIAN_POINT('',(-0.00416553941443487,-0.0102845072636188,-0.00624541652631607));
#22899=CARTESIAN_POINT('',(-0.00238135251366929,-0.0105309442974066,-0.00711943316941079));
#22900=CARTESIAN_POINT('',(-0.00140055501021261,-0.0106506285487331,-0.00737533221518044));
#22901=CARTESIAN_POINT('',(0.000583193290494599,-0.0108829285202512,-0.00748444305656528));
#22902=CARTESIAN_POINT('',(0.00158614408774513,-0.0109955442404428,-0.00733765485218046));
#22903=CARTESIAN_POINT('',(0.00345541968581831,-0.0112137071496912,-0.00666461767854607));
#22904=CARTESIAN_POINT('',(0.00432174448664098,-0.011319254338748,-0.00613836870929649));
#22905=CARTESIAN_POINT('',(0.00578062252289037,-0.0115232801857269,-0.00478972271200753));
#22906=CARTESIAN_POINT('',(0.00637317575831709,-0.0116217588436489,-0.00396732568396815));
#22907=CARTESIAN_POINT('',(0.00719070420265566,-0.0118116476283582,-0.00215657517348927));
#22908=CARTESIAN_POINT('',(0.00741567941156751,-0.0119030577551455,-0.00116822169104975));
#22909=CARTESIAN_POINT('',(0.00746243639028041,-0.0120788094775854,0.000817976784663933));
#22910=CARTESIAN_POINT('',(0.00728421816008147,-0.0121631510732379,0.00181582177793811));
#22911=CARTESIAN_POINT('',(0.00655280170429841,-0.0123247657334084,0.00366303600269487));
#22912=CARTESIAN_POINT('',(0.00599960347871429,-0.0124020387979262,0.00451240523417745));
#22913=CARTESIAN_POINT('',(0.00460580297688281,-0.0125495163958273,0.00592820563009794));
#22914=CARTESIAN_POINT('',(0.00376520070063544,-0.0126197209292105,0.00649463679453584));
#22915=CARTESIAN_POINT('',(0.00192966665559529,-0.0127530614648423,0.00725489000105184));
#22916=CARTESIAN_POINT('',(0.000934734886802496,-0.0128161974670908,0.00744871204312994));
#22917=CARTESIAN_POINT('',(-0.00105195237916533,-0.0129354009404534,0.00743306410648104));
#22918=CARTESIAN_POINT('',(-0.00204370787634037,-0.0129914684115673,0.00722359412775403));
#22919=CARTESIAN_POINT('',(-0.00386703794251527,-0.0130965348226607,0.00643452013346544));
#22920=CARTESIAN_POINT('',(-0.00469861251151514,-0.0131455337626401,0.00585491611790385));
#22921=CARTESIAN_POINT('',(-0.00606994049506089,-0.0132364631114643,0.00441734105626232));
#22922=CARTESIAN_POINT('',(-0.00660969390960677,-0.0132783935203091,0.00355937001018238));
#22923=CARTESIAN_POINT('',(-0.00731191311291048,-0.0133551858068643,0.00170084474001979));
#22924=CARTESIAN_POINT('',(-0.00747437890166831,-0.0133900476845746,0.000700290515937141));
#22925=CARTESIAN_POINT('',(-0.00739637380170993,-0.0134527029088608,-0.00128485474903298));
#22926=CARTESIAN_POINT('',(-0.00715590291299373,-0.0134804962554366,-0.00226944578992046));
#22927=CARTESIAN_POINT('',(-0.00673286612337111,-0.0135047553364452,-0.00316840087294414));
#22928=CARTESIAN_POINT('',(-0.00686715470388323,-0.00940550978882296,-0.00223150495151719));
#22929=CARTESIAN_POINT('',(-0.00656920986402103,-0.00954286536798665,-0.00314838990270961));
#22930=CARTESIAN_POINT('',(-0.00608524196393579,-0.00967668668158289,-0.00400457010203361));
#22931=CARTESIAN_POINT('',(-0.00482169053582163,-0.00993726077764047,-0.00546055196525008));
#22932=CARTESIAN_POINT('',(-0.00404210700779271,-0.0100640135601018,-0.00606035362914253));
#22933=CARTESIAN_POINT('',(-0.00231078876607709,-0.0103104505938897,-0.00690847159094555));
#22934=CARTESIAN_POINT('',(-0.00135905405239039,-0.0104301348452162,-0.0071567878888561));
#22935=CARTESIAN_POINT('',(0.000565912226934413,-0.0106624348167344,-0.00726266558024452));
#22936=CARTESIAN_POINT('',(0.00153914379257251,-0.010775050536926,-0.00712022697372237));
#22937=CARTESIAN_POINT('',(0.00335302940082875,-0.0109932134461746,-0.00646713309910309));
#22938=CARTESIAN_POINT('',(0.0041936834434469,-0.0110987606352314,-0.00595647783100596));
#22939=CARTESIAN_POINT('',(0.00560933230596968,-0.0113027864822104,-0.00464779463435138));
#22940=CARTESIAN_POINT('',(0.00618432712587431,-0.0114012651401325,-0.00384976670579392));
#22941=CARTESIAN_POINT('',(0.00697763073560119,-0.0115911539248419,-0.00209267198178111));
#22942=CARTESIAN_POINT('',(0.00719593952542345,-0.0116825640516293,-0.00113360518632574));
#22943=CARTESIAN_POINT('',(0.00724131101096593,-0.0118583157740692,0.000793738664923998));
#22944=CARTESIAN_POINT('',(0.00706837370668615,-0.0119426573697218,0.00176201572071837));
#22945=CARTESIAN_POINT('',(0.00635863043279213,-0.0121042720298923,0.00355449367373196));
#22946=CARTESIAN_POINT('',(0.00582182446317788,-0.0121815450944102,0.00437869457095119));
#22947=CARTESIAN_POINT('',(0.00446932477096638,-0.0123290226923114,0.00575254226091774));
#22948=CARTESIAN_POINT('',(0.00365363104836911,-0.0123992272256946,0.00630218905366504));
#22949=CARTESIAN_POINT('',(0.0018724871703906,-0.0125325677613264,0.00703991459362902));
#22950=CARTESIAN_POINT('',(0.000907037015009341,-0.012595703763575,0.00722799334084569));
#22951=CARTESIAN_POINT('',(-0.00102078114276233,-0.0127149072369375,0.00721280908063516));
#22952=CARTESIAN_POINT('',(-0.00198314914515274,-0.0127709747080514,0.00700954607320794));
#22953=CARTESIAN_POINT('',(-0.00375245067005612,-0.0128760411191447,0.0062438537571232));
#22954=CARTESIAN_POINT('',(-0.0045593841925691,-0.012925040059124,0.00568142444846567));
#22955=CARTESIAN_POINT('',(-0.00589007726753176,-0.0130159694079481,0.00428644731519142));
#22956=CARTESIAN_POINT('',(-0.00641383681998144,-0.0130578998167929,0.0034538994905747));
#22957=CARTESIAN_POINT('',(-0.00709524800837267,-0.0131346921033478,0.00165044565872487));
#22958=CARTESIAN_POINT('',(-0.00725289964431421,-0.0131695539810581,0.000679539651491767));
#22959=CARTESIAN_POINT('',(-0.007177205975424,-0.0132322092053439,-0.00124678219753841));
#22960=CARTESIAN_POINT('',(-0.00694386067059226,-0.0132600025519196,-0.00220219803933548));
#22961=CARTESIAN_POINT('',(-0.00653335922005691,-0.013284261632928,-0.00307451547034793));
#22962=CARTESIAN_POINT('',(-0.00671887448318071,-0.00934092867827176,-0.00218332079651008));
#22963=CARTESIAN_POINT('',(-0.00642736306858953,-0.00947828425743542,-0.00308040775147493));
#22964=CARTESIAN_POINT('',(-0.00595384532874271,-0.0096121055710317,-0.00391810073238151));
#22965=CARTESIAN_POINT('',(-0.00471757735246688,-0.00987267966708951,-0.00534264405644659));
#22966=CARTESIAN_POINT('',(-0.00395482711603787,-0.00999943244955104,-0.00592949439960509));
#22967=CARTESIAN_POINT('',(-0.00226089266164871,-0.0102458694833393,-0.00675929922824295));
#22968=CARTESIAN_POINT('',(-0.00132970844368856,-0.0103655537346661,-0.00700225371372232));
#22969=CARTESIAN_POINT('',(0.000553692669704888,-0.0105978537061848,-0.00710584522282366));
#22970=CARTESIAN_POINT('',(0.00150590956513818,-0.0107104694263768,-0.00696648224644565));
#22971=CARTESIAN_POINT('',(0.00328062853598501,-0.0109286323356261,-0.00632749041379919));
#22972=CARTESIAN_POINT('',(0.00410313061139855,-0.0110341795246833,-0.00582786155753075));
#22973=CARTESIAN_POINT('',(0.00548821183203415,-0.011238205371663,-0.00454743632819994));
#22974=CARTESIAN_POINT('',(0.00605079097725621,-0.0113366840295855,-0.00376663995513757));
#22975=CARTESIAN_POINT('',(0.00682696504215606,-0.0115265728142956,-0.00204748560158481));
#22976=CARTESIAN_POINT('',(0.00704055996183384,-0.0116179829410833,-0.00110912762109441));
#22977=CARTESIAN_POINT('',(0.00708495175576022,-0.011793734663524,0.00077659972609268));
#22978=CARTESIAN_POINT('',(0.00691574863000882,-0.0118780762591769,0.00172396909278938));
#22979=CARTESIAN_POINT('',(0.00622133060999841,-0.0120396909193479,0.00347774265687652));
#22980=CARTESIAN_POINT('',(0.00569611571573941,-0.0121169639838661,0.00428414685426696));
#22981=CARTESIAN_POINT('',(0.00437282010607869,-0.0122644415817676,0.00562832950136433));
#22982=CARTESIAN_POINT('',(0.00357473939067698,-0.012334646115151,0.00616610795107126));
#22983=CARTESIAN_POINT('',(0.0018320551686576,-0.0124679866507829,0.006887904025252));
#22984=CARTESIAN_POINT('',(0.000887451662039948,-0.0125311226530315,0.00707192164972581));
#22985=CARTESIAN_POINT('',(-0.000998739750123815,-0.0126503261263939,0.00705706525826911));
#22986=CARTESIAN_POINT('',(-0.00194032765566992,-0.0127063935975077,0.00685819124233861));
#22987=CARTESIAN_POINT('',(-0.00367142523266258,-0.0128114600086006,0.00610903226946734));
#22988=CARTESIAN_POINT('',(-0.00446093490410914,-0.0128604589485796,0.00555874731252656));
#22989=CARTESIAN_POINT('',(-0.00576289475965981,-0.0129513882974029,0.00419389146326531));
#22990=CARTESIAN_POINT('',(-0.00627534494376392,-0.0129933187062471,0.00337932057094484));
#22991=CARTESIAN_POINT('',(-0.00694204264370749,-0.0130701109928008,0.00161480812657567));
#22992=CARTESIAN_POINT('',(-0.00709629015954695,-0.0131049728705102,0.00066486657452696));
#22993=CARTESIAN_POINT('',(-0.0070222309192393,-0.0131676280947944,-0.00121986083819952));
#22994=CARTESIAN_POINT('',(-0.00679392416309219,-0.013195421441369,-0.00215464669887731));
#22995=CARTESIAN_POINT('',(-0.00639228653582991,-0.0132196805223763,-0.00300812846551772));
#22996=CARTESIAN_POINT('',(-0.00642231404177568,-0.00934092867827176,-0.00208695248649585));
#22997=CARTESIAN_POINT('',(-0.00614366947772652,-0.00947828425743542,-0.00294444344900556));
#22998=CARTESIAN_POINT('',(-0.00569105205835654,-0.0096121055710317,-0.00374516199307731));
#22999=CARTESIAN_POINT('',(-0.00450935098575736,-0.00987267966708951,-0.00510682823883964));
#23000=CARTESIAN_POINT('',(-0.00378026733252819,-0.00999943244955104,-0.00566777594053021));
#23001=CARTESIAN_POINT('',(-0.00216110045279195,-0.0102458694833393,-0.00646095450283777));
#23002=CARTESIAN_POINT('',(-0.0012710172262849,-0.0103655537346661,-0.00669318536345474));
#23003=CARTESIAN_POINT('',(0.000529253555245836,-0.0105978537061848,-0.00679220450798197));
#23004=CARTESIAN_POINT('',(0.00143944111026952,-0.0107104694263769,-0.00665899279189221));
#23005=CARTESIAN_POINT('',(0.00313582680629751,-0.0109286323356261,-0.0060482050431914));
#23006=CARTESIAN_POINT('',(0.00392202494730184,-0.0110341795246833,-0.00557062901058033));
#23007=CARTESIAN_POINT('',(0.00524597088416309,-0.011238205371663,-0.00434671971589707));
#23008=CARTESIAN_POINT('',(0.00578371868002002,-0.0113366840295855,-0.00360038645382486));
#23009=CARTESIAN_POINT('',(0.00652563365526577,-0.0115265728142956,-0.00195711284119222));
#23010=CARTESIAN_POINT('',(0.0067298008346546,-0.0116179829410833,-0.00106017249063177));
#23011=CARTESIAN_POINT('',(0.00677223324534879,-0.011793734663524,0.00074232184843004));
#23012=CARTESIAN_POINT('',(0.00661049847665415,-0.0118780762591769,0.0016478758369314));
#23013=CARTESIAN_POINT('',(0.00594673096441099,-0.0120396909193479,0.00332424062316563));
#23014=CARTESIAN_POINT('',(0.00544469822086248,-0.0121169639838661,0.00409505142089849));
#23015=CARTESIAN_POINT('',(0.00417981077630333,-0.0122644415817676,0.00537990398225753));
#23016=CARTESIAN_POINT('',(0.00341695607529269,-0.012334646115151,0.00589394574588371));
#23017=CARTESIAN_POINT('',(0.00175119116519162,-0.0124679866507829,0.00658388288849796));
#23018=CARTESIAN_POINT('',(0.000848280956101175,-0.0125311226530315,0.00675977826748603));
#23019=CARTESIAN_POINT('',(-0.000954656964846769,-0.0126503261263939,0.00674557761353704));
#23020=CARTESIAN_POINT('',(-0.00185468467670427,-0.0127063935975077,0.00655548158059996));
#23021=CARTESIAN_POINT('',(-0.0035093743578755,-0.0128114600086006,0.00583938929415562));
#23022=CARTESIAN_POINT('',(-0.00426403632718924,-0.0128604589485796,0.00531339304064834));
#23023=CARTESIAN_POINT('',(-0.00550852974391592,-0.0129513882974029,0.0040087797594131));
#23024=CARTESIAN_POINT('',(-0.00599836119132888,-0.0129933187062471,0.00323016273168512));
#23025=CARTESIAN_POINT('',(-0.00663563191437715,-0.0130701109928008,0.00154353306227724));
#23026=CARTESIAN_POINT('',(-0.00678307119001246,-0.0131049728705102,0.000635520420597347));
#23027=CARTESIAN_POINT('',(-0.00671228080686991,-0.0131676280947944,-0.00116601811952175));
#23028=CARTESIAN_POINT('',(-0.00649405114809204,-0.013195421441369,-0.00205954401796095));
#23029=CARTESIAN_POINT('',(-0.00611014116737591,-0.0132196805223763,-0.0028753544558573));
#23030=CARTESIAN_POINT('',(-0.00627403382107316,-0.00940550978882296,-0.00203876833148874));
#23031=CARTESIAN_POINT('',(-0.00600182268229503,-0.00954286536798665,-0.00287646129777088));
#23032=CARTESIAN_POINT('',(-0.00555965542316345,-0.00967668668158289,-0.0036586926234252));
#23033=CARTESIAN_POINT('',(-0.00440523780240261,-0.00993726077764048,-0.00498892033003616));
#23034=CARTESIAN_POINT('',(-0.00369298744077334,-0.0100640135601018,-0.00553691671099277));
#23035=CARTESIAN_POINT('',(-0.00211120434836358,-0.0103104505938897,-0.00631178214013517));
#23036=CARTESIAN_POINT('',(-0.00124167161758307,-0.0104301348452162,-0.00653865118832096));
#23037=CARTESIAN_POINT('',(0.000517033998016309,-0.0106624348167344,-0.00663538415056111));
#23038=CARTESIAN_POINT('',(0.00140620688283518,-0.010775050536926,-0.00650524806461549));
#23039=CARTESIAN_POINT('',(0.00306342594145377,-0.0109932134461746,-0.00590856235788749));
#23040=CARTESIAN_POINT('',(0.00383147211525347,-0.0110987606352314,-0.00544201273710513));
#23041=CARTESIAN_POINT('',(0.00512485041022755,-0.0113027864822104,-0.00424636140974563));
#23042=CARTESIAN_POINT('',(0.00565018253140191,-0.0114012651401325,-0.00351725970316852));
#23043=CARTESIAN_POINT('',(0.00637496796182063,-0.0115911539248419,-0.00191192646099593));
#23044=CARTESIAN_POINT('',(0.00657442127106498,-0.0116825640516293,-0.00103569492540045));
#23045=CARTESIAN_POINT('',(0.00661587399014308,-0.0118583157740692,0.000725182909598717));
#23046=CARTESIAN_POINT('',(0.00645787339997682,-0.0119426573697218,0.00160982920900241));
#23047=CARTESIAN_POINT('',(0.00580943114161729,-0.0121042720298923,0.00324748960631018));
#23048=CARTESIAN_POINT('',(0.00531898947342402,-0.0121815450944102,0.00400050370421425));
#23049=CARTESIAN_POINT('',(0.00408330611141565,-0.0123290226923114,0.00525569122270413));
#23050=CARTESIAN_POINT('',(0.00333806441760056,-0.0123992272256946,0.00575786464328994));
#23051=CARTESIAN_POINT('',(0.00171075916345863,-0.0125325677613264,0.00643187232012095));
#23052=CARTESIAN_POINT('',(0.000828695603131796,-0.012595703763575,0.00660370657636615));
#23053=CARTESIAN_POINT('',(-0.000932615572208239,-0.0127149072369375,0.006589833791171));
#23054=CARTESIAN_POINT('',(-0.00181186318722145,-0.0127709747080514,0.00640412674973064));
#23055=CARTESIAN_POINT('',(-0.00342834892048197,-0.0128760411191447,0.00570456780649976));
#23056=CARTESIAN_POINT('',(-0.00416558703872928,-0.012925040059124,0.00519071590470924));
#23057=CARTESIAN_POINT('',(-0.00538134723604398,-0.0130159694079481,0.00391622390748699));
#23058=CARTESIAN_POINT('',(-0.00585986931511135,-0.0130578998167929,0.00315558381205526));
#23059=CARTESIAN_POINT('',(-0.00648242654971197,-0.0131346921033478,0.00150789553012803));
#23060=CARTESIAN_POINT('',(-0.00662646170524521,-0.0131695539810581,0.000620847343632542));
#23061=CARTESIAN_POINT('',(-0.00655730575068521,-0.0132322092053439,-0.00113909676018287));
#23062=CARTESIAN_POINT('',(-0.00634411464059197,-0.0132600025519196,-0.00201199267750278));
#23063=CARTESIAN_POINT('',(-0.00596906848314891,-0.013284261632928,-0.00280896745102709));
#23064=CARTESIAN_POINT('',(-0.00606433392192398,-0.00962600349234004,-0.0019706256459862));
#23065=CARTESIAN_POINT('',(-0.00580122102041663,-0.00976335907150372,-0.00278032001749548));
#23066=CARTESIAN_POINT('',(-0.0053738325196232,-0.00989718038509996,-0.00353640646813335));
#23067=CARTESIAN_POINT('',(-0.00425799952648047,-0.0101577544811575,-0.00482217336629522));
#23068=CARTESIAN_POINT('',(-0.00356955503413119,-0.0102845072636188,-0.00535185381381923));
#23069=CARTESIAN_POINT('',(-0.00204064060077137,-0.0105309442974066,-0.00610082056166993));
#23070=CARTESIAN_POINT('',(-0.00120017065976085,-0.0106506285487331,-0.00632010686199662));
#23071=CARTESIAN_POINT('',(0.000499752934456116,-0.0108829285202512,-0.00641360667424036));
#23072=CARTESIAN_POINT('',(0.00135920658766256,-0.0109955442404428,-0.0062878201861574));
#23073=CARTESIAN_POINT('',(0.0029610356564642,-0.0112137071496912,-0.00571107777844453));
#23074=CARTESIAN_POINT('',(0.00370341107205939,-0.011319254338748,-0.0052601218588146));
#23075=CARTESIAN_POINT('',(0.00495356019330686,-0.0115232801857269,-0.00410443333208948));
#23076=CARTESIAN_POINT('',(0.00546133389895913,-0.0116217588436489,-0.00339970072499429));
#23077=CARTESIAN_POINT('',(0.00616189449476617,-0.0118116476283582,-0.00184802326928778));
#23078=CARTESIAN_POINT('',(0.00635468138492093,-0.0119030577551455,-0.00100107842067645));
#23079=CARTESIAN_POINT('',(0.0063947486108286,-0.0120788094775854,0.000700944789858772));
#23080=CARTESIAN_POINT('',(0.0062420289465815,-0.0121631510732379,0.00155602315178267));
#23081=CARTESIAN_POINT('',(0.005615259870111,-0.0123247657334084,0.00313894727734728));
#23082=CARTESIAN_POINT('',(0.00514121045788761,-0.0124020387979262,0.00386679304098799));
#23083=CARTESIAN_POINT('',(0.00394682790549922,-0.0125495163958273,0.00508002785352392));
#23084=CARTESIAN_POINT('',(0.00322649476533423,-0.0126197209292105,0.00556541690241914));
#23085=CARTESIAN_POINT('',(0.00165357967825393,-0.0127530614648423,0.00621689691269813));
#23086=CARTESIAN_POINT('',(0.000800997731338632,-0.0128161974670908,0.00638298787408191));
#23087=CARTESIAN_POINT('',(-0.000901444335805244,-0.0129354009404534,0.00636957876532512));
#23088=CARTESIAN_POINT('',(-0.00175130445603382,-0.0129914684115673,0.00619007869518455));
#23089=CARTESIAN_POINT('',(-0.00331376164802281,-0.0130965348226607,0.00551390143015753));
#23090=CARTESIAN_POINT('',(-0.00402635871978323,-0.0131455337626401,0.00501722423527107));
#23091=CARTESIAN_POINT('',(-0.00520148400851484,-0.0132364631114643,0.00378533016641609));
#23092=CARTESIAN_POINT('',(-0.00566401222548603,-0.0132783935203091,0.00305011329244757));
#23093=CARTESIAN_POINT('',(-0.00626576144517416,-0.0133551858068643,0.00145749644883311));
#23094=CARTESIAN_POINT('',(-0.00640498244789111,-0.0133900476845746,0.000600096479187167));
#23095=CARTESIAN_POINT('',(-0.00633813792439929,-0.0134527029088608,-0.00110102420868829));
#23096=CARTESIAN_POINT('',(-0.00613207239819051,-0.0134804962554366,-0.0019447449269178));
#23097=CARTESIAN_POINT('',(-0.00576956157983471,-0.0135047553364452,-0.00271508204843087));
#23098=CARTESIAN_POINT('',(-0.00600291424347732,-0.00978191608530591,-0.00195066711549076));
#23099=CARTESIAN_POINT('',(-0.00574246615396974,-0.00991927166446956,-0.00275216088845478));
#23100=CARTESIAN_POINT('',(-0.00531940625127603,-0.0100530929780658,-0.00350058968249359));
#23101=CARTESIAN_POINT('',(-0.0042148744339131,-0.0103136670741236,-0.00477333431135776));
#23102=CARTESIAN_POINT('',(-0.00353340251924386,-0.010440419856585,-0.00529765014618313));
#23103=CARTESIAN_POINT('',(-0.00201997295760755,-0.0106868568903732,-0.00603903134590728));
#23104=CARTESIAN_POINT('',(-0.00118801531064046,-0.0108065411416999,-0.00625609671080607));
#23105=CARTESIAN_POINT('',(0.00049469142812545,-0.0110388411132185,-0.00634864955534044));
#23106=CARTESIAN_POINT('',(0.00134544051992427,-0.0111514568334104,-0.00622413703497603));
#23107=CARTESIAN_POINT('',(0.00293104623631838,-0.0113696197426594,-0.00565323588430546));
#23108=CARTESIAN_POINT('',(0.00366590286091366,-0.0114751669317165,-0.00520684725399929));
#23109=CARTESIAN_POINT('',(0.0049033904503217,-0.011679192778696,-0.00406286356058477));
#23110=CARTESIAN_POINT('',(0.00540602141513444,-0.0117776714366183,-0.00336526849747642));
#23111=CARTESIAN_POINT('',(0.00609948672115684,-0.0119675602213283,-0.00182930645777592));
#23112=CARTESIAN_POINT('',(0.0062903210623665,-0.0120589703481159,-0.000990939481183775));
#23113=CARTESIAN_POINT('',(0.00632998248671984,-0.0122347220705563,0.00069384560895015));
#23114=CARTESIAN_POINT('',(0.00617880956986351,-0.0123190636662091,0.00154026372249193));
#23115=CARTESIAN_POINT('',(0.00555838842139843,-0.01248067832638,0.00310715596523984));
#23116=CARTESIAN_POINT('',(0.00508914018978966,-0.0125579513908981,0.00382763009444596));
#23117=CARTESIAN_POINT('',(0.00390685436447047,-0.0127054289887995,0.0050285772438971));
#23118=CARTESIAN_POINT('',(0.00319381677076005,-0.0127756335221828,0.00550905026414211));
#23119=CARTESIAN_POINT('',(0.00163683219478224,-0.0129089740578147,0.00615393207365234));
#23120=CARTESIAN_POINT('',(0.000792885212514846,-0.0129721100600633,0.00631834086291755));
#23121=CARTESIAN_POINT('',(-0.000892314492040779,-0.0130913135334257,0.00630506756184527));
#23122=CARTESIAN_POINT('',(-0.00173356721432901,-0.0131473810045395,0.00612738547150779));
#23123=CARTESIAN_POINT('',(-0.00328019981295719,-0.0132524474156325,0.00545805654147115));
#23124=CARTESIAN_POINT('',(-0.00398557968929714,-0.0133014463556116,0.004966409701772));
#23125=CARTESIAN_POINT('',(-0.00514880328885766,-0.0133923757044352,0.0037469922772713));
#23126=CARTESIAN_POINT('',(-0.00560664701207822,-0.0134343061132796,0.00301922169246975));
#23127=CARTESIAN_POINT('',(-0.00620230170530152,-0.0135110983998336,0.0014427348996874));
#23128=CARTESIAN_POINT('',(-0.00634011267530426,-0.0135459602775433,0.000594018691706598));
#23129=CARTESIAN_POINT('',(-0.00627394515429806,-0.013608615501828,-0.0010898730165326));
#23130=CARTESIAN_POINT('',(-0.00606996666328912,-0.013636408848403,-0.00192504851679101));
#23131=CARTESIAN_POINT('',(-0.00571112736074751,-0.0136606679294106,-0.00268758365066487));
#23132=CARTESIAN_POINT('',(-0.00600291424347732,-0.0099532476683191,-0.00195066711549076));
#23133=CARTESIAN_POINT('',(-0.00574246615396974,-0.0100906032474828,-0.00275216088845478));
#23134=CARTESIAN_POINT('',(-0.00531940625127604,-0.010224424561079,-0.0035005896824936));
#23135=CARTESIAN_POINT('',(-0.0042148744339131,-0.0104849986571369,-0.00477333431135777));
#23136=CARTESIAN_POINT('',(-0.00353340251924388,-0.0106117514395984,-0.00529765014618313));
#23137=CARTESIAN_POINT('',(-0.00201997295760755,-0.0108581884733867,-0.00603903134590727));
#23138=CARTESIAN_POINT('',(-0.00118801531064046,-0.0109778727247135,-0.00625609671080606));
#23139=CARTESIAN_POINT('',(0.000494691428125452,-0.0112101726962322,-0.00634864955534044));
#23140=CARTESIAN_POINT('',(0.00134544051992427,-0.0113227884164243,-0.00622413703497603));
#23141=CARTESIAN_POINT('',(0.00293104623631838,-0.0115409513256735,-0.00565323588430545));
#23142=CARTESIAN_POINT('',(0.00366590286091367,-0.0116464985147308,-0.00520684725399928));
#23143=CARTESIAN_POINT('',(0.0049033904503217,-0.0118505243617105,-0.00406286356058477));
#23144=CARTESIAN_POINT('',(0.00540602141513444,-0.011949003019633,-0.00336526849747643));
#23145=CARTESIAN_POINT('',(0.00609948672115684,-0.0121388918043431,-0.00182930645777592));
#23146=CARTESIAN_POINT('',(0.0062903210623665,-0.0122303019311308,-0.000990939481183762));
#23147=CARTESIAN_POINT('',(0.00632998248671984,-0.0124060536535715,0.000693845608950163));
#23148=CARTESIAN_POINT('',(0.00617880956986351,-0.0124903952492244,0.00154026372249193));
#23149=CARTESIAN_POINT('',(0.00555838842139842,-0.0126520099093955,0.00310715596523983));
#23150=CARTESIAN_POINT('',(0.00508914018978966,-0.0127292829739137,0.00382763009444597));
#23151=CARTESIAN_POINT('',(0.00390685436447048,-0.0128767605718152,0.00502857724389711));
#23152=CARTESIAN_POINT('',(0.00319381677076006,-0.0129469651051986,0.00550905026414211));
#23153=CARTESIAN_POINT('',(0.00163683219478224,-0.0130803056408305,0.00615393207365233));
#23154=CARTESIAN_POINT('',(0.000792885212514845,-0.0131434416430791,0.00631834086291754));
#23155=CARTESIAN_POINT('',(-0.000892314492040781,-0.0132626451164415,0.00630506756184527));
#23156=CARTESIAN_POINT('',(-0.00173356721432902,-0.0133187125875553,0.00612738547150779));
#23157=CARTESIAN_POINT('',(-0.00328019981295719,-0.0134237789986481,0.00545805654147115));
#23158=CARTESIAN_POINT('',(-0.00398557968929714,-0.0134727779386271,0.004966409701772));
#23159=CARTESIAN_POINT('',(-0.00514880328885766,-0.0135637072874504,0.0037469922772713));
#23160=CARTESIAN_POINT('',(-0.00560664701207823,-0.0136056376962946,0.00301922169246975));
#23161=CARTESIAN_POINT('',(-0.00620230170530153,-0.0136824299828483,0.0014427348996874));
#23162=CARTESIAN_POINT('',(-0.00634011267530426,-0.0137172918605577,0.000594018691706601));
#23163=CARTESIAN_POINT('',(-0.00627394515429805,-0.0137799470848417,-0.0010898730165326));
#23164=CARTESIAN_POINT('',(-0.00606996666328913,-0.0138077404314164,-0.00192504851679101));
#23165=CARTESIAN_POINT('',(-0.00571112736074751,-0.0138319995124236,-0.00268758365066487));
#23166=CARTESIAN_POINT('',(-0.00600351494261159,-0.00996866665836644,-0.00195086231468902));
#23167=CARTESIAN_POINT('',(-0.00574304079060577,-0.0101060222375301,-0.00275243629146672));
#23168=CARTESIAN_POINT('',(-0.00531993855318813,-0.0102398435511264,-0.00350093997921721));
#23169=CARTESIAN_POINT('',(-0.00421529620762514,-0.0105004176471842,-0.00477381196898739));
#23170=CARTESIAN_POINT('',(-0.00353375609947977,-0.0106271704296457,-0.00529818027100706));
#23171=CARTESIAN_POINT('',(-0.00202017509209718,-0.0108736074634341,-0.0060396356592048));
#23172=CARTESIAN_POINT('',(-0.00118813419285994,-0.0109932917147608,-0.00625672274538287));
#23173=CARTESIAN_POINT('',(0.000494740930867045,-0.0112255916862796,-0.00634928485148777));
#23174=CARTESIAN_POINT('',(0.00134557515535679,-0.0113382074064716,-0.0062247598714146));
#23175=CARTESIAN_POINT('',(0.00293133954001475,-0.0115563703157209,-0.00565380159185411));
#23176=CARTESIAN_POINT('',(0.00366626970018299,-0.0116619175047782,-0.00520736829236679));
#23177=CARTESIAN_POINT('',(0.00490388112239846,-0.0118659433517579,-0.0040632701228851));
#23178=CARTESIAN_POINT('',(0.00540656238444571,-0.0119644220096804,-0.00336560525289072));
#23179=CARTESIAN_POINT('',(0.00610009708409794,-0.0121543107943906,-0.00182948951266575));
#23180=CARTESIAN_POINT('',(0.00629095052170294,-0.0122457209211783,-0.000991038642435164));
#23181=CARTESIAN_POINT('',(0.00633061591489246,-0.012421472643619,0.000693915040636126));
#23182=CARTESIAN_POINT('',(0.00617942787047698,-0.0125058142392719,0.00154041785347683));
#23183=CARTESIAN_POINT('',(0.00555894463775888,-0.012667428899443,0.00310746689187023));
#23184=CARTESIAN_POINT('',(0.00508964944945624,-0.0127447019639612,0.00382801311742293));
#23185=CARTESIAN_POINT('',(0.00390724531525525,-0.0128921795618627,0.00502908044315575));
#23186=CARTESIAN_POINT('',(0.0031941363693569,-0.0129623840952461,0.00550960154333586));
#23187=CARTESIAN_POINT('',(0.00163699598917317,-0.0130957246308781,0.00615454788482654));
#23188=CARTESIAN_POINT('',(0.000792964554887801,-0.0131588606331266,0.0063189731261371));
#23189=CARTESIAN_POINT('',(-0.000892403784094793,-0.013278064106489,0.00630569849683322));
#23190=CARTESIAN_POINT('',(-0.00173374068879202,-0.0133341315776028,0.00612799862621877));
#23191=CARTESIAN_POINT('',(-0.00328052805572528,-0.0134391979886957,0.0054586027178292));
#23192=CARTESIAN_POINT('',(-0.00398597851796132,-0.0134881969286747,0.00496690668005408));
#23193=CARTESIAN_POINT('',(-0.00514931851888639,-0.0135791262774979,0.00374736723098973));
#23194=CARTESIAN_POINT('',(-0.00560720805757541,-0.0136210566863421,0.0030195238197005));
#23195=CARTESIAN_POINT('',(-0.0062029223567241,-0.0136978489728957,0.001442879271166));
#23196=CARTESIAN_POINT('',(-0.00634074711718376,-0.0137327108506051,0.000594078133920727));
#23197=CARTESIAN_POINT('',(-0.00627457297493145,-0.0137953660748891,-0.00108998207785698));
#23198=CARTESIAN_POINT('',(-0.00607057407221948,-0.0138231594214637,-0.00192524115238941));
#23199=CARTESIAN_POINT('',(-0.00571169886137572,-0.0138474185024709,-0.00268785259156703));
#23200=CARTESIAN_POINT('',(-0.0060046989412083,-0.00998404147970407,-0.00195124705900381));
#23201=CARTESIAN_POINT('',(-0.00574417341912455,-0.0101213970588677,-0.00275297912024915));
#23202=CARTESIAN_POINT('',(-0.00532098773851402,-0.010255218372464,-0.00350163042607414));
#23203=CARTESIAN_POINT('',(-0.00421612753807775,-0.0105157924685218,-0.00477475344855832));
#23204=CARTESIAN_POINT('',(-0.00353445301825201,-0.0106425452509834,-0.00529922516521753));
#23205=CARTESIAN_POINT('',(-0.00202057350610914,-0.0108889822847717,-0.00604082678144128));
#23206=CARTESIAN_POINT('',(-0.00118836851379201,-0.0110086665360985,-0.00625795668100581));
#23207=CARTESIAN_POINT('',(0.000494838502468596,-0.0112409665076173,-0.00635053704198386));
#23208=CARTESIAN_POINT('',(0.00134584052641207,-0.0113535822278093,-0.00622598750339738));
#23209=CARTESIAN_POINT('',(0.00293191765166019,-0.0115717451370586,-0.00565491662083544));
#23210=CARTESIAN_POINT('',(0.00366699275296484,-0.0116772923261159,-0.00520839527685999));
#23211=CARTESIAN_POINT('',(0.00490484825389107,-0.0118813181730956,-0.00406407147112351));
#23212=CARTESIAN_POINT('',(0.00540762865351265,-0.0119797968310181,-0.00336626900936249));
#23213=CARTESIAN_POINT('',(0.0061013001303894,-0.0121696856157283,-0.00182985032013211));
#23214=CARTESIAN_POINT('',(0.00629219120764457,-0.0122610957425161,-0.000991234092662764));
#23215=CARTESIAN_POINT('',(0.00633186442354634,-0.0124368474649567,0.00069405189287056));
#23216=CARTESIAN_POINT('',(0.00618064656219293,-0.0125211890606097,0.00154072165093453));
#23217=CARTESIAN_POINT('',(0.00556004095928272,-0.0126828037207808,0.00310807973892308));
#23218=CARTESIAN_POINT('',(0.00509065321772592,-0.0127600767852989,0.00382876806884765));
#23219=CARTESIAN_POINT('',(0.00390801589266107,-0.0129075543832005,0.00503007226615351));
#23220=CARTESIAN_POINT('',(0.00319476630915303,-0.0129777589165839,0.00551068813353479));
#23221=CARTESIAN_POINT('',(0.0016373188335356,-0.0131110994522158,0.00615576166977231));
#23222=CARTESIAN_POINT('',(0.000793120941426221,-0.0131742354544644,0.00632021933862854));
#23223=CARTESIAN_POINT('',(-0.000892579781795835,-0.0132934389278268,0.0063069420913346));
#23224=CARTESIAN_POINT('',(-0.00173408261290851,-0.0133495063989406,0.00612920717518442));
#23225=CARTESIAN_POINT('',(-0.00328117503347941,-0.0134545728100334,0.00545967925016396));
#23226=CARTESIAN_POINT('',(-0.00398676462293764,-0.0135035717500124,0.00496788624129369));
#23227=CARTESIAN_POINT('',(-0.00515033405494463,-0.0135945010988356,0.00374810627762912));
#23228=CARTESIAN_POINT('',(-0.00560831389749338,-0.0136364315076798,0.00302011932283482));
#23229=CARTESIAN_POINT('',(-0.00620414568196542,-0.0137132237942334,0.00144316383230204));
#23230=CARTESIAN_POINT('',(-0.00634199762388869,-0.0137480856719428,0.00059419529656355));
#23231=CARTESIAN_POINT('',(-0.0062758104309332,-0.0138107408962268,-0.00109019704146795));
#23232=CARTESIAN_POINT('',(-0.00607177129605443,-0.0138385342428014,-0.00192562084376098));
#23233=CARTESIAN_POINT('',(-0.00571282530871555,-0.0138627933238085,-0.00268838268330946));
#23234=CARTESIAN_POINT('',(-0.00697848962230257,-0.0100021880761874,-0.00276298368595472));
#23235=CARTESIAN_POINT('',(-0.0069784927334439,-0.00984627346412808,-0.00276298497368024));
#23236=CARTESIAN_POINT('',(-0.00685840540887306,-0.00953444168472413,-0.0027154390780474));
#23237=CARTESIAN_POINT('',(-0.00642351660340855,-0.00934069305043517,-0.00254325430359987));
#23238=CARTESIAN_POINT('',(-0.00598862778407599,-0.00953444167233752,-0.0023710695004056));
#23239=CARTESIAN_POINT('',(-0.0058685404369188,-0.0098462734648897,-0.00232352356685033));
#23240=CARTESIAN_POINT('',(-0.00586854353315033,-0.0100021880910911,-0.00232352483977624));
#23241=CARTESIAN_POINT('',(-0.00595196988716087,0.0137864962072417,0.00210067694133285));
#23242=CARTESIAN_POINT('',(-0.00572722627692746,0.0138067909284317,0.00273633130246211));
#23243=CARTESIAN_POINT('',(-0.00540062531389276,0.0138270856496218,0.00333605153597525));
#23244=CARTESIAN_POINT('',(-0.00446089318476394,0.0138732460374782,0.00454750491924395));
#23245=CARTESIAN_POINT('',(-0.00379371870698236,0.0138991117041446,0.00511734584923682));
#23246=CARTESIAN_POINT('',(-0.00228794870083571,0.0139508430374775,0.00594516609786777));
#23247=CARTESIAN_POINT('',(-0.00144935317247064,0.013976708704144,0.00620314541650586));
#23248=CARTESIAN_POINT('',(0.000261328061997682,0.0140284400374772,0.00636484747719175));
#23249=CARTESIAN_POINT('',(0.00113341376810093,0.0140543057041439,0.00626857021923956));
#23250=CARTESIAN_POINT('',(0.00276762255858251,0.0141060370374773,0.00573758506115909));
#23251=CARTESIAN_POINT('',(0.00352974564296082,0.0141319027041441,0.00530287716103082));
#23252=CARTESIAN_POINT('',(0.00481866773505796,0.0141836340374777,0.00416653903580334));
#23253=CARTESIAN_POINT('',(0.00534546674277679,0.0142094997041445,0.00346490881070412));
#23254=CARTESIAN_POINT('',(0.00607708692013597,0.0142612310374782,0.00191013694324312));
#23255=CARTESIAN_POINT('',(0.00628190808977635,0.0142870967041451,0.00105699530088134));
#23256=CARTESIAN_POINT('',(0.00633588145473074,0.0143388280374788,-0.000660465289815461));
#23257=CARTESIAN_POINT('',(0.00618503365004477,0.0143646937041458,-0.00152478423815047));
#23258=CARTESIAN_POINT('',(0.00555248212780469,0.0144164250374796,-0.00312242701203853));
#23259=CARTESIAN_POINT('',(0.00507077841025057,0.0144422907041465,-0.00385575083759157));
#23260=CARTESIAN_POINT('',(0.00385575084356898,0.0144940220374802,-0.00507077841625911));
#23261=CARTESIAN_POINT('',(0.00312242699444151,0.0145198877041471,-0.00555248216937361));
#23262=CARTESIAN_POINT('',(0.00152478425570669,0.0145716190374808,-0.00618503360849201));
#23263=CARTESIAN_POINT('',(0.000660465366099334,0.0145974847041477,-0.00633588129449591));
#23264=CARTESIAN_POINT('',(-0.00105699537720861,0.0146492160374812,-0.0062819082500098));
#23265=CARTESIAN_POINT('',(-0.0019101372309092,0.014675081704148,-0.00607708751951978));
#23266=CARTESIAN_POINT('',(-0.00346490852307661,0.0147268130374814,-0.00534546614337484));
#23267=CARTESIAN_POINT('',(-0.00416653796154343,0.0147526787041481,-0.00481866549771993));
#23268=CARTESIAN_POINT('',(-0.00530287823531816,0.0148044100374813,-0.00352974788026773));
#23269=CARTESIAN_POINT('',(-0.00573758907062607,0.0148302757041478,-0.00276763090847045));
#23270=CARTESIAN_POINT('',(-0.00626856620978494,0.0148820070374808,-0.00113340541817491));
#23271=CARTESIAN_POINT('',(-0.00636483251363591,0.0149078727041471,-0.000261296899676647));
#23272=CARTESIAN_POINT('',(-0.0062205710326375,0.0149540330324328,0.00126510354979954));
#23273=CARTESIAN_POINT('',(-0.00604811696439261,0.014974327694052,0.00192585262016124));
#23274=CARTESIAN_POINT('',(-0.00577681402884133,0.0149946223556712,0.00254307073910409));
#23275=CARTESIAN_POINT('',(-0.00595190119996603,0.013790242654245,0.00210065269900483));
#23276=CARTESIAN_POINT('',(-0.0057271601833291,0.013810537375435,0.00273629972452659));
#23277=CARTESIAN_POINT('',(-0.00540056298934976,0.0138308320966251,0.00333601303712089));
#23278=CARTESIAN_POINT('',(-0.00446084170496059,0.0138769924844815,0.00454745243991991));
#23279=CARTESIAN_POINT('',(-0.0037936749265364,0.0139028581511479,0.00511728679380844));
#23280=CARTESIAN_POINT('',(-0.00228792229734557,0.0139545894844808,0.00594509748919034));
#23281=CARTESIAN_POINT('',(-0.00144933644657894,0.0139804551511473,0.00620307383068371));
#23282=CARTESIAN_POINT('',(0.000261325046207641,0.0140321864844806,0.00636477402528809));
#23283=CARTESIAN_POINT('',(0.00113340068822758,0.0140580521511472,0.00626849787839911));
#23284=CARTESIAN_POINT('',(0.0027675906195382,0.0141097834844806,0.00573751884801782));
#23285=CARTESIAN_POINT('',(0.00352970490882888,0.0141356491511474,0.00530281596452552));
#23286=CARTESIAN_POINT('',(0.0048186121264484,0.014187380484481,0.00416649095291919));
#23287=CARTESIAN_POINT('',(0.00534540505477725,0.0142132461511478,0.00346486882480515));
#23288=CARTESIAN_POINT('',(0.00607701678905984,0.0142649774844815,0.00191011489979349));
#23289=CARTESIAN_POINT('',(0.00628183559501359,0.0142908431511484,0.00105698310289587));
#23290=CARTESIAN_POINT('',(0.00633580833710209,0.0143425744844822,-0.000660457667883747));
#23291=CARTESIAN_POINT('',(0.00618496227323685,0.0143684401511491,-0.00152476664176574));
#23292=CARTESIAN_POINT('',(0.00555241805079674,0.0144201714844829,-0.00312239097846366));
#23293=CARTESIAN_POINT('',(0.00507071989222187,0.0144460371511498,-0.00385570634127959));
#23294=CARTESIAN_POINT('',(0.00385570634725693,0.0144977684844836,-0.00507071989823035));
#23295=CARTESIAN_POINT('',(0.00312239096086684,0.0145236341511504,-0.00555241809236518));
#23296=CARTESIAN_POINT('',(0.00152476665932175,0.0145753654844841,-0.00618496223168457));
#23297=CARTESIAN_POINT('',(0.00066045774416674,0.014601231151151,-0.00633580817686911));
#23298=CARTESIAN_POINT('',(-0.00105698317922226,0.0146529624844846,-0.0062818357552452));
#23299=CARTESIAN_POINT('',(-0.00191011518745625,0.0146788281511513,-0.00607701738843673));
#23300=CARTESIAN_POINT('',(-0.00346486853718096,0.0147305594844847,-0.00534540445538222));
#23301=CARTESIAN_POINT('',(-0.00416648987867168,0.0147564251511514,-0.00481860988913619));
#23302=CARTESIAN_POINT('',(-0.00530281703880047,0.0148081564844846,-0.00352970714610997));
#23303=CARTESIAN_POINT('',(-0.00573752285743853,0.0148340221511511,-0.00276759896932979));
#23304=CARTESIAN_POINT('',(-0.00626849386899076,0.0148857534844841,-0.00113339233839792));
#23305=CARTESIAN_POINT('',(-0.00636475906190493,0.0149116191511505,-0.000261293884246227));
#23306=CARTESIAN_POINT('',(-0.00622049924571945,0.0149577794794361,0.00126508895019375));
#23307=CARTESIAN_POINT('',(-0.00604804716763688,0.0149780741410553,0.00192583039534884));
#23308=CARTESIAN_POINT('',(-0.00577674736298813,0.0149983688026745,0.00254304139144295));
#23309=CARTESIAN_POINT('',(-0.00595186675769869,0.0137939897453371,0.00210064054301644));
#23310=CARTESIAN_POINT('',(-0.00572712704158573,0.0138142844665271,0.00273628389019677));
#23311=CARTESIAN_POINT('',(-0.00540053173754835,0.0138345791877171,0.00333599373238967));
#23312=CARTESIAN_POINT('',(-0.0044608158911076,0.0138807395755735,0.00454742612487075));
#23313=CARTESIAN_POINT('',(-0.00379365297342232,0.0139066052422399,0.00511725718126046));
#23314=CARTESIAN_POINT('',(-0.0022879090576716,0.0139583365755728,0.00594506308629448));
#23315=CARTESIAN_POINT('',(-0.00144932805960615,0.0139842022422394,0.00620303793493879));
#23316=CARTESIAN_POINT('',(0.000261323533980404,0.0140359335755726,0.00636473719382177));
#23317=CARTESIAN_POINT('',(0.00113339412950152,0.0140617992422392,0.00626846160406045));
#23318=CARTESIAN_POINT('',(0.00276757460413526,0.0141135305755727,0.00573748564633126));
#23319=CARTESIAN_POINT('',(0.00352968448324787,0.0141393962422394,0.0053027852783634));
#23320=CARTESIAN_POINT('',(0.00481858424226123,0.014191127575573,0.00416646684240551));
#23321=CARTESIAN_POINT('',(0.00534537412216198,0.0142169932422398,0.00346484877441548));
#23322=CARTESIAN_POINT('',(0.00607698162277769,0.0142687245755735,0.00191010384640302));
#23323=CARTESIAN_POINT('',(0.00628179924349267,0.0142945902422404,0.00105697698638059));
#23324=CARTESIAN_POINT('',(0.00633577167325347,0.0143463215755742,-0.000660453845968899));
#23325=CARTESIAN_POINT('',(0.0061849264822993,0.0143721872422411,-0.00152475781829597));
#23326=CARTESIAN_POINT('',(0.00555238592024543,0.0144239185755749,-0.00312237290991359));
#23327=CARTESIAN_POINT('',(0.00507069054914572,0.0144497842422418,-0.00385568402920415));
#23328=CARTESIAN_POINT('',(0.00385568403518144,0.0145015155755756,-0.00507069055515416));
#23329=CARTESIAN_POINT('',(0.00312237289231688,0.0145273812422425,-0.00555238596181363));
#23330=CARTESIAN_POINT('',(0.00152475783585188,0.0145791125755762,-0.00618492644074726));
#23331=CARTESIAN_POINT('',(0.000660453922251451,0.014604978242243,-0.00633577151302142));
#23332=CARTESIAN_POINT('',(-0.00105697706270654,0.0146567095755766,-0.00628179940372335));
#23333=CARTESIAN_POINT('',(-0.00191010413406411,0.0146825752422434,-0.00607698222215111));
#23334=CARTESIAN_POINT('',(-0.00346484848679295,0.0147343065755768,-0.00534537352277041));
#23335=CARTESIAN_POINT('',(-0.00416646576816422,0.0147601722422434,-0.00481858200496196));
#23336=CARTESIAN_POINT('',(-0.00530278635263213,0.0148119035755766,-0.00352968672051601));
#23337=CARTESIAN_POINT('',(-0.00573748965572877,0.0148377692422432,-0.00276758295387852));
#23338=CARTESIAN_POINT('',(-0.0062684575946753,0.0148895005755761,-0.00113338577972018));
#23339=CARTESIAN_POINT('',(-0.0063647222305252,0.0149153662422425,-0.000261292372199317));
#23340=CARTESIAN_POINT('',(-0.00622046324913771,0.0149615265705281,0.00126508162941836));
#23341=CARTESIAN_POINT('',(-0.00604801216899519,0.0149818212321474,0.00192581925101645));
#23342=CARTESIAN_POINT('',(-0.00577671393429529,0.0150021158937665,0.00254302667545414));
#23343=CARTESIAN_POINT('',(-0.00595186675769868,0.0139226378312596,0.00210064054301645));
#23344=CARTESIAN_POINT('',(-0.00572712704158573,0.0139429325524496,0.00273628389019677));
#23345=CARTESIAN_POINT('',(-0.00540053173754835,0.0139632272736397,0.00333599373238967));
#23346=CARTESIAN_POINT('',(-0.00446081589110761,0.0140093876614961,0.00454742612487074));
#23347=CARTESIAN_POINT('',(-0.00379365297342231,0.0140352533281625,0.00511725718126046));
#23348=CARTESIAN_POINT('',(-0.0022879090576716,0.0140869846614954,0.00594506308629448));
#23349=CARTESIAN_POINT('',(-0.00144932805960616,0.0141128503281619,0.00620303793493879));
#23350=CARTESIAN_POINT('',(0.000261323533980407,0.0141645816614952,0.00636473719382179));
#23351=CARTESIAN_POINT('',(0.00113339412950153,0.0141904473281618,0.00626846160406046));
#23352=CARTESIAN_POINT('',(0.00276757460413526,0.0142421786614953,0.00573748564633127));
#23353=CARTESIAN_POINT('',(0.00352968448324788,0.014268044328162,0.00530278527836341));
#23354=CARTESIAN_POINT('',(0.00481858424226124,0.0143197756614956,0.00416646684240551));
#23355=CARTESIAN_POINT('',(0.00534537412216198,0.0143456413281624,0.00346484877441548));
#23356=CARTESIAN_POINT('',(0.00607698162277769,0.0143973726614961,0.00191010384640303));
#23357=CARTESIAN_POINT('',(0.00628179924349266,0.014423238328163,0.0010569769863806));
#23358=CARTESIAN_POINT('',(0.00633577167325347,0.0144749696614968,-0.000660453845968898));
#23359=CARTESIAN_POINT('',(0.00618492648229931,0.0145008353281637,-0.00152475781829598));
#23360=CARTESIAN_POINT('',(0.00555238592024543,0.0145525666614975,-0.00312237290991359));
#23361=CARTESIAN_POINT('',(0.00507069054914572,0.0145784323281644,-0.00385568402920415));
#23362=CARTESIAN_POINT('',(0.00385568403518144,0.0146301636614982,-0.00507069055515416));
#23363=CARTESIAN_POINT('',(0.00312237289231687,0.014656029328165,-0.00555238596181364));
#23364=CARTESIAN_POINT('',(0.00152475783585188,0.0147077606614987,-0.00618492644074726));
#23365=CARTESIAN_POINT('',(0.000660453922251451,0.0147336263281656,-0.00633577151302143));
#23366=CARTESIAN_POINT('',(-0.00105697706270654,0.0147853576614992,-0.00628179940372336));
#23367=CARTESIAN_POINT('',(-0.00191010413406411,0.0148112233281659,-0.00607698222215111));
#23368=CARTESIAN_POINT('',(-0.00346484848679296,0.0148629546614993,-0.00534537352277042));
#23369=CARTESIAN_POINT('',(-0.00416646576816423,0.014888820328166,-0.00481858200496196));
#23370=CARTESIAN_POINT('',(-0.00530278635263215,0.0149405516614992,-0.003529686720516));
#23371=CARTESIAN_POINT('',(-0.00573748965572878,0.0149664173281658,-0.00276758295387851));
#23372=CARTESIAN_POINT('',(-0.00626845759467531,0.0150181486614987,-0.00113338577972016));
#23373=CARTESIAN_POINT('',(-0.0063647222305252,0.0150440143281651,-0.000261292372199312));
#23374=CARTESIAN_POINT('',(-0.00622046324913772,0.0150901746564507,0.00126508162941836));
#23375=CARTESIAN_POINT('',(-0.0060480121689952,0.0151104693180699,0.00192581925101644));
#23376=CARTESIAN_POINT('',(-0.00577671393429529,0.0151307639796891,0.00254302667545414));
#23377=CARTESIAN_POINT('',(-0.00599013469261116,0.0140475388260902,0.00211414675524317));
#23378=CARTESIAN_POINT('',(-0.0057639499971029,0.0140678335472802,0.00275387701485411));
#23379=CARTESIAN_POINT('',(-0.00543525482619242,0.0140881282684702,0.00335744273254653));
#23380=CARTESIAN_POINT('',(-0.00448949701236366,0.0141342886563267,0.004576664112556));
#23381=CARTESIAN_POINT('',(-0.00381804452501068,0.014160154322993,0.00515015893674575));
#23382=CARTESIAN_POINT('',(-0.00230261932563776,0.014211885656326,0.00598328727653573));
#23383=CARTESIAN_POINT('',(-0.00145864661361782,0.0142377513229925,0.00624292079213596));
#23384=CARTESIAN_POINT('',(0.000263003731538004,0.0142894826563257,0.00640565970747737));
#23385=CARTESIAN_POINT('',(0.00114068136467389,0.0143153483229924,0.00630876510721855));
#23386=CARTESIAN_POINT('',(0.00278536891458071,0.0143670796563258,0.00577437520320702));
#23387=CARTESIAN_POINT('',(0.00355237883135164,0.0143929453229926,0.0053368798994543));
#23388=CARTESIAN_POINT('',(0.00484956565963161,0.0144446766563261,0.00419325542629542));
#23389=CARTESIAN_POINT('',(0.00537974257114063,0.014470542322993,0.00348712625688925));
#23390=CARTESIAN_POINT('',(0.00611605399228327,0.0145222736563267,0.0019223849898906));
#23391=CARTESIAN_POINT('',(0.00632218850191688,0.0145481393229936,0.0010637728922981));
#23392=CARTESIAN_POINT('',(0.00637650795111096,0.0145998706563273,-0.000664700279200542));
#23393=CARTESIAN_POINT('',(0.00622469289067142,0.0146257363229942,-0.00153456135310668));
#23394=CARTESIAN_POINT('',(0.00558808536575638,0.014677467656328,-0.00314244842036324));
#23395=CARTESIAN_POINT('',(0.00510329290128087,0.014703333322995,-0.00388047441371365));
#23396=CARTESIAN_POINT('',(0.00388047441972938,0.0147550646563287,-0.00510329290732795));
#23397=CARTESIAN_POINT('',(0.00314244840265338,0.0147809303229956,-0.00558808540759184));
#23398=CARTESIAN_POINT('',(0.00153456137077547,0.0148326616563293,-0.00622469284885221));
#23399=CARTESIAN_POINT('',(0.000664700355973563,0.0148585273229961,-0.00637650778984869));
#23400=CARTESIAN_POINT('',(-0.00106377296911478,0.0149102586563297,-0.00632218866317778));
#23401=CARTESIAN_POINT('',(-0.00192238527940122,0.0149361243229965,-0.0061160545955104));
#23402=CARTESIAN_POINT('',(-0.00348712596741744,0.0149878556563299,-0.00537974196789524));
#23403=CARTESIAN_POINT('',(-0.00419325434514722,0.0150137213229966,-0.00484956340794746));
#23404=CARTESIAN_POINT('',(-0.00533688098063012,0.0150654526563297,-0.00355238108300445));
#23405=CARTESIAN_POINT('',(-0.00577437923838323,0.0150913183229963,-0.00278537731800922));
#23406=CARTESIAN_POINT('',(-0.0063087610720548,0.0151430496563293,-0.00114067296120705));
#23407=CARTESIAN_POINT('',(-0.00640564464797325,0.0151689153229957,-0.000262972369400112));
#23408=CARTESIAN_POINT('',(-0.00626045814358583,0.0152150756512812,0.00127321555838962));
#23409=CARTESIAN_POINT('',(-0.0060868982774138,0.0152353703129005,0.0019382014377742));
#23410=CARTESIAN_POINT('',(-0.00581385571213493,0.0152556649745197,0.00255937723961472));
#23411=CARTESIAN_POINT('',(-0.00612858938180376,0.0142496328809547,0.00216301269013872));
#23412=CARTESIAN_POINT('',(-0.00589717670173025,0.0142699276021447,0.0028175295378327));
#23413=CARTESIAN_POINT('',(-0.00556088414110103,0.0142902223233348,0.00343504594413876));
#23414=CARTESIAN_POINT('',(-0.00459326628390352,0.0143363827111912,0.00468244814576388));
#23415=CARTESIAN_POINT('',(-0.0039062939876957,0.0143622483778576,0.0052691986063811));
#23416=CARTESIAN_POINT('',(-0.00235584157512295,0.0144139797111905,0.00612158369602103));
#23417=CARTESIAN_POINT('',(-0.00149236145875801,0.014439845377857,0.00638721832504375));
#23418=CARTESIAN_POINT('',(0.000269082743409222,0.0144915767111902,0.00655371875278837));
#23419=CARTESIAN_POINT('',(0.00116704682921152,0.0145174423778569,0.00645458455151026));
#23420=CARTESIAN_POINT('',(0.00284974933457872,0.0145691737111903,0.00590784287381343));
#23421=CARTESIAN_POINT('',(0.00363448775414362,0.0145950393778571,0.00546023539739471));
#23422=CARTESIAN_POINT('',(0.00496165748069727,0.0146467707111907,0.00429017743331958));
#23423=CARTESIAN_POINT('',(0.00550408878768602,0.0146726363778575,0.00356772694566317));
#23424=CARTESIAN_POINT('',(0.00625741915317544,0.0147243677111912,0.00196681858444935));
#23425=CARTESIAN_POINT('',(0.00646831821167611,0.0147502333778581,0.00108836071089195));
#23426=CARTESIAN_POINT('',(0.00652389318897451,0.0148019647111919,-0.000680064018963598));
#23427=CARTESIAN_POINT('',(0.00636856910777225,0.0148278303778588,-0.00157003087526174));
#23428=CARTESIAN_POINT('',(0.00571724717299452,0.0148795617111926,-0.00321508229951153));
#23429=CARTESIAN_POINT('',(0.00522124931941905,0.0149054273778595,-0.00397016686746319));
#23430=CARTESIAN_POINT('',(0.00397016687361797,0.0149571587111933,-0.0052212493256059));
#23431=CARTESIAN_POINT('',(0.00321508228139234,0.0149830243778601,-0.00571724721579696));
#23432=CARTESIAN_POINT('',(0.00157003089333893,0.0150347557111939,-0.00636856906498643));
#23433=CARTESIAN_POINT('',(0.000680064097511137,0.0150606213778607,-0.00652389302398486));
#23434=CARTESIAN_POINT('',(-0.00108836078948416,0.0151123527111943,-0.00646831837666436));
#23435=CARTESIAN_POINT('',(-0.00196681888065166,0.015138218377861,-0.00625741977034543));
#23436=CARTESIAN_POINT('',(-0.00356772664950055,0.0151899497111945,-0.00550408817049734));
#23437=CARTESIAN_POINT('',(-0.00429017632718195,0.0152158153778611,-0.00496165517696819));
#23438=CARTESIAN_POINT('',(-0.00546023650356059,0.0152675467111943,-0.00363449005784066));
#23439=CARTESIAN_POINT('',(-0.00590784700225784,0.0152934123778609,-0.00284975793224229));
#23440=CARTESIAN_POINT('',(-0.00645458042307859,0.0153451437111938,-0.00116703823150876));
#23441=CARTESIAN_POINT('',(-0.0065537033452021,0.0153710093778602,-0.000269050656373603));
#23442=CARTESIAN_POINT('',(-0.00640516103107559,0.0154171697061458,0.00130264438986973));
#23443=CARTESIAN_POINT('',(-0.00622758953936252,0.015437464367765,0.0019830006103188));
#23444=CARTESIAN_POINT('',(-0.00594823592676135,0.0154577590293842,0.00261853413648293));
#23445=CARTESIAN_POINT('',(-0.00622877613608389,0.0143268259409887,0.00219837241280755));
#23446=CARTESIAN_POINT('',(-0.00599358045084044,0.0143471206621787,0.00286358893615395));
#23447=CARTESIAN_POINT('',(-0.00565179036736558,0.0143674153833687,0.00349120015557414));
#23448=CARTESIAN_POINT('',(-0.00466835443418733,0.0144135757712251,0.00475899419128652));
#23449=CARTESIAN_POINT('',(-0.00397015189879237,0.0144394414378915,0.00535533652053114));
#23450=CARTESIAN_POINT('',(-0.00239435355664198,0.0144911727712245,0.00622165592526508));
#23451=CARTESIAN_POINT('',(-0.00151675774988655,0.014517038437891,0.00649163300075439));
#23452=CARTESIAN_POINT('',(0.000273481557722839,0.0145687697712242,0.00666085528444379));
#23453=CARTESIAN_POINT('',(0.00118612505857679,0.0145946354378909,0.00656010049264387));
#23454=CARTESIAN_POINT('',(0.00289633544413129,0.0146463667712243,0.00600442098754409));
#23455=CARTESIAN_POINT('',(0.00369390232883182,0.014672232437891,0.00554949627424423));
#23456=CARTESIAN_POINT('',(0.00504276788439256,0.0147239637712246,0.00436031085645383));
#23457=CARTESIAN_POINT('',(0.00559406655525276,0.0147498294378914,0.0036260501519633));
#23458=CARTESIAN_POINT('',(0.00635971194456203,0.0148015607712252,0.00199897103552053));
#23459=CARTESIAN_POINT('',(0.00657405866301112,0.014827426437892,0.0011061526235683));
#23460=CARTESIAN_POINT('',(0.00663054214898058,0.0148791577712258,-0.000691181325495012));
#23461=CARTESIAN_POINT('',(0.00647267891650096,0.0149050234378927,-0.00159569686260609));
#23462=CARTESIAN_POINT('',(0.0058107095347217,0.0149567547712265,-0.0032676406682102));
#23463=CARTESIAN_POINT('',(0.00530660338542208,0.0149826204378934,-0.00403506893670324));
#23464=CARTESIAN_POINT('',(0.00403506894295862,0.0150343517712272,-0.00530660339171006));
#23465=CARTESIAN_POINT('',(0.0032676406497948,0.0150602174378941,-0.00581070957822385));
#23466=CARTESIAN_POINT('',(0.00159569688097878,0.0151119487712278,-0.00647267887301571));
#23467=CARTESIAN_POINT('',(0.000691181405326598,0.0151378144378947,-0.00663054198129377));
#23468=CARTESIAN_POINT('',(-0.00110615270344529,0.0151895457712282,-0.0065740588306965));
#23469=CARTESIAN_POINT('',(-0.001998971336565,0.015215411437895,-0.00635971257182118));
#23470=CARTESIAN_POINT('',(-0.00362604985095919,0.0152671427712284,-0.00559406592797463));
#23471=CARTESIAN_POINT('',(-0.00436030973223368,0.015293008437895,-0.0050427655430034));
#23472=CARTESIAN_POINT('',(-0.00554949739849309,0.0153447397712283,-0.00369390467018841));
#23473=CARTESIAN_POINT('',(-0.006004425183478,0.0153706054378948,-0.00289634418234465));
#23474=CARTESIAN_POINT('',(-0.00656009629672291,0.0154223367712278,-0.00118611632032359));
#23475=CARTESIAN_POINT('',(-0.00666083962498291,0.0154482024378941,-0.000273448946146293));
#23476=CARTESIAN_POINT('',(-0.00650986902411724,0.0154943627661797,0.00132393929237858));
#23477=CARTESIAN_POINT('',(-0.00632939469289264,0.015514657427799,0.00201541759610565));
#23478=CARTESIAN_POINT('',(-0.00604547436354813,0.0155349520894182,0.00266134046919056));
#23479=CARTESIAN_POINT('',(-0.00645280052909932,0.0144040190010226,0.0022774391563606));
#23480=CARTESIAN_POINT('',(-0.00620914578713664,0.0144243137222126,0.00296658088180299));
#23481=CARTESIAN_POINT('',(-0.00585506286887108,0.0144446084434027,0.00361676478956652));
#23482=CARTESIAN_POINT('',(-0.00483625664252665,0.0144907688312591,0.00493015635248392));
#23483=CARTESIAN_POINT('',(-0.00411294252890566,0.0145166344979255,0.00554794675201068));
#23484=CARTESIAN_POINT('',(-0.00248046896526675,0.0145683658312584,0.00644542423251471));
#23485=CARTESIAN_POINT('',(-0.00157130951524883,0.014594231497925,0.00672511131349197));
#23486=CARTESIAN_POINT('',(0.000283317605548484,0.0146459628312582,0.00690041985209886));
#23487=CARTESIAN_POINT('',(0.00122878527632787,0.0146718284979248,0.00679604130972849));
#23488=CARTESIAN_POINT('',(0.00300050515189807,0.0147235598312582,0.00622037621498455));
#23489=CARTESIAN_POINT('',(0.00382675735668889,0.014749425497925,0.00574908966261098));
#23490=CARTESIAN_POINT('',(0.00522413626073768,0.0148011568312586,0.00451713395807678));
#23491=CARTESIAN_POINT('',(0.00579526295999565,0.0148270224979254,0.00375646480591615));
#23492=CARTESIAN_POINT('',(0.00658844557971067,0.0148787538312591,0.00207086610175894));
#23493=CARTESIAN_POINT('',(0.0068105015001677,0.014904619497926,0.00114593654976237));
#23494=CARTESIAN_POINT('',(0.0068690164732838,0.0149563508312598,-0.000716040378625947));
#23495=CARTESIAN_POINT('',(0.00670547552594285,0.0149822164979267,-0.00165308775501769));
#23496=CARTESIAN_POINT('',(0.00601969772888137,0.0150339478312605,-0.00338516475340689));
#23497=CARTESIAN_POINT('',(0.00549746087916084,0.0150598134979274,-0.00418019437540437));
#23498=CARTESIAN_POINT('',(0.00418019438188475,0.0151115448312611,-0.00549746088567498));
#23499=CARTESIAN_POINT('',(0.00338516473432918,0.015137410497928,-0.00601969777394812));
#23500=CARTESIAN_POINT('',(0.00165308777405119,0.0151891418312618,-0.00670547548089361));
#23501=CARTESIAN_POINT('',(0.000716040461328761,0.0152150074979286,-0.00686901629956595));
#23502=CARTESIAN_POINT('',(-0.00114593663251221,0.0152667388312622,-0.00681050167388406));
#23503=CARTESIAN_POINT('',(-0.00207086641363077,0.0152926044979289,-0.00658844622952983));
#23504=CARTESIAN_POINT('',(-0.00375646449408611,0.0153443358312623,-0.00579526231015681));
#23505=CARTESIAN_POINT('',(-0.00451713279342289,0.015370201497929,-0.00522413383513803));
#23506=CARTESIAN_POINT('',(-0.00574909082729462,0.0154219328312622,-0.00382675978225479));
#23507=CARTESIAN_POINT('',(-0.00622038056182957,0.0154477984979287,-0.00300051420439034));
#23508=CARTESIAN_POINT('',(-0.00679603696289688,0.0154995298312617,-0.00122877622379433));
#23509=CARTESIAN_POINT('',(-0.00690040362942923,0.0155253954979281,-0.000283283821062771));
#23510=CARTESIAN_POINT('',(-0.00674400321434594,0.0155715558262137,0.00137155614196259));
#23511=CARTESIAN_POINT('',(-0.0065570379366458,0.0155918504878329,0.00208790417995068));
#23512=CARTESIAN_POINT('',(-0.00626290611822919,0.0156121451494521,0.00275705833899229));
#23513=CARTESIAN_POINT('',(-0.00657663816783462,0.0144040190010226,0.00232114617724482));
#23514=CARTESIAN_POINT('',(-0.00632830737432266,0.0144243137222126,0.00302351342913078));
#23515=CARTESIAN_POINT('',(-0.00596742914411203,0.0144446084434027,0.00368617521212354));
#23516=CARTESIAN_POINT('',(-0.00492907070058215,0.0144907688312591,0.00502477246815869));
#23517=CARTESIAN_POINT('',(-0.00419187524792228,0.0145166344979255,0.00565441906934018));
#23518=CARTESIAN_POINT('',(-0.00252807239237249,0.0145683658312584,0.00656912031052029));
#23519=CARTESIAN_POINT('',(-0.00160146498948257,0.014594231497925,0.00685417495051891));
#23520=CARTESIAN_POINT('',(0.000288754839060511,0.0146459628312582,0.00703284788809851));
#23521=CARTESIAN_POINT('',(0.00125236726471367,0.0146718284979248,0.00692646618567949));
#23522=CARTESIAN_POINT('',(0.00305808875011229,0.0147235598312582,0.00633975332869435));
#23523=CARTESIAN_POINT('',(0.00390019780985774,0.014749425497925,0.00585942217412823));
#23524=CARTESIAN_POINT('',(0.0053243942333875,0.0148011568312586,0.00460382363656548));
#23525=CARTESIAN_POINT('',(0.00590648159717181,0.0148270224979254,0.00382855625356886));
#23526=CARTESIAN_POINT('',(0.0067148864234727,0.0148787538312591,0.00211060871692616));
#23527=CARTESIAN_POINT('',(0.00694120388598928,0.014904619497926,0.00116792856328008));
#23528=CARTESIAN_POINT('',(0.00700084183758095,0.0149563508312598,-0.000729782125225469));
#23529=CARTESIAN_POINT('',(0.00683416232665603,0.0149822164979267,-0.00168481266008494));
#23530=CARTESIAN_POINT('',(0.00613522356131385,0.0150339478312605,-0.00345013046990494));
#23531=CARTESIAN_POINT('',(0.00560296430689659,0.0150598134979274,-0.00426041774486547));
#23532=CARTESIAN_POINT('',(0.00426041775147021,0.0151115448312612,-0.00560296431353574));
#23533=CARTESIAN_POINT('',(0.0034501304504611,0.015137410497928,-0.00613522360724549));
#23534=CARTESIAN_POINT('',(0.00168481267948373,0.0151891418312618,-0.00683416228074224));
#23535=CARTESIAN_POINT('',(0.000729782209515462,0.0152150074979286,-0.00700084166052923));
#23536=CARTESIAN_POINT('',(-0.00116792864761801,0.0152667388312622,-0.00694120406303948));
#23537=CARTESIAN_POINT('',(-0.00211060903478322,0.0152926044979289,-0.00671488708576274));
#23538=CARTESIAN_POINT('',(-0.00382855593575439,0.0153443358312623,-0.00590648093486172));
#23539=CARTESIAN_POINT('',(-0.00460382244956036,0.015370201497929,-0.00532439176123744));
#23540=CARTESIAN_POINT('',(-0.00585942336116365,0.0154219328312622,-0.00390020028197342));
#23541=CARTESIAN_POINT('',(-0.00633975775896098,0.0154477984979287,-0.00305809797633367));
#23542=CARTESIAN_POINT('',(-0.00692646175542653,0.0154995298312617,-0.00125235803845024));
#23543=CARTESIAN_POINT('',(-0.00703283135409475,0.0155253954979281,-0.000288720406206559));
#23544=CARTESIAN_POINT('',(-0.00687342941153299,0.0155715558262137,0.00139787808903776));
#23545=CARTESIAN_POINT('',(-0.00668287602686883,0.0155918504878329,0.00212797377800887));
#23546=CARTESIAN_POINT('',(-0.00638309943612347,0.0156121451494521,0.00280996987608639));
#23547=CARTESIAN_POINT('',(-0.00680066256085005,0.0143268259409887,0.00240021292079786));
#23548=CARTESIAN_POINT('',(-0.00654387271061886,0.0143471206621787,0.00312650537477982));
#23549=CARTESIAN_POINT('',(-0.00617070164561753,0.0143674153833687,0.00381173984611592));
#23550=CARTESIAN_POINT('',(-0.00509697290892147,0.0144135757712251,0.00519593462935609));
#23551=CARTESIAN_POINT('',(-0.00433466587803557,0.0144394414378915,0.00584702930081972));
#23552=CARTESIAN_POINT('',(-0.00261418780099725,0.0144911727712245,0.00679288861776992));
#23553=CARTESIAN_POINT('',(-0.00165601675484485,0.014517038437891,0.00708765326325648));
#23554=CARTESIAN_POINT('',(0.000298590886886155,0.0145687697712242,0.00727241245575358));
#23555=CARTESIAN_POINT('',(0.00129502748246475,0.0145946354378909,0.00716240700276411));
#23556=CARTESIAN_POINT('',(0.00316225845787908,0.0146463667712243,0.00655570855613481));
#23557=CARTESIAN_POINT('',(0.00403305283771481,0.014672232437891,0.00605901556249498));
#23558=CARTESIAN_POINT('',(0.00550576260973262,0.0147239637712246,0.00476064673818843));
#23559=CARTESIAN_POINT('',(0.00610767800191471,0.0147498294378915,0.0039589709075217));
#23560=CARTESIAN_POINT('',(0.00694362005862133,0.0148015607712252,0.00218250378316456));
#23561=CARTESIAN_POINT('',(0.00717764672314587,0.014827426437892,0.00120771248947415));
#23562=CARTESIAN_POINT('',(0.00723931616188416,0.0148791577712258,-0.000754641178356403));
#23563=CARTESIAN_POINT('',(0.00706695893609793,0.0149050234378927,-0.00174220355249655));
#23564=CARTESIAN_POINT('',(0.00634421175547352,0.0149567547712265,-0.00356765455510164));
#23565=CARTESIAN_POINT('',(0.00579382180063536,0.0149826204378934,-0.00440554318356661));
#23566=CARTESIAN_POINT('',(0.00440554319039633,0.0150343517712272,-0.00579382180750066));
#23567=CARTESIAN_POINT('',(0.00356765453499547,0.0150602174378941,-0.00634421180296976));
#23568=CARTESIAN_POINT('',(0.00174220357255612,0.0151119487712278,-0.00706695888862014));
#23569=CARTESIAN_POINT('',(0.000754641265517627,0.0151378144378947,-0.00723931597880142));
#23570=CARTESIAN_POINT('',(-0.00120771257668493,0.0151895457712282,-0.00717764690622705));
#23571=CARTESIAN_POINT('',(-0.00218250411184899,0.015215411437895,-0.00694362074347139));
#23572=CARTESIAN_POINT('',(-0.00395897057888131,0.0152671427712284,-0.00610767731704391));
#23573=CARTESIAN_POINT('',(-0.00476064551074956,0.015293008437895,-0.00550576005337207));
#23574=CARTESIAN_POINT('',(-0.00605901678996518,0.0153447397712283,-0.0040330553940398));
#23575=CARTESIAN_POINT('',(-0.00655571313731255,0.0153706054378948,-0.00316226799837936));
#23576=CARTESIAN_POINT('',(-0.00716240242160049,0.0154223367712278,-0.00129501794192098));
#23577=CARTESIAN_POINT('',(-0.00727239535854106,0.0154482024378941,-0.000298555281123038));
#23578=CARTESIAN_POINT('',(-0.00710756360176169,0.0154943627661797,0.00144549493862177));
#23579=CARTESIAN_POINT('',(-0.00691051927062198,0.015514657427799,0.0022004603618539));
#23580=CARTESIAN_POINT('',(-0.00660053119080453,0.0155349520894182,0.00290568774588812));
#23581=CARTESIAN_POINT('',(-0.00690084931513019,0.0142496328809547,0.00243557264346669));
#23582=CARTESIAN_POINT('',(-0.00664027645972905,0.0142699276021447,0.00317256477310107));
#23583=CARTESIAN_POINT('',(-0.00626160787188208,0.0142902223233348,0.00386789405755129));
#23584=CARTESIAN_POINT('',(-0.00517206105920528,0.0143363827111912,0.00527248067487872));
#23585=CARTESIAN_POINT('',(-0.00439852378913223,0.0143622483778576,0.00593316721496976));
#23586=CARTESIAN_POINT('',(-0.00265269978251628,0.0144139797111905,0.00689296084701396));
#23587=CARTESIAN_POINT('',(-0.00168041304597338,0.014439845377857,0.00719206793896712));
#23588=CARTESIAN_POINT('',(0.000302989701199774,0.0144915767111902,0.007379548987409));
#23589=CARTESIAN_POINT('',(0.00131410571183002,0.0145174423778569,0.00726792294389772));
#23590=CARTESIAN_POINT('',(0.00320884456743164,0.0145691737111903,0.00665228666986547));
#23591=CARTESIAN_POINT('',(0.00409246741240301,0.0145950393778571,0.0061482764393445));
#23592=CARTESIAN_POINT('',(0.00558687301342791,0.0146467707111907,0.00483078016132268));
#23593=CARTESIAN_POINT('',(0.00619765576948144,0.0146726363778575,0.00401729411382184));
#23594=CARTESIAN_POINT('',(0.00704591285000792,0.0147243677111912,0.00221465623423575));
#23595=CARTESIAN_POINT('',(0.00728338717448087,0.0147502333778581,0.0012255044021505));
#23596=CARTESIAN_POINT('',(0.00734596512189023,0.0148019647111919,-0.000765758484887816));
#23597=CARTESIAN_POINT('',(0.00717106874482664,0.0148278303778588,-0.00176786953984089));
#23598=CARTESIAN_POINT('',(0.00643767411720071,0.0148795617111926,-0.00362021292380031));
#23599=CARTESIAN_POINT('',(0.00587917586663838,0.0149054273778595,-0.00447044525280665));
#23600=CARTESIAN_POINT('',(0.00447044525973699,0.0149571587111933,-0.00587917587360483));
#23601=CARTESIAN_POINT('',(0.00362021290339794,0.0149830243778601,-0.00643767416539666));
#23602=CARTESIAN_POINT('',(0.00176786956019598,0.0150347557111939,-0.00717106869664941));
#23603=CARTESIAN_POINT('',(0.000765758573333092,0.0150606213778607,-0.00734596493611033));
#23604=CARTESIAN_POINT('',(-0.00122550449064606,0.0151123527111943,-0.0072833873602592));
#23605=CARTESIAN_POINT('',(-0.00221465656776232,0.015138218377861,-0.00704591354494714));
#23606=CARTESIAN_POINT('',(-0.00401729378033993,0.0151899497111945,-0.00619765507452119));
#23607=CARTESIAN_POINT('',(-0.00483077891580129,0.0152158153778611,-0.00558687041940729));
#23608=CARTESIAN_POINT('',(-0.00614827768489768,0.0152675467111943,-0.00409247000638756));
#23609=CARTESIAN_POINT('',(-0.00665229131853271,0.0152934123778609,-0.00320885424848173));
#23610=CARTESIAN_POINT('',(-0.00726791829524481,0.0153451437111938,-0.00131409603073581));
#23611=CARTESIAN_POINT('',(-0.00737953163832187,0.0153710093778602,-0.00030295357089573));
#23612=CARTESIAN_POINT('',(-0.00721227159480333,0.0154171697061458,0.00146678984113062));
#23613=CARTESIAN_POINT('',(-0.0070123244241521,0.015437464367765,0.00223287734764075));
#23614=CARTESIAN_POINT('',(-0.00669776962759131,0.0154577590293842,0.00294849407859576));
#23615=CARTESIAN_POINT('',(-0.00703930400432278,0.0140475388260902,0.00248443857836225));
#23616=CARTESIAN_POINT('',(-0.0067735031643564,0.0140678335472802,0.00323621729607965));
#23617=CARTESIAN_POINT('',(-0.0063872371867907,0.0140881282684702,0.00394549726914353));
#23618=CARTESIAN_POINT('',(-0.00527583033074515,0.0141342886563267,0.00537826470808661));
#23619=CARTESIAN_POINT('',(-0.00448677325181727,0.014160154322993,0.0060522068846051));
#23620=CARTESIAN_POINT('',(-0.00270592203200148,0.014211885656326,0.00703125726649926));
#23621=CARTESIAN_POINT('',(-0.00171412789111358,0.0142377513229925,0.00733636547187492));
#23622=CARTESIAN_POINT('',(0.000309068713070991,0.0142894826563257,0.00752760803272));
#23623=CARTESIAN_POINT('',(0.00134047117636765,0.0143153483229924,0.00741374238818943));
#23624=CARTESIAN_POINT('',(0.00327322498742965,0.0143670796563258,0.00678575434047188));
#23625=CARTESIAN_POINT('',(0.00417457633519498,0.0143929453229926,0.00627163193728491));
#23626=CARTESIAN_POINT('',(0.00569896483449358,0.0144446766563261,0.00492770216834684));
#23627=CARTESIAN_POINT('',(0.00632200198602683,0.014470542322993,0.00409789480259574));
#23628=CARTESIAN_POINT('',(0.00718727801090009,0.0145222736563267,0.0022590898287945));
#23629=CARTESIAN_POINT('',(0.00742951688424009,0.0145481393229936,0.00125009222074435));
#23630=CARTESIAN_POINT('',(0.00749335035975378,0.0145998706563273,-0.000781122224650873));
#23631=CARTESIAN_POINT('',(0.00731494496192747,0.0146257363229942,-0.00180333906199595));
#23632=CARTESIAN_POINT('',(0.00656683592443885,0.014677467656328,-0.0036928468029486));
#23633=CARTESIAN_POINT('',(0.00599713228477656,0.014703333322995,-0.00456013770655619));
#23634=CARTESIAN_POINT('',(0.00456013771362558,0.0147550646563287,-0.00599713229188277));
#23635=CARTESIAN_POINT('',(0.00369284678213689,0.0147809303229956,-0.00656683597360177));
#23636=CARTESIAN_POINT('',(0.00180333908275944,0.0148326616563293,-0.00731494491278363));
#23637=CARTESIAN_POINT('',(0.000781122314870668,0.0148585273229961,-0.0074933501702465));
#23638=CARTESIAN_POINT('',(-0.00125009231101543,0.0149102586563297,-0.00742951707374577));
#23639=CARTESIAN_POINT('',(-0.00225909016901275,0.0149361243229965,-0.00718727871978218));
#23640=CARTESIAN_POINT('',(-0.00409789446242306,0.0149878556563299,-0.0063220012771233));
#23641=CARTESIAN_POINT('',(-0.00492770089783603,0.0150137213229966,-0.005698962188428));
#23642=CARTESIAN_POINT('',(-0.00627163320782816,0.0150654526563298,-0.00417457898122375));
#23643=CARTESIAN_POINT('',(-0.00678575908240733,0.0150913183229963,-0.00327323486271478));
#23644=CARTESIAN_POINT('',(-0.00741373764626861,0.0151430496563293,-0.00134046130103752));
#23645=CARTESIAN_POINT('',(-0.00752759033555073,0.0151689153229957,-0.000309031857869217));
#23646=CARTESIAN_POINT('',(-0.0073569744822931,0.0152150756512812,0.00149621867261073));
#23647=CARTESIAN_POINT('',(-0.00715301568610083,0.0152353703129005,0.00227767652018535));
#23648=CARTESIAN_POINT('',(-0.00683214984221773,0.0152556649745197,0.00300765097546396));
#23649=CARTESIAN_POINT('',(-0.00707757193923525,0.0139226378312596,0.00249794479058897));
#23650=CARTESIAN_POINT('',(-0.00681032611987357,0.0139429325524497,0.003253810420737));
#23651=CARTESIAN_POINT('',(-0.00642196027543476,0.0139632272736397,0.00396694626930039));
#23652=CARTESIAN_POINT('',(-0.0053045114520012,0.0140093876614961,0.00540750269577186));
#23653=CARTESIAN_POINT('',(-0.00451116480340562,0.0140352533281625,0.0060851086400904));
#23654=CARTESIAN_POINT('',(-0.00272063229996764,0.0140869846614954,0.00706948145674052));
#23655=CARTESIAN_POINT('',(-0.00172344644512523,0.014112850328162,0.00737624832907208));
#23656=CARTESIAN_POINT('',(0.000310748910628593,0.0141645816614952,0.00756853054637559));
#23657=CARTESIAN_POINT('',(0.00134775841154002,0.0141904473281618,0.00745404589134753));
#23658=CARTESIAN_POINT('',(0.0032910192978751,0.0142421786614952,0.00682264389734763));
#23659=CARTESIAN_POINT('',(0.00419727068329876,0.014268044328162,0.0063057265583758));
#23660=CARTESIAN_POINT('',(0.00572994625186395,0.0143197756614956,0.00495449075223675));
#23661=CARTESIAN_POINT('',(0.00635637043500549,0.0143456413281624,0.00412017228506952));
#23662=CARTESIAN_POINT('',(0.00722635038040567,0.0143973726614961,0.00227137097228208));
#23663=CARTESIAN_POINT('',(0.00746990614266432,0.014423238328163,0.00125688812666185));
#23664=CARTESIAN_POINT('',(0.00753408663761127,0.0144749696614968,-0.000785368657882517));
#23665=CARTESIAN_POINT('',(0.00735471137029958,0.0145008353281637,-0.00181314259680666));
#23666=CARTESIAN_POINT('',(0.00660253536994981,0.0145525666614975,-0.00371292231339824));
#23667=CARTESIAN_POINT('',(0.00602973463691172,0.0145784323281644,-0.00458492809106568));
#23668=CARTESIAN_POINT('',(0.00458492809817352,0.0146301636614982,-0.00602973464405655));
#23669=CARTESIAN_POINT('',(0.0037129222924734,0.014656029328165,-0.00660253541937998));
#23670=CARTESIAN_POINT('',(0.00181314261768302,0.0147077606614987,-0.00735471132088858));
#23671=CARTESIAN_POINT('',(0.000785368748592778,0.0147336263281656,-0.00753408644707376));
#23672=CARTESIAN_POINT('',(-0.00125688821742367,0.0147853576614992,-0.0074699063332002));
#23673=CARTESIAN_POINT('',(-0.00227137131434987,0.0148112233281659,-0.00722635109314147));
#23674=CARTESIAN_POINT('',(-0.00412017194304755,0.0148629546614994,-0.00635636972224812));
#23675=CARTESIAN_POINT('',(-0.00495448947481904,0.014888820328166,-0.0057299435914135));
#23676=CARTESIAN_POINT('',(-0.00630572783582616,0.0149405516614992,-0.00419727334371219));
#23677=CARTESIAN_POINT('',(-0.00682264866506178,0.0149664173281658,-0.00329102922684548));
#23678=CARTESIAN_POINT('',(-0.0074540411236481,0.0150181486614987,-0.0013477484825244));
#23679=CARTESIAN_POINT('',(-0.00756851275299878,0.0150440143281651,-0.000310711855070012));
#23680=CARTESIAN_POINT('',(-0.00739696937674122,0.0150901746564507,0.00150435260158199));
#23681=CARTESIAN_POINT('',(-0.00719190179451943,0.01511046931807,0.0022900587069431));
#23682=CARTESIAN_POINT('',(-0.00686929162005737,0.0151307639796891,0.00302400153962454));
#23683=CARTESIAN_POINT('',(-0.00707757193923526,0.0137939897455748,0.00249794479058897));
#23684=CARTESIAN_POINT('',(-0.00681032611987357,0.0138142844667648,0.003253810420737));
#23685=CARTESIAN_POINT('',(-0.00642196027543476,0.0138345791879549,0.00396694626930039));
#23686=CARTESIAN_POINT('',(-0.0053045114520012,0.0138807395758113,0.00540750269577185));
#23687=CARTESIAN_POINT('',(-0.00451116480340562,0.0139066052424777,0.0060851086400904));
#23688=CARTESIAN_POINT('',(-0.00272063229996764,0.0139583365758106,0.00706948145674052));
#23689=CARTESIAN_POINT('',(-0.00172344644512524,0.0139842022424771,0.00737624832907208));
#23690=CARTESIAN_POINT('',(0.000310748910628593,0.0140359335758103,0.00756853054637559));
#23691=CARTESIAN_POINT('',(0.00134775841154002,0.014061799242477,0.00745404589134753));
#23692=CARTESIAN_POINT('',(0.0032910192978751,0.0141135305758104,0.00682264389734764));
#23693=CARTESIAN_POINT('',(0.00419727068329876,0.0141393962424772,0.00630572655837581));
#23694=CARTESIAN_POINT('',(0.00572994625186395,0.0141911275758108,0.00495449075223675));
#23695=CARTESIAN_POINT('',(0.00635637043500548,0.0142169932424776,0.00412017228506952));
#23696=CARTESIAN_POINT('',(0.00722635038040566,0.0142687245758113,0.00227137097228208));
#23697=CARTESIAN_POINT('',(0.00746990614266432,0.0142945902424782,0.00125688812666185));
#23698=CARTESIAN_POINT('',(0.00753408663761127,0.014346321575812,-0.000785368657882514));
#23699=CARTESIAN_POINT('',(0.00735471137029958,0.0143721872424789,-0.00181314259680666));
#23700=CARTESIAN_POINT('',(0.00660253536994981,0.0144239185758127,-0.00371292231339824));
#23701=CARTESIAN_POINT('',(0.00602973463691172,0.0144497842424796,-0.00458492809106569));
#23702=CARTESIAN_POINT('',(0.00458492809817352,0.0145015155758134,-0.00602973464405656));
#23703=CARTESIAN_POINT('',(0.0037129222924734,0.0145273812424802,-0.00660253541937998));
#23704=CARTESIAN_POINT('',(0.00181314261768302,0.0145791125758139,-0.00735471132088859));
#23705=CARTESIAN_POINT('',(0.000785368748592778,0.0146049782424808,-0.00753408644707376));
#23706=CARTESIAN_POINT('',(-0.00125688821742367,0.0146567095758144,-0.0074699063332002));
#23707=CARTESIAN_POINT('',(-0.00227137131434987,0.0146825752424811,-0.00722635109314146));
#23708=CARTESIAN_POINT('',(-0.00412017194304755,0.0147343065758145,-0.00635636972224813));
#23709=CARTESIAN_POINT('',(-0.00495448947481902,0.0147601722424812,-0.00572994359141352));
#23710=CARTESIAN_POINT('',(-0.00630572783582614,0.0148119035758144,-0.0041972733437122));
#23711=CARTESIAN_POINT('',(-0.00682264866506178,0.0148377692424809,-0.00329102922684549));
#23712=CARTESIAN_POINT('',(-0.0074540411236481,0.0148895005758139,-0.0013477484825244));
#23713=CARTESIAN_POINT('',(-0.00756851275299878,0.0149153662424803,-0.000310711855070013));
#23714=CARTESIAN_POINT('',(-0.00739696937674121,0.0149615265707659,0.00150435260158199));
#23715=CARTESIAN_POINT('',(-0.00719190179451944,0.0149818212323851,0.0022900587069431));
#23716=CARTESIAN_POINT('',(-0.00686929162005737,0.0150021158940043,0.00302400153962454));
#23717=CARTESIAN_POINT('',(-0.00707753749697229,0.0137902426547206,0.00249793263460213));
#23718=CARTESIAN_POINT('',(-0.0068102929781344,0.0138105373759106,0.00325379458640919));
#23719=CARTESIAN_POINT('',(-0.00642192902363732,0.0138308320971006,0.00396692696457162));
#23720=CARTESIAN_POINT('',(-0.00530448563815149,0.013876992484957,0.00540747638072603));
#23721=CARTESIAN_POINT('',(-0.00451114285029432,0.0139028581516234,0.00608507902754618));
#23722=CARTESIAN_POINT('',(-0.00272061906029534,0.0139545894849563,0.00706944705384903));
#23723=CARTESIAN_POINT('',(-0.00172343805815352,0.0139804551516229,0.00737621243333172));
#23724=CARTESIAN_POINT('',(0.000310747398401548,0.0140321864849561,0.00756849371491394));
#23725=CARTESIAN_POINT('',(0.00134775185281479,0.0140580521516227,0.00745400961701348));
#23726=CARTESIAN_POINT('',(0.00329100328247419,0.0141097834849562,0.00682261069566529));
#23727=CARTESIAN_POINT('',(0.00419725025772034,0.0141356491516229,0.00630569587221758));
#23728=CARTESIAN_POINT('',(0.00572991836768031,0.0141873804849565,0.00495446664172613));
#23729=CARTESIAN_POINT('',(0.00635633950239413,0.0142132461516233,0.00412015223468239));
#23730=CARTESIAN_POINT('',(0.00722631521412797,0.0142649774849571,0.00227135991889301));
#23731=CARTESIAN_POINT('',(0.00746986979114801,0.0142908431516239,0.00125688201014735));
#23732=CARTESIAN_POINT('',(0.0075340499737673,0.0143425744849577,-0.000785364835968151));
#23733=CARTESIAN_POINT('',(0.00735467557936657,0.0143684401516246,-0.00181313377333801));
#23734=CARTESIAN_POINT('',(0.00660250323940257,0.0144201714849584,-0.00371290424485047));
#23735=CARTESIAN_POINT('',(0.00602970529383929,0.0144460371516253,-0.00458490577899308));
#23736=CARTESIAN_POINT('',(0.00458490578610087,0.0144977684849591,-0.0060297053009841));
#23737=CARTESIAN_POINT('',(0.00371290422392572,0.014523634151626,-0.0066025032888325));
#23738=CARTESIAN_POINT('',(0.00181313379421427,0.0145753654849597,-0.00735467552995582));
#23739=CARTESIAN_POINT('',(0.000785364926677974,0.0146012311516265,-0.00753404978323072));
#23740=CARTESIAN_POINT('',(-0.00125688210090873,0.0146529624849601,-0.00746986998168296));
#23741=CARTESIAN_POINT('',(-0.00227136026095913,0.0146788281516269,-0.00722631592686031));
#23742=CARTESIAN_POINT('',(-0.00412015189266208,0.0147305594849603,-0.00635633878964025));
#23743=CARTESIAN_POINT('',(-0.00495446536431462,0.0147564251516269,-0.00572991570724283));
#23744=CARTESIAN_POINT('',(-0.0063056971496617,0.0148081564849601,-0.00419725291812084));
#23745=CARTESIAN_POINT('',(-0.00682261546335623,0.0148340221516267,-0.00329101321139626));
#23746=CARTESIAN_POINT('',(-0.00745400484933725,0.0148857534849596,-0.00134774192384749));
#23747=CARTESIAN_POINT('',(-0.00756847592162372,0.014911619151626,-0.000310710343023295));
#23748=CARTESIAN_POINT('',(-0.00739693338016404,0.0149577794799116,0.00150434528080753));
#23749=CARTESIAN_POINT('',(-0.00719186679588219,0.0149780741415309,0.00229004756261212));
#23750=CARTESIAN_POINT('',(-0.00686925819136877,0.0149983688031501,0.0030239868236376));
#23751=CARTESIAN_POINT('',(-0.00707746880978615,0.0137864962079549,0.00249790839227718));
#23752=CARTESIAN_POINT('',(-0.00681022688454442,0.0138067909291449,0.00325376300847767));
#23753=CARTESIAN_POINT('',(-0.00642186669910222,0.013827085650335,0.00396688846572214));
#23754=CARTESIAN_POINT('',(-0.00530443415835466,0.0138732460381914,0.00540742390140863));
#23755=CARTESIAN_POINT('',(-0.00451109906985392,0.0138991117048577,0.00608501997212528));
#23756=CARTESIAN_POINT('',(-0.00272059265680856,0.0139508430381907,0.00706937844518029));
#23757=CARTESIAN_POINT('',(-0.00172342133226394,0.0139767087048572,0.00737614084751863));
#23758=CARTESIAN_POINT('',(0.000310744382611889,0.0140284400381904,0.00756842026301959));
#23759=CARTESIAN_POINT('',(0.0013477387729431,0.0140543057048571,0.00745393727618219));
#23760=CARTESIAN_POINT('',(0.00329097134343394,0.0141060370381905,0.00682254448253241));
#23761=CARTESIAN_POINT('',(0.00419720952359356,0.0141319027048573,0.00630563467572004));
#23762=CARTESIAN_POINT('',(0.0057298627590778,0.0141836340381909,0.00495441855884807));
#23763=CARTESIAN_POINT('',(0.00635627781440241,0.0142094997048577,0.00412011224878849));
#23764=CARTESIAN_POINT('',(0.00722624508306073,0.0142612310381914,0.00227133787544617));
#23765=CARTESIAN_POINT('',(0.00746979729639444,0.0142870967048583,0.00125686981216344));
#23766=CARTESIAN_POINT('',(0.00753397685614792,0.014338828038192,-0.000785357214037403));
#23767=CARTESIAN_POINT('',(0.0073546042025677,0.0143646937048589,-0.00181311617695551));
#23768=CARTESIAN_POINT('',(0.00660243916240275,0.0144164250381928,-0.00371286821128017));
#23769=CARTESIAN_POINT('',(0.00602964677581802,0.0144422907048597,-0.00458486128268673));
#23770=CARTESIAN_POINT('',(0.00458486128979446,0.0144940220381934,-0.00602964678296275));
#23771=CARTESIAN_POINT('',(0.00371286819035562,0.0145198877048603,-0.0066024392118322));
#23772=CARTESIAN_POINT('',(0.00181311619783157,0.014571619038194,-0.00735460415315743));
#23773=CARTESIAN_POINT('',(0.000785357304746346,0.0145974847048609,-0.00753397666561319));
#23774=CARTESIAN_POINT('',(-0.00125686990292393,0.0146492160381944,-0.00746979748692755));
#23775=CARTESIAN_POINT('',(-0.00227133821750898,0.0146750817048612,-0.00722624579578614));
#23776=CARTESIAN_POINT('',(-0.00412011190677149,0.0147268130381946,-0.00635627710165544));
#23777=CARTESIAN_POINT('',(-0.00495441728144896,0.0147526787048613,-0.00572986009866614));
#23778=CARTESIAN_POINT('',(-0.00630563595315176,0.0148044100381945,-0.00419721218396824));
#23779=CARTESIAN_POINT('',(-0.00682254925017708,0.014830275704861,-0.00329098127225964));
#23780=CARTESIAN_POINT('',(-0.00745393250855223,0.0148820070381939,-0.00134772884407215));
#23781=CARTESIAN_POINT('',(-0.00756840246990205,0.0149078727048603,-0.000310707327593257));
#23782=CARTESIAN_POINT('',(-0.00739686159325509,0.0149540330331459,0.00150433068120359));
#23783=CARTESIAN_POINT('',(-0.0071917969991353,0.0149743276947652,0.00229002533780254));
#23784=CARTESIAN_POINT('',(-0.00686919152552402,0.0149946223563844,0.00302395747598018));
#23785=CARTESIAN_POINT('',(-0.00586834142534816,0.0138049000898792,0.002323445101092));
#23786=CARTESIAN_POINT('',(-0.00586834150722695,0.0139610262791494,0.00232344513351016));
#23787=CARTESIAN_POINT('',(-0.00598853868710003,0.0142723828532714,0.00237103465301815));
#23788=CARTESIAN_POINT('',(-0.00642329524186585,0.0144661077682987,0.00254316727348483));
#23789=CARTESIAN_POINT('',(-0.00685805179684844,0.014272382853826,0.00271529989403731));
#23790=CARTESIAN_POINT('',(-0.00697824897705869,0.0139610262798587,0.00276288941367881));
#23791=CARTESIAN_POINT('',(-0.00697824905911604,0.0138049000905885,0.00276288944616767));
#23792=CARTESIAN_POINT('',(-0.00713652355335438,0.00998404077070117,0.0023190372625396));
#23793=CARTESIAN_POINT('',(-0.00682689162296045,0.0101213963498648,0.00327188765430387));
#23794=CARTESIAN_POINT('',(-0.00632393975032057,0.0102552176634611,0.00416165210870539));
#23795=CARTESIAN_POINT('',(-0.00501082465149917,0.0105157917595189,0.00567474585832276));
#23796=CARTESIAN_POINT('',(-0.00420066142531763,0.0106425445419805,0.00629807515353861));
#23797=CARTESIAN_POINT('',(-0.0024014310390604,0.0108889815757688,0.00717946112362713));
#23798=CARTESIAN_POINT('',(-0.00141236387898469,0.0110086658270955,0.0074375177984998));
#23799=CARTESIAN_POINT('',(0.000588110521868161,0.0112409657986143,0.00754754861489316));
#23800=CARTESIAN_POINT('',(0.00159951776264531,0.0113535815188063,0.00739952275641386));
#23801=CARTESIAN_POINT('',(0.00348455427698092,0.0115717444280555,0.00672081082698304));
#23802=CARTESIAN_POINT('',(0.00435818355053937,0.0116772916171128,0.00619012475603152));
#23803=CARTESIAN_POINT('',(0.0058293622098697,0.0118813174640925,0.00483010756411885));
#23804=CARTESIAN_POINT('',(0.00642691159564158,0.0119797961220149,0.00400077644315771));
#23805=CARTESIAN_POINT('',(0.00725133308312823,0.0121696849067251,0.00217475847441996));
#23806=CARTESIAN_POINT('',(0.00747820518484301,0.0122610950335128,0.00117807162664336));
#23807=CARTESIAN_POINT('',(0.00752535639799984,0.0124368467559534,-0.000824873608022594));
#23808=CARTESIAN_POINT('',(0.0073456355094419,0.0125211883516063,-0.00183113199491196));
#23809=CARTESIAN_POINT('',(0.00660805206922664,0.0126828030117774,-0.00369392112405686));
#23810=CARTESIAN_POINT('',(0.00605018951756932,0.0127600760762956,-0.00455045186631239));
#23811=CARTESIAN_POINT('',(0.00464463709803305,0.0129075536741971,-0.00597818967344566));
#23812=CARTESIAN_POINT('',(0.0037969472301541,0.0129777582075804,-0.00654939673832338));
#23813=CARTESIAN_POINT('',(0.00194593676290491,0.0131110987432124,-0.00731606006817175));
#23814=CARTESIAN_POINT('',(0.000942616163534665,0.013174234745461,-0.00751151633314239));
#23815=CARTESIAN_POINT('',(-0.00106082198265159,0.0132934382188234,-0.00749573645991879));
#23816=CARTESIAN_POINT('',(-0.0020609395294676,0.0133495056899372,-0.00728450032172455));
#23817=CARTESIAN_POINT('',(-0.0038996431192263,0.01345457210103,-0.00648877319979548));
#23818=CARTESIAN_POINT('',(-0.00473822916216899,0.0135035710410091,-0.00590428221606065));
#23819=CARTESIAN_POINT('',(-0.00612111958495,0.0135945003898323,-0.0044545861487252));
#23820=CARTESIAN_POINT('',(-0.00666542396478831,0.0136364307986766,-0.00358938106512457));
#23821=CARTESIAN_POINT('',(-0.00737356397402995,0.0137132230852302,-0.00171518552077393));
#23822=CARTESIAN_POINT('',(-0.00753739960343328,0.0137480849629397,-0.000706195060023929));
#23823=CARTESIAN_POINT('',(-0.00745873679850607,0.0138107401872238,0.00129568808368499));
#23824=CARTESIAN_POINT('',(-0.00721623836417553,0.0138385335337985,0.0022885807666439));
#23825=CARTESIAN_POINT('',(-0.00678963471291716,0.0138627926148057,0.00319511544670599));
#23826=CARTESIAN_POINT('',(-0.00713768608282461,0.00996866665836644,0.00231941503038975));
#23827=CARTESIAN_POINT('',(-0.0068280037138325,0.0101060222375301,0.00327242064011874));
#23828=CARTESIAN_POINT('',(-0.00632496991105259,0.0102398435511264,0.00416233003587611));
#23829=CARTESIAN_POINT('',(-0.00501164090766143,0.0105004176471842,0.00567567026629915));
#23830=CARTESIAN_POINT('',(-0.00420134570705017,0.0106271704296457,0.00629910110096484));
#23831=CARTESIAN_POINT('',(-0.00240182222873878,0.010873607463434,0.00718063064756609));
#23832=CARTESIAN_POINT('',(-0.00141259395103865,0.0109932917147608,0.00743872935950167));
#23833=CARTESIAN_POINT('',(0.000588206324230238,0.0112255916862796,0.00754877809975751));
#23834=CARTESIAN_POINT('',(0.00159977832179899,0.0113382074064716,0.00740072812807777));
#23835=CARTESIAN_POINT('',(0.00348512190588417,0.0115563703157208,0.00672190563744528));
#23836=CARTESIAN_POINT('',(0.0043588934924006,0.011661917504778,0.00619113311849253));
#23837=CARTESIAN_POINT('',(0.00583031180462841,0.0118659433517577,0.00483089438172629));
#23838=CARTESIAN_POINT('',(0.00642795853033978,0.0119644220096802,0.0040014281639128));
#23839=CARTESIAN_POINT('',(0.00725251431490651,0.0121543107943904,0.00217511273946207));
#23840=CARTESIAN_POINT('',(0.00747942337376187,0.0122457209211781,0.00117826353282482));
#23841=CARTESIAN_POINT('',(0.00752658226778383,0.0124214726436187,-0.000825007978752457));
#23842=CARTESIAN_POINT('',(0.00734683210295042,0.0125058142392716,-0.00183143028369249));
#23843=CARTESIAN_POINT('',(0.00660912851144867,0.0126674288994427,-0.00369452285851977));
#23844=CARTESIAN_POINT('',(0.00605117508478032,0.0127447019639608,-0.00455119312840702));
#23845=CARTESIAN_POINT('',(0.00464539370276709,0.0128921795618623,-0.00597916351198512));
#23846=CARTESIAN_POINT('',(0.00379756574742221,0.0129623840952457,-0.00655046362567598));
#23847=CARTESIAN_POINT('',(0.00194625375321779,0.0130957246308777,-0.00731725184388323));
#23848=CARTESIAN_POINT('',(0.000942769714358262,0.0131588606331263,-0.00751273994839962));
#23849=CARTESIAN_POINT('',(-0.0010609947890339,0.0132780641064887,-0.00749695750465726));
#23850=CARTESIAN_POINT('',(-0.00206127525356652,0.0133341315776025,-0.00728568695639851));
#23851=CARTESIAN_POINT('',(-0.00390027836550772,0.0134391979886953,-0.00648983021166044));
#23852=CARTESIAN_POINT('',(-0.00473900101291629,0.0134881969286743,-0.00590524401518111));
#23853=CARTESIAN_POINT('',(-0.00612211670656743,0.0135791262774976,-0.00445531179443167));
#23854=CARTESIAN_POINT('',(-0.00666650975281,0.0136210566863418,-0.00358996577016154));
#23855=CARTESIAN_POINT('',(-0.00737476511704538,0.0136978489728955,-0.00171546492203982));
#23856=CARTESIAN_POINT('',(-0.00753862743503819,0.013732710850605,-0.000706310098188223));
#23857=CARTESIAN_POINT('',(-0.00745995181605267,0.0137953660748891,0.00129589914941892));
#23858=CARTESIAN_POINT('',(-0.00721741387907434,0.0138231594214637,0.00228895357317447));
#23859=CARTESIAN_POINT('',(-0.0067907407346919,0.013847418502471,0.00319563592643815));
#23860=CARTESIAN_POINT('',(-0.00713827428147907,0.0099532476683191,0.00231960616751517));
#23861=CARTESIAN_POINT('',(-0.00682856639234631,0.0100906032474828,0.00327269031202572));
#23862=CARTESIAN_POINT('',(-0.00632549113582319,0.010224424561079,0.00416267304296526));
#23863=CARTESIAN_POINT('',(-0.00501205390431109,0.0104849986571369,0.00567613798392852));
#23864=CARTESIAN_POINT('',(-0.00420169192932209,0.0106117514395984,0.00629962019395224));
#23865=CARTESIAN_POINT('',(-0.00240202015683297,0.0108581884733867,0.0071812223851735));
#23866=CARTESIAN_POINT('',(-0.00141271035933283,0.0109778727247134,0.00743934236637103));
#23867=CARTESIAN_POINT('',(0.00058825479682548,0.0112101726962322,0.00754940017546518));
#23868=CARTESIAN_POINT('',(0.00159991015548366,0.0113227884164242,0.00740133800336178));
#23869=CARTESIAN_POINT('',(0.00348540910596441,0.0115409513256735,0.00672245957268501));
#23870=CARTESIAN_POINT('',(0.00435925269778697,0.0116464985147307,0.00619164331411162));
#23871=CARTESIAN_POINT('',(0.00583079226587576,0.0118505243617104,0.00483129248351197));
#23872=CARTESIAN_POINT('',(0.00642848824214198,0.0119490030196329,0.0040017579114857));
#23873=CARTESIAN_POINT('',(0.00725311197626511,0.012138891804343,0.00217529198500073));
#23874=CARTESIAN_POINT('',(0.00748003973412201,0.0122303019311307,0.00117836063054201));
#23875=CARTESIAN_POINT('',(0.00752720251438913,0.0124060536535713,-0.000825075965573031));
#23876=CARTESIAN_POINT('',(0.00734743753679934,0.0124903952492243,-0.00183158120722935));
#23877=CARTESIAN_POINT('',(0.00660967315301072,0.0126520099093953,-0.0036948273148028));
#23878=CARTESIAN_POINT('',(0.00605167374681189,0.0127292829739135,-0.00455156818071995));
#23879=CARTESIAN_POINT('',(0.00464577651791106,0.012876760571815,-0.00597965623972514));
#23880=CARTESIAN_POINT('',(0.00379787869520906,0.0129469651051984,-0.0065510034328132));
#23881=CARTESIAN_POINT('',(0.00194641413906631,0.0130803056408303,-0.00731785484009783));
#23882=CARTESIAN_POINT('',(0.000942847405625574,0.0131434416430789,-0.0075133590542944));
#23883=CARTESIAN_POINT('',(-0.00106108222293055,0.0132626451164413,-0.00749757530996077));
#23884=CARTESIAN_POINT('',(-0.00206144511804593,0.0133187125875551,-0.00728628735143058));
#23885=CARTESIAN_POINT('',(-0.00390059977758161,0.013423778998648,-0.00649036502215139));
#23886=CARTESIAN_POINT('',(-0.0047393915420019,0.013472777938627,-0.00590573065140239));
#23887=CARTESIAN_POINT('',(-0.0061226212147186,0.0135637072874502,-0.0044556789454064));
#23888=CARTESIAN_POINT('',(-0.006667059123015,0.0136056376962945,-0.00359026161015942));
#23889=CARTESIAN_POINT('',(-0.00737537285278333,0.0136824299828482,-0.00171560628916457));
#23890=CARTESIAN_POINT('',(-0.00753924867425526,0.0137172918605576,-0.000706368303416719));
#23891=CARTESIAN_POINT('',(-0.00746056657181099,0.0137799470848417,0.00129600594118969));
#23892=CARTESIAN_POINT('',(-0.0072180086478948,0.0138077404314164,0.00228914220004825));
#23893=CARTESIAN_POINT('',(-0.00679130034245786,0.0138319995124236,0.0031958992707111));
#23894=CARTESIAN_POINT('',(-0.00713827428147907,0.00981292768344121,0.00231960616751517));
#23895=CARTESIAN_POINT('',(-0.0068285663923463,0.00995028326260487,0.00327269031202572));
#23896=CARTESIAN_POINT('',(-0.00632549113582319,0.0100841045762011,0.00416267304296526));
#23897=CARTESIAN_POINT('',(-0.00501205390431109,0.0103446786722589,0.00567613798392853));
#23898=CARTESIAN_POINT('',(-0.0042016919293221,0.0104714314547205,0.00629962019395224));
#23899=CARTESIAN_POINT('',(-0.00240202015683296,0.0107178684885088,0.0071812223851735));
#23900=CARTESIAN_POINT('',(-0.00141271035933283,0.0108375527398355,0.00743934236637104));
#23901=CARTESIAN_POINT('',(0.000588254796825484,0.0110698527113543,0.00754940017546518));
#23902=CARTESIAN_POINT('',(0.00159991015548366,0.0111824684315463,0.00740133800336179));
#23903=CARTESIAN_POINT('',(0.00348540910596441,0.0114006313407956,0.00672245957268501));
#23904=CARTESIAN_POINT('',(0.00435925269778698,0.0115061785298528,0.00619164331411163));
#23905=CARTESIAN_POINT('',(0.00583079226587577,0.0117102043768325,0.00483129248351197));
#23906=CARTESIAN_POINT('',(0.00642848824214199,0.011808683034755,0.00400175791148571));
#23907=CARTESIAN_POINT('',(0.00725311197626511,0.0119985718194651,0.00217529198500072));
#23908=CARTESIAN_POINT('',(0.00748003973412199,0.0120899819462528,0.001178360630542));
#23909=CARTESIAN_POINT('',(0.00752720251438914,0.0122657336686934,-0.000825075965573036));
#23910=CARTESIAN_POINT('',(0.00734743753679934,0.0123500752643464,-0.00183158120722935));
#23911=CARTESIAN_POINT('',(0.00660967315301072,0.0125116899245174,-0.0036948273148028));
#23912=CARTESIAN_POINT('',(0.00605167374681189,0.0125889629890356,-0.00455156818071994));
#23913=CARTESIAN_POINT('',(0.00464577651791106,0.0127364405869371,-0.00597965623972514));
#23914=CARTESIAN_POINT('',(0.00379787869520905,0.0128066451203205,-0.00655100343281321));
#23915=CARTESIAN_POINT('',(0.00194641413906632,0.0129399856559524,-0.00731785484009784));
#23916=CARTESIAN_POINT('',(0.000942847405625574,0.013003121658201,-0.00751335905429439));
#23917=CARTESIAN_POINT('',(-0.00106108222293055,0.0131223251315634,-0.00749757530996077));
#23918=CARTESIAN_POINT('',(-0.00206144511804593,0.0131783926026772,-0.00728628735143058));
#23919=CARTESIAN_POINT('',(-0.0039005997775816,0.01328345901377,-0.00649036502215138));
#23920=CARTESIAN_POINT('',(-0.0047393915420019,0.0133324579537491,-0.00590573065140239));
#23921=CARTESIAN_POINT('',(-0.00612262121471859,0.0134233873025723,-0.00445567894540641));
#23922=CARTESIAN_POINT('',(-0.006667059123015,0.0134653177114166,-0.00359026161015941));
#23923=CARTESIAN_POINT('',(-0.00737537285278332,0.0135421099979703,-0.00171560628916458));
#23924=CARTESIAN_POINT('',(-0.00753924867425525,0.0135769718756797,-0.000706368303416716));
#23925=CARTESIAN_POINT('',(-0.007460566571811,0.0136396270999638,0.0012960059411897));
#23926=CARTESIAN_POINT('',(-0.0072180086478948,0.0136674204465385,0.00228914220004825));
#23927=CARTESIAN_POINT('',(-0.00679130034245786,0.0136916795275457,0.0031958992707111));
#23928=CARTESIAN_POINT('',(-0.00709967813326097,0.00968802668861064,0.00230706421971116));
#23929=CARTESIAN_POINT('',(-0.00679164481295561,0.00982538226777431,0.00325499510512079));
#23930=CARTESIAN_POINT('',(-0.00629128964904872,0.0099592035813706,0.00414016576187539));
#23931=CARTESIAN_POINT('',(-0.00498495408049655,0.0102197776774284,0.00564544750408768));
#23932=CARTESIAN_POINT('',(-0.00417897367585126,0.0103465304598899,0.00626555858954536));
#23933=CARTESIAN_POINT('',(-0.00238903260237088,0.0105929674936782,0.00714239401957196));
#23934=CARTESIAN_POINT('',(-0.00140507193353578,0.010712651745005,0.00739911836414088));
#23935=CARTESIAN_POINT('',(0.00058507414441105,0.0109449517165238,0.00750858109838291));
#23936=CARTESIAN_POINT('',(0.00159125955352277,0.0110575674367158,0.00736131948805603));
#23937=CARTESIAN_POINT('',(0.00346656374346502,0.011275730345965,0.00668611170542376));
#23938=CARTESIAN_POINT('',(0.00433568252429554,0.0113812775350222,0.00615816553311837));
#23939=CARTESIAN_POINT('',(0.00579926558118299,0.0115853033820019,0.00480517002401746));
#23940=CARTESIAN_POINT('',(0.00639372985723993,0.0116837820399244,0.00398012068722193));
#23941=CARTESIAN_POINT('',(0.00721389490868832,0.0118736708246346,0.00216353033385647));
#23942=CARTESIAN_POINT('',(0.00743959568407976,0.0119650809514223,0.00117198931728653));
#23943=CARTESIAN_POINT('',(0.00748650345850291,0.0121408326738629,-0.00082061483771457));
#23944=CARTESIAN_POINT('',(0.00730771045753463,0.0122251742695158,-0.00182167797614574));
#23945=CARTESIAN_POINT('',(0.00657393511400755,0.0123867889296869,-0.00367484964274103));
#23946=CARTESIAN_POINT('',(0.00601895277144875,0.012464061994205,-0.00452695817090515));
#23947=CARTESIAN_POINT('',(0.00462065713022673,0.0126115395921065,-0.00594732465797007));
#23948=CARTESIAN_POINT('',(0.00377734383156351,0.0126817441254899,-0.00651558261687086));
#23949=CARTESIAN_POINT('',(0.00193589001437694,0.0128150846611219,-0.00727828771239866));
#23950=CARTESIAN_POINT('',(0.0009377494958536,0.0128782206633705,-0.00747273484902566));
#23951=CARTESIAN_POINT('',(-0.00105534502579677,0.0129974241367329,-0.00745703644629026));
#23952=CARTESIAN_POINT('',(-0.0020502990289238,0.0130534916078467,-0.00724689090692786));
#23953=CARTESIAN_POINT('',(-0.00387950950825059,0.0131585580189395,-0.0064552720738411));
#23954=CARTESIAN_POINT('',(-0.00471376598445036,0.0132075569589185,-0.00587379878011675));
#23955=CARTESIAN_POINT('',(-0.00608951663137417,0.0132984863077418,-0.00443158740195935));
#23956=CARTESIAN_POINT('',(-0.00663101080209822,0.013340416716586,-0.0035708493175263));
#23957=CARTESIAN_POINT('',(-0.00733549472922503,0.0134172090031397,-0.00170633012632612));
#23958=CARTESIAN_POINT('',(-0.0074984844856278,0.0134520708808492,-0.000702549019558996));
#23959=CARTESIAN_POINT('',(-0.00742022781179112,0.0135147261051333,0.00128899852799355));
#23960=CARTESIAN_POINT('',(-0.00717898138155166,0.0135425194517079,0.00227676496877898));
#23961=CARTESIAN_POINT('',(-0.00675458025798432,0.0135667785327152,0.00317861926757889));
#23962=CARTESIAN_POINT('',(-0.00696003595717303,0.00948593263374612,0.00226168702627111));
#23963=CARTESIAN_POINT('',(-0.00665806128380176,0.00962328821290979,0.00319097324510079));
#23964=CARTESIAN_POINT('',(-0.00616754750743291,0.00975710952650608,0.00405873365389791));
#23965=CARTESIAN_POINT('',(-0.00488690599684642,0.0100176836225639,0.00553440830489247));
#23966=CARTESIAN_POINT('',(-0.00409677826262877,0.0101444364050254,0.00614232254708991));
#23967=CARTESIAN_POINT('',(-0.00234204318889632,0.0103908734388137,0.00700191167309798));
#23968=CARTESIAN_POINT('',(-0.00137743584938151,0.0105105576901405,0.00725358655690861));
#23969=CARTESIAN_POINT('',(0.000573566435869221,0.0107428576616592,0.00736089629010987));
#23970=CARTESIAN_POINT('',(0.00155996138160514,0.0108554733818512,0.0072165311395005));
#23971=CARTESIAN_POINT('',(0.00339838058141192,0.0110736362911005,0.006554603886254));
#23972=CARTESIAN_POINT('',(0.00425040483548277,0.0111791834801577,0.00603704178361687));
#23973=CARTESIAN_POINT('',(0.00568520096441194,0.0113832093271374,0.00471065807769657));
#23974=CARTESIAN_POINT('',(0.00626797283927026,0.0114816879850599,0.0039018364744134));
#23975=CARTESIAN_POINT('',(0.00707200622525638,0.01167157676977,0.00212097628025275));
#23976=CARTESIAN_POINT('',(0.00729326773638417,0.0117629868965577,0.00114893768937527));
#23977=CARTESIAN_POINT('',(0.00733925289099655,0.0119387386189984,-0.000804474325494489));
#23978=CARTESIAN_POINT('',(0.00716397653448113,0.0120230802146513,-0.00178584774948676));
#23979=CARTESIAN_POINT('',(0.0064446336742028,0.0121846948748224,-0.00360256974620541));
#23980=CARTESIAN_POINT('',(0.00590056717043989,0.0122619679393405,-0.00443791831893177));
#23981=CARTESIAN_POINT('',(0.00452977433180828,0.012409445537242,-0.00583034789627018));
#23982=CARTESIAN_POINT('',(0.00370304799693959,0.0124796500706254,-0.00638742890088223));
#23983=CARTESIAN_POINT('',(0.00189781337354895,0.0126129906062573,-0.00713513249954584));
#23984=CARTESIAN_POINT('',(0.000919305085027019,0.0126761266085059,-0.00732575509359739));
#23985=CARTESIAN_POINT('',(-0.0010345876515666,0.0127953300818683,-0.00731036545966501));
#23986=CARTESIAN_POINT('',(-0.00200997209963829,0.0128513975529821,-0.00710435323168109));
#23987=CARTESIAN_POINT('',(-0.00380320419697909,0.012956463964075,-0.00632830459408905));
#23988=CARTESIAN_POINT('',(-0.00462105184624821,0.013005462904054,-0.00575826818448094));
#23989=CARTESIAN_POINT('',(-0.00596974312365063,0.0130963922528773,-0.00434442337892649));
#23990=CARTESIAN_POINT('',(-0.00650058675178394,0.0131383226617215,-0.00350061498298014));
#23991=CARTESIAN_POINT('',(-0.00719121432278355,0.0132151149482752,-0.00167276865389143));
#23992=CARTESIAN_POINT('',(-0.00735099826564986,0.0132499768259846,-0.000688730720749077));
#23993=CARTESIAN_POINT('',(-0.00727428080697516,0.0133126320502687,0.0012636454688767));
#23994=CARTESIAN_POINT('',(-0.00703777940543416,0.0133404253968434,0.00223198372536013));
#23995=CARTESIAN_POINT('',(-0.00662172574428931,0.0133646844778507,0.00311609962892087));
#23996=CARTESIAN_POINT('',(-0.0068589899293032,0.00940873957371216,0.00222885178063507));
#23997=CARTESIAN_POINT('',(-0.00656139933403859,0.00954609515287583,0.00314464659198573));
#23998=CARTESIAN_POINT('',(-0.00607800685259157,0.00967991646647212,0.0039998088270103));
#23999=CARTESIAN_POINT('',(-0.00481595773701083,0.00994049056252993,0.0054540595855381));
#24000=CARTESIAN_POINT('',(-0.00403730110287711,0.0100672433449915,0.00605314810904134));
#24001=CARTESIAN_POINT('',(-0.00230804132988384,0.0103136803787797,0.00690025769222555));
#24002=CARTESIAN_POINT('',(-0.00135743819102429,0.0104333646301065,0.00714827875190651));
#24003=CARTESIAN_POINT('',(0.000565239379741828,0.0106656646016253,0.0072540305589191));
#24004=CARTESIAN_POINT('',(0.00153731381164839,0.0107782803218173,0.00711176130625072));
#24005=CARTESIAN_POINT('',(0.00334904278185819,0.0109964432310665,0.00645944393434548));
#24006=CARTESIAN_POINT('',(0.00418869732016143,0.0111019904201238,0.00594939581510862));
#24007=CARTESIAN_POINT('',(0.00560266303233365,0.0113060162671035,0.0046422685908702));
#24008=CARTESIAN_POINT('',(0.00617697420620263,0.0114044949250259,0.00384518948586864));
#24009=CARTESIAN_POINT('',(0.00696933460940123,0.0115943837097361,0.00209018387779328));
#24010=CARTESIAN_POINT('',(0.00718738383873084,0.0116857938365238,0.00113225737471947));
#24011=CARTESIAN_POINT('',(0.0072327013793764,0.0118615455589644,-0.000792794941132875));
#24012=CARTESIAN_POINT('',(0.00705996969069235,0.0119458871546173,-0.00175992075391141));
#24013=CARTESIAN_POINT('',(0.00635107027340123,0.0121075018147884,-0.00355026752173156));
#24014=CARTESIAN_POINT('',(0.00581490254479415,0.0121847748793065,-0.00437348847677317));
#24015=CARTESIAN_POINT('',(0.00446401092107414,0.0123322524772081,-0.00574570271632536));
#24016=CARTESIAN_POINT('',(0.00364928702596121,0.0124024570105914,-0.00629469600083595));
#24017=CARTESIAN_POINT('',(0.00187026085741034,0.0125357975462234,-0.0070315444143922));
#24018=CARTESIAN_POINT('',(0.000905958583972412,0.012598933548472,-0.00721939954343787));
#24019=CARTESIAN_POINT('',(-0.00101956747447022,0.0127181370218344,-0.00720423333671029));
#24020=CARTESIAN_POINT('',(-0.00198079125947491,0.0127742044929482,-0.00700121200093706));
#24021=CARTESIAN_POINT('',(-0.0037479891550386,0.012879270904041,-0.00623643006264729));
#24022=CARTESIAN_POINT('',(-0.0045539632655976,0.01292826984402,-0.00567466946013077));
#24023=CARTESIAN_POINT('',(-0.00588307419927152,0.0130191991928433,-0.00428135089934067));
#24024=CARTESIAN_POINT('',(-0.00640621102238644,0.0130611296016875,-0.0034497929410671));
#24025=CARTESIAN_POINT('',(-0.00708681203990037,0.0131379218882412,-0.0016484833442952));
#24026=CARTESIAN_POINT('',(-0.00724427623429937,0.0131727837659507,-0.000678731705796877));
#24027=CARTESIAN_POINT('',(-0.00716867256217909,0.0132354389902348,0.00124529982295599));
#24028=CARTESIAN_POINT('',(-0.0069356046956598,0.0132632323368094,0.00219957971321054));
#24029=CARTESIAN_POINT('',(-0.00652559131506782,0.0132874914178167,0.00307085999339506));
#24030=CARTESIAN_POINT('',(-0.00663304414212992,0.0093315465136782,0.00215542993933499));
#24031=CARTESIAN_POINT('',(-0.00634525664353049,0.00946890209284187,0.00304105704645039));
#24032=CARTESIAN_POINT('',(-0.00587778786161648,0.00960272340643816,0.00386804890852719));
#24033=CARTESIAN_POINT('',(-0.00465731260513313,0.00986329750249597,0.00527439438715669));
#24034=CARTESIAN_POINT('',(-0.00390430613056378,0.0099900502849575,0.0058537480037094));
#24035=CARTESIAN_POINT('',(-0.00223201086177059,0.0102364873187458,0.00667295248081131));
#24036=CARTESIAN_POINT('',(-0.00131272206754674,0.0103561715700725,0.00691280334136051));
#24037=CARTESIAN_POINT('',(0.000546619516188517,0.0105884715415913,0.00701507151951131));
#24038=CARTESIAN_POINT('',(0.00148667230569993,0.0107010872617833,0.00687748883711291));
#24039=CARTESIAN_POINT('',(0.00323872010819583,0.0109192501710326,0.00624665981314244));
#24040=CARTESIAN_POINT('',(0.00405071512118033,0.0110247973600898,0.00575341347157038));
#24041=CARTESIAN_POINT('',(0.00541810260548434,0.0112288232070695,0.00448934504938012));
#24042=CARTESIAN_POINT('',(0.00597349507680387,0.011327301864992,0.00371852296876192));
#24043=CARTESIAN_POINT('',(0.00673975389698938,0.0115171906497021,0.00202132997270337));
#24044=CARTESIAN_POINT('',(0.00695062024585536,0.0116086007764898,0.00109495905726303));
#24045=CARTESIAN_POINT('',(0.0069944449562884,0.0117843524989304,-0.000766679043764952));
#24046=CARTESIAN_POINT('',(0.00682740331785544,0.0118686940945834,-0.00170194622935258));
#24047=CARTESIAN_POINT('',(0.00614185614900286,0.0120303087547544,-0.00343331619243359));
#24048=CARTESIAN_POINT('',(0.00562335061858323,0.0121075818192726,-0.00422941896992696));
#24049=CARTESIAN_POINT('',(0.00431695946424038,0.0122550594171741,-0.00555643034000104));
#24050=CARTESIAN_POINT('',(0.00352907384031716,0.0123252639505575,-0.00608733893258175));
#24051=CARTESIAN_POINT('',(0.00180865155837324,0.0124586044861894,-0.00679991441432962));
#24052=CARTESIAN_POINT('',(0.000876114900352539,0.012521740488438,-0.00698158130349679));
#24053=CARTESIAN_POINT('',(-0.0009859813374486,0.0126409439618004,-0.00696691469518718));
#24054=CARTESIAN_POINT('',(-0.00191554091722904,0.0126970114329142,-0.0067705811977104));
#24055=CARTESIAN_POINT('',(-0.00362452456787917,0.0128020778440071,-0.00603099236494257));
#24056=CARTESIAN_POINT('',(-0.00440394863874887,0.0128510767839861,-0.00548773702965151));
#24057=CARTESIAN_POINT('',(-0.00568927659282304,0.0129420061328093,-0.00414031654747732));
#24058=CARTESIAN_POINT('',(-0.00619518047602752,0.0129839365416536,-0.00333615140059418));
#24059=CARTESIAN_POINT('',(-0.00685336143836741,0.0130607288282073,-0.00159417974118338));
#24060=CARTESIAN_POINT('',(-0.00700563851750282,0.0130955907059167,-0.000656373228655722));
#24061=CARTESIAN_POINT('',(-0.00693252534783064,0.0131582459302008,0.00120427771158615));
#24062=CARTESIAN_POINT('',(-0.00670713509902304,0.0131860392767755,0.00212712213930035));
#24063=CARTESIAN_POINT('',(-0.00631062819635045,0.0132102983577827,0.00296970109308201));
#24064=CARTESIAN_POINT('',(-0.00650814438282647,0.0093315465136782,0.00211484334367094));
#24065=CARTESIAN_POINT('',(-0.00622577590278555,0.00946890209284187,0.00298379415403012));
#24066=CARTESIAN_POINT('',(-0.00576710952548273,0.00960272340643816,0.00379521381693169));
#24067=CARTESIAN_POINT('',(-0.00456961573309102,0.00986329750249597,0.00517507790812964));
#24068=CARTESIAN_POINT('',(-0.00383078831800211,0.0099900502849575,0.00574352233642602));
#24069=CARTESIAN_POINT('',(-0.0021899822526698,0.0102364873187458,0.00654730125026951));
#24070=CARTESIAN_POINT('',(-0.00128800360242641,0.0103561715700726,0.00678263573581662));
#24071=CARTESIAN_POINT('',(0.000536326708762601,0.0105884715415913,0.0068829782112943));
#24072=CARTESIAN_POINT('',(0.0014586783697082,0.0107010872617833,0.00674798620122487));
#24073=CARTESIAN_POINT('',(0.00317773523408718,0.0109192501710326,0.00612903564384791));
#24074=CARTESIAN_POINT('',(0.00397444043752055,0.0110247973600898,0.00564507709654038));
#24075=CARTESIAN_POINT('',(0.00531608011071332,0.0112288232070695,0.00440481099471639));
#24076=CARTESIAN_POINT('',(0.00586101458047273,0.011327301864992,0.00364850344019995));
#24077=CARTESIAN_POINT('',(0.00661284480043267,0.0115171906497021,0.00198326847007294));
#24078=CARTESIAN_POINT('',(0.00681974055063321,0.0116086007764898,0.00107434105446238));
#24079=CARTESIAN_POINT('',(0.00686274004482053,0.0117843524989304,-0.000752242530758643));
#24080=CARTESIAN_POINT('',(0.00669884378880731,0.0118686940945834,-0.00166989870036911));
#24081=CARTESIAN_POINT('',(0.00602620542540606,0.0120303087547544,-0.00336866708760947));
#24082=CARTESIAN_POINT('',(0.00551746331801803,0.0121075818192726,-0.00414977930523935));
#24083=CARTESIAN_POINT('',(0.00423567141814074,0.0122550594171741,-0.00545180314362154));
#24084=CARTESIAN_POINT('',(0.00346262162565148,0.0123252639505575,-0.00597271476437384));
#24085=CARTESIAN_POINT('',(0.00177459477547475,0.0124586044861894,-0.00667187249942069));
#24086=CARTESIAN_POINT('',(0.000859617717787273,0.012521740488438,-0.00685011861371523));
#24087=CARTESIAN_POINT('',(-0.000967415377523374,0.0126409439618004,-0.00683572817661878));
#24088=CARTESIAN_POINT('',(-0.00187947141514655,0.0126970114329142,-0.00664309162522779));
#24089=CARTESIAN_POINT('',(-0.00355627502266023,0.0128020778440071,-0.00591742919867961));
#24090=CARTESIAN_POINT('',(-0.00432102259255074,0.0128510767839861,-0.00538440332352243));
#24091=CARTESIAN_POINT('',(-0.00558214791075367,0.0129420061328093,-0.00406235467519978));
#24092=CARTESIAN_POINT('',(-0.00607852565906608,0.0129839365416536,-0.00327333190203431));
#24093=CARTESIAN_POINT('',(-0.00672431311971763,0.0130607288282073,-0.00156416144766781));
#24094=CARTESIAN_POINT('',(-0.00687372283205676,0.0130955907059167,-0.000644013766466766));
#24095=CARTESIAN_POINT('',(-0.00680198637827826,0.0131582459302008,0.00118160124613701));
#24096=CARTESIAN_POINT('',(-0.00658084021216063,0.0131860392767755,0.00208706857753974));
#24097=CARTESIAN_POINT('',(-0.00619179950685455,0.0132102983577827,0.00291378182829478));
#24098=CARTESIAN_POINT('',(-0.0062821985956532,0.00940873957371216,0.00204142150237086));
#24099=CARTESIAN_POINT('',(-0.00600963321227745,0.00954609515287583,0.00288020460849478));
#24100=CARTESIAN_POINT('',(-0.00556689053450765,0.00967991646647212,0.00366345389844858));
#24101=CARTESIAN_POINT('',(-0.00441097060121332,0.00994049056252993,0.00499541270974823));
#24102=CARTESIAN_POINT('',(-0.00369779334568878,0.0100672433449915,0.00554412223109408));
#24103=CARTESIAN_POINT('',(-0.00211395178455655,0.0103136803787797,0.00631999603885527));
#24104=CARTESIAN_POINT('',(-0.00124328747894885,0.0104333646301065,0.00654716032527062));
#24105=CARTESIAN_POINT('',(0.000517706845209291,0.0106656646016253,0.00664401917188651));
#24106=CARTESIAN_POINT('',(0.00140803686375974,0.0107782803218173,0.00651371373208705));
#24107=CARTESIAN_POINT('',(0.00306741256042481,0.0109964432310665,0.00591625152264486));
#24108=CARTESIAN_POINT('',(0.00383645823853945,0.0111019904201238,0.00544909475300212));
#24109=CARTESIAN_POINT('',(0.00513151968386402,0.0113060162671035,0.0042518874532263));
#24110=CARTESIAN_POINT('',(0.00565753545107397,0.0114044949250259,0.00352183692309322));
#24111=CARTESIAN_POINT('',(0.00638326408802082,0.0115943837097361,0.00191441456498304));
#24112=CARTESIAN_POINT('',(0.00658297695775774,0.0116857938365238,0.00103704273700594));
#24113=CARTESIAN_POINT('',(0.00662448362173252,0.0118615455589644,-0.000726126633390719));
#24114=CARTESIAN_POINT('',(0.00646627741597039,0.0119458871546173,-0.00161192417581028));
#24115=CARTESIAN_POINT('',(0.00581699130100768,0.0121075018147884,-0.0032517157583115));
#24116=CARTESIAN_POINT('',(0.0053259113918071,0.0121847748793065,-0.00400570979839314));
#24117=CARTESIAN_POINT('',(0.00408861996130697,0.0123322524772081,-0.00526253076729722));
#24118=CARTESIAN_POINT('',(0.00334240844000743,0.0124024570105914,-0.00576535769611964));
#24119=CARTESIAN_POINT('',(0.00171298547643764,0.0125357975462234,-0.00644024249935811));
#24120=CARTESIAN_POINT('',(0.000829774034167402,0.012598933548472,-0.00661230037377415));
#24121=CARTESIAN_POINT('',(-0.000933829240501756,0.0127181370218344,-0.00659840953509566));
#24122=CARTESIAN_POINT('',(-0.00181422107290067,0.0127742044929482,-0.00641246082200114));
#24123=CARTESIAN_POINT('',(-0.0034328104355008,0.012879270904041,-0.00571199150097489));
#24124=CARTESIAN_POINT('',(-0.004171007965702,0.01292826984402,-0.00519747089304317));
#24125=CARTESIAN_POINT('',(-0.00538835030430518,0.0130191991928433,-0.00392132032333643));
#24126=CARTESIAN_POINT('',(-0.00586749511270716,0.0130611296016875,-0.0031596903615614));
#24127=CARTESIAN_POINT('',(-0.00649086251818467,0.0131379218882412,-0.00150985784455599));
#24128=CARTESIAN_POINT('',(-0.00663508511526021,0.0131727837659507,-0.000621655289325611));
#24129=CARTESIAN_POINT('',(-0.00656583916392981,0.0132354389902348,0.00114057913476716));
#24130=CARTESIAN_POINT('',(-0.00635237061552386,0.0132632323368094,0.00201461100362955));
#24131=CARTESIAN_POINT('',(-0.00597683638813717,0.0132874914178167,0.00281262292798174));
#24132=CARTESIAN_POINT('',(-0.00618115256778337,0.00948593263374612,0.00200858625673482));
#24133=CARTESIAN_POINT('',(-0.00591297126251429,0.00962328821290979,0.00283387795537971));
#24134=CARTESIAN_POINT('',(-0.0054773498796663,0.00975710952650608,0.00360452907156096));
#24135=CARTESIAN_POINT('',(-0.00434002234137772,0.0100176836225639,0.00491506399039386));
#24136=CARTESIAN_POINT('',(-0.00363831618593712,0.0101444364050254,0.00545494779304551));
#24137=CARTESIAN_POINT('',(-0.00207994992554408,0.0103908734388137,0.00621834205798284));
#24138=CARTESIAN_POINT('',(-0.00122328982059163,0.0105105576901405,0.00644185252026851));
#24139=CARTESIAN_POINT('',(0.000509379789081899,0.0107428576616592,0.00653715344069573));
#24140=CARTESIAN_POINT('',(0.00138538929380299,0.0108554733818512,0.00640894389883727));
#24141=CARTESIAN_POINT('',(0.0030180747608711,0.0110736362911005,0.00582109157073635));
#24142=CARTESIAN_POINT('',(0.00377475072321812,0.0111791834801577,0.00536144878449388));
#24143=CARTESIAN_POINT('',(0.00504898175178574,0.0113832093271374,0.00418349796639994));
#24144=CARTESIAN_POINT('',(0.00556653681800634,0.0114816879850599,0.00346518993454846));
#24145=CARTESIAN_POINT('',(0.00628059247216568,0.01167157676977,0.00188362216252356));
#24146=CARTESIAN_POINT('',(0.00647709306010441,0.0117629868965577,0.00102036242235014));
#24147=CARTESIAN_POINT('',(0.00651793211011238,0.0119387386189984,-0.000714447249029104));
#24148=CARTESIAN_POINT('',(0.00636227057218162,0.0120230802146513,-0.00158599718023493));
#24149=CARTESIAN_POINT('',(0.00572342790020611,0.0121846948748224,-0.00319941353383765));
#24150=CARTESIAN_POINT('',(0.00524024676616137,0.0122619679393405,-0.00394127995623455));
#24151=CARTESIAN_POINT('',(0.00402285655057284,0.012409445537242,-0.0051778855873524));
#24152=CARTESIAN_POINT('',(0.00328864746902905,0.0124796500706254,-0.00567262479607335));
#24153=CARTESIAN_POINT('',(0.00168543296029903,0.0126129906062574,-0.00633665441420447));
#24154=CARTESIAN_POINT('',(0.000816427533112798,0.0126761266085059,-0.00650594482361463));
#24155=CARTESIAN_POINT('',(-0.000918809063405365,0.0127953300818683,-0.00649227741214095));
#24156=CARTESIAN_POINT('',(-0.0017850402327373,0.0128513975529821,-0.0063093195912571));
#24157=CARTESIAN_POINT('',(-0.00337759539356031,0.012956463964075,-0.00562011696953312));
#24158=CARTESIAN_POINT('',(-0.0041039193850514,0.013005462904054,-0.005113872168693));
#24159=CARTESIAN_POINT('',(-0.00530168137992607,0.0130963922528773,-0.00385824784375061));
#24160=CARTESIAN_POINT('',(-0.00577311938330966,0.0131383226617215,-0.00310886831964835));
#24161=CARTESIAN_POINT('',(-0.00638646023530149,0.0132151149482752,-0.00148557253495975));
#24162=CARTESIAN_POINT('',(-0.00652836308390973,0.0132499768259846,-0.000611656274373411));
#24163=CARTESIAN_POINT('',(-0.00646023091913374,0.0133126320502687,0.00112223348884645));
#24164=CARTESIAN_POINT('',(-0.00625019590574951,0.0133404253968434,0.00198220699147998));
#24165=CARTESIAN_POINT('',(-0.00588070195891569,0.0133646844778507,0.00276738329245591));
#24166=CARTESIAN_POINT('',(-0.00604151039169543,0.00968802668861064,0.00196320906329477));
#24167=CARTESIAN_POINT('',(-0.00577938773336043,0.00982538226777431,0.00276985609535972));
#24168=CARTESIAN_POINT('',(-0.00535360773805049,0.0099592035813706,0.00352309696358349));
#24169=CARTESIAN_POINT('',(-0.00424197425772759,0.0102197776774284,0.00480402479119866));
#24170=CARTESIAN_POINT('',(-0.00355612077271463,0.0103465304598899,0.00533171175059006));
#24171=CARTESIAN_POINT('',(-0.00203296051206952,0.0105929674936782,0.00607785971150886));
#24172=CARTESIAN_POINT('',(-0.00119565373643737,0.010712651745005,0.00629632071303625));
#24173=CARTESIAN_POINT('',(0.000497872080540071,0.0109449517165238,0.0063894686324227));
#24174=CARTESIAN_POINT('',(0.00135409112188536,0.0110575674367158,0.00626415555028175));
#24175=CARTESIAN_POINT('',(0.00294989159881799,0.011275730345965,0.00568958375156659));
#24176=CARTESIAN_POINT('',(0.00368947303440534,0.0113812775350222,0.00524032503499238));
#24177=CARTESIAN_POINT('',(0.00493491713501468,0.0115853033820019,0.00408898602007905));
#24178=CARTESIAN_POINT('',(0.00544077980003666,0.0116837820399244,0.00338690572173993));
#24179=CARTESIAN_POINT('',(0.00613870378873374,0.0118736708246346,0.00184106810891984));
#24180=CARTESIAN_POINT('',(0.00633076511240882,0.0119650809514223,0.000997310794438875));
#24181=CARTESIAN_POINT('',(0.00637068154260601,0.0121408326738629,-0.000698306736809027));
#24182=CARTESIAN_POINT('',(0.00621853664912812,0.0122251742695158,-0.00155016695357596));
#24183=CARTESIAN_POINT('',(0.00559412646040137,0.0123867889296869,-0.00312713363730202));
#24184=CARTESIAN_POINT('',(0.0051218611651525,0.012464061994205,-0.00385224010426115));
#24185=CARTESIAN_POINT('',(0.00393197375215438,0.0126115395921065,-0.00506090882565251));
#24186=CARTESIAN_POINT('',(0.00321435163440513,0.0126817441254899,-0.00554447108008473));
#24187=CARTESIAN_POINT('',(0.00164735631947105,0.0128150846611219,-0.00619349920135166));
#24188=CARTESIAN_POINT('',(0.000797983122286219,0.0128782206633705,-0.00635896506818636));
#24189=CARTESIAN_POINT('',(-0.000898051689175195,0.0129974241367329,-0.0063456064255157));
#24190=CARTESIAN_POINT('',(-0.00174471330345178,0.0130534916078467,-0.00616678191601033));
#24191=CARTESIAN_POINT('',(-0.0033012900822888,0.0131585580189395,-0.00549314948978108));
#24192=CARTESIAN_POINT('',(-0.00401120524684925,0.0132075569589185,-0.00499834157305719));
#24193=CARTESIAN_POINT('',(-0.00518190787220253,0.0132984863077418,-0.00377108382071775));
#24194=CARTESIAN_POINT('',(-0.00564269533299538,0.013340416716586,-0.0030386339851022));
#24195=CARTESIAN_POINT('',(-0.00624217982886001,0.0134172090031397,-0.00145201106252507));
#24196=CARTESIAN_POINT('',(-0.00638087686393179,0.0134520708808492,-0.000597837975563491));
#24197=CARTESIAN_POINT('',(-0.00631428391431779,0.0135147261051333,0.0010968804297296));
#24198=CARTESIAN_POINT('',(-0.00610899392963201,0.0135425194517079,0.00193742574806112));
#24199=CARTESIAN_POINT('',(-0.00574784744522067,0.0135667785327152,0.00270486365379789));
#24200=CARTESIAN_POINT('',(-0.00600291424347733,0.0098129276834412,0.00195066711549076));
#24201=CARTESIAN_POINT('',(-0.00574246615396974,0.00995028326260487,0.00275216088845479));
#24202=CARTESIAN_POINT('',(-0.00531940625127602,0.0100841045762011,0.00350058968249363));
#24203=CARTESIAN_POINT('',(-0.00421487443391305,0.010344678672259,0.00477333431135782));
#24204=CARTESIAN_POINT('',(-0.0035334025192438,0.0104714314547205,0.00529765014618318));
#24205=CARTESIAN_POINT('',(-0.00201997295760744,0.0107178684885088,0.00603903134590732));
#24206=CARTESIAN_POINT('',(-0.00118801531064032,0.0108375527398356,0.0062560967108061));
#24207=CARTESIAN_POINT('',(0.000494691428125636,0.0110698527113543,0.00634864955534044));
#24208=CARTESIAN_POINT('',(0.00134544051992447,0.0111824684315463,0.006224137034976));
#24209=CARTESIAN_POINT('',(0.00293104623631861,0.0114006313407956,0.00565323588430534));
#24210=CARTESIAN_POINT('',(0.0036659028609139,0.0115061785298528,0.00520684725399912));
#24211=CARTESIAN_POINT('',(0.0049033904503219,0.0117102043768325,0.00406286356058453));
#24212=CARTESIAN_POINT('',(0.00540602141513461,0.011808683034755,0.00336526849747616));
#24213=CARTESIAN_POINT('',(0.00609948672115694,0.0119985718194651,0.0018293064577756));
#24214=CARTESIAN_POINT('',(0.00629032106236656,0.0120899819462528,0.000990939481183402));
#24215=CARTESIAN_POINT('',(0.0063299824867198,0.0122657336686934,-0.000693845608950565));
#24216=CARTESIAN_POINT('',(0.00617880956986341,0.0123500752643464,-0.00154026372249235));
#24217=CARTESIAN_POINT('',(0.0055583884213982,0.0125116899245174,-0.00310715596524024));
#24218=CARTESIAN_POINT('',(0.00508914018978937,0.0125889629890356,-0.00382763009444636));
#24219=CARTESIAN_POINT('',(0.00390685436447006,0.0127364405869371,-0.00502857724389744));
#24220=CARTESIAN_POINT('',(0.00319381677075958,0.0128066451203205,-0.0055090502641424));
#24221=CARTESIAN_POINT('',(0.00163683219478167,0.0129399856559524,-0.00615393207365249));
#24222=CARTESIAN_POINT('',(0.000792885212514245,0.013003121658201,-0.00631834086291762));
#24223=CARTESIAN_POINT('',(-0.000892314492041416,0.0131223251315634,-0.00630506756184518));
#24224=CARTESIAN_POINT('',(-0.00173356721432965,0.0131783926026772,-0.00612738547150761));
#24225=CARTESIAN_POINT('',(-0.00328019981295779,0.0132834590137701,-0.0054580565414708));
#24226=CARTESIAN_POINT('',(-0.00398557968929771,0.0133324579537491,-0.00496640970177156));
#24227=CARTESIAN_POINT('',(-0.00514880328885811,0.0134233873025723,-0.0037469922772707));
#24228=CARTESIAN_POINT('',(-0.0056066470120786,0.0134653177114166,-0.00301922169246908));
#24229=CARTESIAN_POINT('',(-0.00620230170530171,0.0135421099979703,-0.00144273489968662));
#24230=CARTESIAN_POINT('',(-0.00634011267530433,0.0135769718756797,-0.000594018691705771));
#24231=CARTESIAN_POINT('',(-0.00627394515429791,0.0136396270999638,0.00108987301653346));
#24232=CARTESIAN_POINT('',(-0.00606996666328886,0.0136674204465385,0.00192504851679185));
#24233=CARTESIAN_POINT('',(-0.00571112736074713,0.0136916795275457,0.00268758365066568));
#24234=CARTESIAN_POINT('',(-0.00600291424347733,0.0099532476683191,0.00195066711549077));
#24235=CARTESIAN_POINT('',(-0.00574246615396974,0.0100906032474828,0.00275216088845479));
#24236=CARTESIAN_POINT('',(-0.00531940625127602,0.010224424561079,0.00350058968249362));
#24237=CARTESIAN_POINT('',(-0.00421487443391306,0.0104849986571369,0.00477333431135782));
#24238=CARTESIAN_POINT('',(-0.0035334025192438,0.0106117514395984,0.00529765014618318));
#24239=CARTESIAN_POINT('',(-0.00201997295760744,0.0108581884733867,0.00603903134590732));
#24240=CARTESIAN_POINT('',(-0.00118801531064032,0.0109778727247135,0.00625609671080609));
#24241=CARTESIAN_POINT('',(0.000494691428125636,0.0112101726962322,0.00634864955534043));
#24242=CARTESIAN_POINT('',(0.00134544051992447,0.0113227884164242,0.00622413703497599));
#24243=CARTESIAN_POINT('',(0.0029310462363186,0.0115409513256735,0.00565323588430534));
#24244=CARTESIAN_POINT('',(0.0036659028609139,0.0116464985147307,0.00520684725399913));
#24245=CARTESIAN_POINT('',(0.0049033904503219,0.0118505243617104,0.00406286356058454));
#24246=CARTESIAN_POINT('',(0.00540602141513462,0.0119490030196329,0.00336526849747616));
#24247=CARTESIAN_POINT('',(0.00609948672115694,0.012138891804343,0.00182930645777559));
#24248=CARTESIAN_POINT('',(0.00629032106236656,0.0122303019311307,0.000990939481183403));
#24249=CARTESIAN_POINT('',(0.0063299824867198,0.0124060536535713,-0.000693845608950565));
#24250=CARTESIAN_POINT('',(0.00617880956986341,0.0124903952492243,-0.00154026372249235));
#24251=CARTESIAN_POINT('',(0.0055583884213982,0.0126520099093953,-0.00310715596524024));
#24252=CARTESIAN_POINT('',(0.00508914018978937,0.0127292829739135,-0.00382763009444637));
#24253=CARTESIAN_POINT('',(0.00390685436447006,0.012876760571815,-0.00502857724389744));
#24254=CARTESIAN_POINT('',(0.00319381677075958,0.0129469651051984,-0.00550905026414239));
#24255=CARTESIAN_POINT('',(0.00163683219478167,0.0130803056408303,-0.00615393207365248));
#24256=CARTESIAN_POINT('',(0.000792885212514244,0.0131434416430789,-0.00631834086291762));
#24257=CARTESIAN_POINT('',(-0.000892314492041418,0.0132626451164413,-0.00630506756184519));
#24258=CARTESIAN_POINT('',(-0.00173356721432965,0.0133187125875551,-0.00612738547150761));
#24259=CARTESIAN_POINT('',(-0.00328019981295779,0.013423778998648,-0.0054580565414708));
#24260=CARTESIAN_POINT('',(-0.0039855796892977,0.013472777938627,-0.00496640970177156));
#24261=CARTESIAN_POINT('',(-0.00514880328885811,0.0135637072874503,-0.0037469922772707));
#24262=CARTESIAN_POINT('',(-0.0056066470120786,0.0136056376962945,-0.00301922169246908));
#24263=CARTESIAN_POINT('',(-0.00620230170530171,0.0136824299828482,-0.00144273489968662));
#24264=CARTESIAN_POINT('',(-0.00634011267530433,0.0137172918605576,-0.000594018691705768));
#24265=CARTESIAN_POINT('',(-0.00627394515429791,0.0137799470848417,0.00108987301653346));
#24266=CARTESIAN_POINT('',(-0.00606996666328886,0.0138077404314164,0.00192504851679185));
#24267=CARTESIAN_POINT('',(-0.00571112736074713,0.0138319995124236,0.00268758365066568));
#24268=CARTESIAN_POINT('',(-0.00600350244213179,0.00996866665836644,0.00195085825261618));
#24269=CARTESIAN_POINT('',(-0.00574302883248355,0.0101060222375301,0.00275243056036177));
#24270=CARTESIAN_POINT('',(-0.00531992747604663,0.0102398435511264,0.00350093268958277));
#24271=CARTESIAN_POINT('',(-0.00421528743056271,0.0105004176471842,0.00477380202898718));
#24272=CARTESIAN_POINT('',(-0.00353374874151571,0.0106271704296457,0.00529816923917059));
#24273=CARTESIAN_POINT('',(-0.00202017088570161,0.010873607463434,0.00603962308351473));
#24274=CARTESIAN_POINT('',(-0.0011881317189345,0.0109932917147608,0.00625670971767546));
#24275=CARTESIAN_POINT('',(0.000494739900720878,0.0112255916862796,0.0063492716310481));
#24276=CARTESIAN_POINT('',(0.00134557235360914,0.0113382074064716,0.00622474691026));
#24277=CARTESIAN_POINT('',(0.00293133343639884,0.0115563703157208,0.00565378981954506));
#24278=CARTESIAN_POINT('',(0.00366626206630027,0.011661917504778,0.00520735744961822));
#24279=CARTESIAN_POINT('',(0.00490387091156926,0.0118659433517577,0.00406326166237022));
#24280=CARTESIAN_POINT('',(0.00540655112693682,0.0119644220096802,0.00336559824504906));
#24281=CARTESIAN_POINT('',(0.00610008438251554,0.0121543107943904,0.00182948570331425));
#24282=CARTESIAN_POINT('',(0.00629093742272671,0.0122457209211781,0.000991036578900586));
#24283=CARTESIAN_POINT('',(0.0063306027333251,0.0124214726436187,-0.000693913595771138));
#24284=CARTESIAN_POINT('',(0.00617941500371233,0.0125058142392716,-0.0015404146460292));
#24285=CARTESIAN_POINT('',(0.00555893306296025,0.0126674288994427,-0.00310746042152328));
#24286=CARTESIAN_POINT('',(0.00508963885182094,0.0127447019639608,-0.0038280051467593));
#24287=CARTESIAN_POINT('',(0.00390723717961403,0.0128921795618623,-0.00502906997163746));
#24288=CARTESIAN_POINT('',(0.00319412971854643,0.0129623840952457,-0.00550959007127961));
#24289=CARTESIAN_POINT('',(0.00163699258063019,0.0130957246308777,-0.00615453506986708));
#24290=CARTESIAN_POINT('',(0.000792962903781556,0.0131588606331263,-0.0063189599688124));
#24291=CARTESIAN_POINT('',(-0.00089240192593807,0.0132780641064887,-0.0063056853671487));
#24292=CARTESIAN_POINT('',(-0.00173373707880906,0.0133341315776025,-0.00612798586653968));
#24293=CARTESIAN_POINT('',(-0.00328052122503168,0.0134391979886953,-0.00545859135196174));
#24294=CARTESIAN_POINT('',(-0.00398597021838331,0.0134881969286743,-0.00496689633799283));
#24295=CARTESIAN_POINT('',(-0.00514930779700927,0.0135791262774976,-0.00374735942824544));
#24296=CARTESIAN_POINT('',(-0.0056071963822836,0.0136210566863418,-0.00301951753246696));
#24297=CARTESIAN_POINT('',(-0.00620290944103967,0.0136978489728955,-0.00144287626681137));
#24298=CARTESIAN_POINT('',(-0.0063407339145214,0.013732710850605,-0.000594076896934264));
#24299=CARTESIAN_POINT('',(-0.00627455991005623,0.0137953660748891,0.00108997980830424));
#24300=CARTESIAN_POINT('',(-0.00607056143210933,0.0138231594214637,0.00192523714366563));
#24301=CARTESIAN_POINT('',(-0.00571168696851309,0.013847418502471,0.00268784699493864));
#24302=CARTESIAN_POINT('',(-0.00600466497160202,0.00998404077070117,0.00195123602046633));
#24303=CARTESIAN_POINT('',(-0.00574414092335559,0.0101213963498648,0.00275296354617664));
#24304=CARTESIAN_POINT('',(-0.00532095763677864,0.0102552176634611,0.00350161061675348));
#24305=CARTESIAN_POINT('',(-0.00421610368672497,0.0105157917595189,0.00477472643696357));
#24306=CARTESIAN_POINT('',(-0.00353443302324826,0.0106425445419805,0.00529919518659681));
#24307=CARTESIAN_POINT('',(-0.00202056207538,0.0108889815757688,0.00604079260745369));
#24308=CARTESIAN_POINT('',(-0.00118836179098845,0.0110086658270955,0.00625792127867733));
#24309=CARTESIAN_POINT('',(0.000494835703082955,0.0112409657986143,0.00635050111591244));
#24310=CARTESIAN_POINT('',(0.00134583291276282,0.0113535815188063,0.00622595228192391));
#24311=CARTESIAN_POINT('',(0.0029319010653021,0.0115717444280555,0.00565488463000731));
#24312=CARTESIAN_POINT('',(0.00366697200816151,0.0116772916171128,0.00520836581207923));
#24313=CARTESIAN_POINT('',(0.00490482050632797,0.0118813174640925,0.00406404847997765));
#24314=CARTESIAN_POINT('',(0.00540759806163502,0.0119797961220149,0.00336624996580416));
#24315=CARTESIAN_POINT('',(0.00610126561429382,0.0121696849067251,0.00182983996835635));
#24316=CARTESIAN_POINT('',(0.00629215561164556,0.0122610950335128,0.000991228485082046));
#24317=CARTESIAN_POINT('',(0.00633182860310908,0.0124368467559534,-0.000694047966501001));
#24318=CARTESIAN_POINT('',(0.00618061159722085,0.0125211883516063,-0.00154071293480974));
#24319=CARTESIAN_POINT('',(0.00556000950518228,0.0126828030117774,-0.00310806215598619));
#24320=CARTESIAN_POINT('',(0.00509062441903194,0.0127600760762956,-0.00382874640885392));
#24321=CARTESIAN_POINT('',(0.00390799378434807,0.0129075536741971,-0.00503004381017692));
#24322=CARTESIAN_POINT('',(0.00319474823581454,0.0129777582075804,-0.0055106569586322));
#24323=CARTESIAN_POINT('',(0.00163730957094308,0.0131110987432124,-0.00615572684557856));
#24324=CARTESIAN_POINT('',(0.000793116454605152,0.013174234745461,-0.00632018358406963));
#24325=CARTESIAN_POINT('',(-0.000892574732320377,0.0132934382188234,-0.00630690641188717));
#24326=CARTESIAN_POINT('',(-0.00173407280290798,0.0133495056899372,-0.00612917250121364));
#24327=CARTESIAN_POINT('',(-0.0032811564713131,0.01345457210103,-0.0054596483638267));
#24328=CARTESIAN_POINT('',(-0.00398674206913061,0.0135035710410091,-0.00496785813711329));
#24329=CARTESIAN_POINT('',(-0.0051503049186267,0.0135945003898323,-0.00374808507395191));
#24330=CARTESIAN_POINT('',(-0.00560828217030528,0.0136364307986766,-0.00302010223750393));
#24331=CARTESIAN_POINT('',(-0.00620411058405509,0.0137132230852302,-0.00144315566807726));
#24332=CARTESIAN_POINT('',(-0.00634196174612631,0.0137480849629397,-0.000594191935098558));
#24333=CARTESIAN_POINT('',(-0.00627577492760283,0.0138107401872238,0.00109019087403817));
#24334=CARTESIAN_POINT('',(-0.00607173694700813,0.0138385335337985,0.0019256099501962));
#24335=CARTESIAN_POINT('',(-0.00571279299028783,0.0138627926148057,0.0026883674746708));
#24336=CARTESIAN_POINT('',(-0.00697849090552825,0.0138048999657612,0.00276297995550743));
#24337=CARTESIAN_POINT('',(-0.00770093960806379,0.0137551587719337,0.000935651043377239));
#24338=CARTESIAN_POINT('',(-0.00763327349501092,0.0136285000940253,-0.00330117175933696));
#24339=CARTESIAN_POINT('',(-0.00306209458664848,0.0133569832064022,-0.00773417999788023));
#24340=CARTESIAN_POINT('',(0.00330337857838533,0.0130039374480187,-0.00763353819154981));
#24341=CARTESIAN_POINT('',(0.00773369503189247,0.0125693628188748,-0.00306198864781927));
#24342=CARTESIAN_POINT('',(0.00763357751275619,0.0120532593189706,0.00330328794520609));
#24343=CARTESIAN_POINT('',(0.00306224339866001,0.0114556269483061,0.00773412121643255));
#24344=CARTESIAN_POINT('',(-0.00330460558482244,0.0107764657068814,0.0076317876877591));
#24345=CARTESIAN_POINT('',(-0.00625423884549511,0.0102693389654248,0.00458959876393758));
#24346=CARTESIAN_POINT('',(-0.00697848972311123,0.0100021874495699,0.00276298343174812));
#24347=CARTESIAN_POINT('',(-0.00697764147125442,0.0100021874312087,0.00276264710354824));
#24348=CARTESIAN_POINT('',(-0.00697848972311123,0.0100021874495699,0.00276298343174812));
#24349=CARTESIAN_POINT('',(-0.00697849262258089,0.00984605923679087,0.00276298464249866));
#24350=CARTESIAN_POINT('',(-0.00685829363455566,0.00953469610649544,0.00271539455481491));
#24351=CARTESIAN_POINT('',(-0.00642351637787649,0.00934096612656149,0.00254325398177964));
#24352=CARTESIAN_POINT('',(-0.00598873928938105,0.00953469656153736,0.00237111344924713));
#24353=CARTESIAN_POINT('',(-0.00586854056022389,0.00984605983716938,0.00232352343153022));
#24354=CARTESIAN_POINT('',(-0.00586854359428379,0.0100021880658147,0.00232352468558586));
#24355=CARTESIAN_POINT('',(-0.00586720616262124,0.0100021880960647,0.00232299439006458));
#24356=CARTESIAN_POINT('',(-0.00586854359418786,0.0100021812334169,0.00232352468554787));
#24357=CARTESIAN_POINT('',(-0.00525948646019975,0.0102693332225451,0.00385961228953058));
#24358=CARTESIAN_POINT('',(-0.00277899942182948,0.0107764609112978,0.00641793334267154));
#24359=CARTESIAN_POINT('',(0.00257518653164471,0.0114556235759148,0.00650399005855098));
#24360=CARTESIAN_POINT('',(0.00641943843133522,0.0120532573720201,0.00277789149481545));
#24361=CARTESIAN_POINT('',(0.00650363171566794,0.0125693622996134,-0.00257497215866852));
#24362=CARTESIAN_POINT('',(0.00277796785160325,0.0130039383586948,-0.00641940530424472));
#24363=CARTESIAN_POINT('',(-0.00257506110685358,0.0133569855492641,-0.00650403960238204));
#24364=CARTESIAN_POINT('',(-0.00641918264818325,0.0136285038713214,-0.00277611217167013));
#24365=CARTESIAN_POINT('',(-0.00647608625583389,0.0137551635070182,0.000786833513742433));
#24366=CARTESIAN_POINT('',(-0.00586854479004135,0.0138049051801146,0.00232352125385291));
#24367=CARTESIAN_POINT('',(0.00629981614599573,7.12593715023016E-5,-0.000371046098527164));
#24368=CARTESIAN_POINT('',(0.00635939064243718,-9.87832735314357E-5,0.000679057046437751));
#24369=CARTESIAN_POINT('',(0.00615655112478957,-0.000268825918565176,0.00174473886966687));
#24370=CARTESIAN_POINT('',(0.0051361018555028,-0.000655582350006689,0.00390539125841257));
#24371=CARTESIAN_POINT('',(0.00416503815747573,-0.000872296136414462,0.00492812037847502));
#24372=CARTESIAN_POINT('',(0.00180511324459718,-0.00130572370923002,0.00619497473129327));
#24373=CARTESIAN_POINT('',(0.000416252029745715,-0.0015224374956378,0.00643909996404906));
#24374=CARTESIAN_POINT('',(-0.00223424743743527,-0.00195586506845336,0.00605333155596514));
#24375=CARTESIAN_POINT('',(-0.00349588568976479,-0.00217257885486115,0.00542343791512543));
#24376=CARTESIAN_POINT('',(-0.00539693087742614,-0.00260600642767672,0.00353668295944536));
#24377=CARTESIAN_POINT('',(-0.00603633781275798,-0.0028227202140845,0.00227982164460499));
#24378=CARTESIAN_POINT('',(-0.00644203138574409,-0.00325614778690008,-0.000367688090038442));
#24379=CARTESIAN_POINT('',(-0.00620831802339835,-0.00347286157330787,-0.0017583365098415));
#24380=CARTESIAN_POINT('',(-0.00495947437447419,-0.00390628914612344,-0.00412777982800341));
#24381=CARTESIAN_POINT('',(-0.00394434408789578,-0.00412300293253122,-0.00510657472636225));
#24382=CARTESIAN_POINT('',(-0.00153097222593843,-0.0045564305053468,-0.00626825994707743));
#24383=CARTESIAN_POINT('',(-0.00013273065055952,-0.00477314429175458,-0.00645115026943376));
#24384=CARTESIAN_POINT('',(0.00249823664508958,-0.00520657186457014,-0.00594926641608398));
#24385=CARTESIAN_POINT('',(0.00373096236535976,-0.00542328565097793,-0.00526449224037788));
#24386=CARTESIAN_POINT('',(0.0055472139220739,-0.00585671322379348,-0.00329596320100655));
#24387=CARTESIAN_POINT('',(0.00613073975851787,-0.00607342701020125,-0.00201220833734133));
#24388=CARTESIAN_POINT('',(0.00641963495622596,-0.00650685458301679,0.000650574354163938));
#24389=CARTESIAN_POINT('',(0.00612500431749009,-0.00672356836942456,0.00202960218200398));
#24390=CARTESIAN_POINT('',(0.00477318663605599,-0.00715699594224009,0.00434184871435166));
#24391=CARTESIAN_POINT('',(0.00371599959335776,-0.00737370972864785,0.00527506741885931));
#24392=CARTESIAN_POINT('',(0.00125389165517365,-0.00780713730146336,0.00632950640194064));
#24393=CARTESIAN_POINT('',(-0.000151029240312234,-0.00802385108787111,0.00645072668051431));
#24394=CARTESIAN_POINT('',(-0.00275741214342121,-0.0084572786606866,0.00583369114460101));
#24395=CARTESIAN_POINT('',(-0.00395887415104431,-0.00867399244709434,0.00509543533011404));
#24396=CARTESIAN_POINT('',(-0.00568671665155151,-0.0091074200199098,0.00304879763889559));
#24397=CARTESIAN_POINT('',(-0.00621309714443561,-0.00932413380631752,0.00174041576216412));
#24398=CARTESIAN_POINT('',(-0.00636649778120604,-0.00971089047793098,-0.000644161934661731));
#24399=CARTESIAN_POINT('',(-0.00616278887993832,-0.00988093336313673,-0.00170967957115776));
#24400=CARTESIAN_POINT('',(-0.00572082786621745,-0.0100509762483425,-0.00266411098250738));
#24401=CARTESIAN_POINT('',(0.00629974209765909,6.75166926736438E-5,-0.00037104173723379));
#24402=CARTESIAN_POINT('',(0.00635931589385908,-0.000102525952360093,0.000679049064769141));
#24403=CARTESIAN_POINT('',(0.00615647876039675,-0.000272568597393834,0.00174471836192376));
#24404=CARTESIAN_POINT('',(0.00513604148551891,-0.000659325028835347,0.00390534535425919));
#24405=CARTESIAN_POINT('',(0.00416498920142043,-0.00087603881524312,0.00492806245311524));
#24406=CARTESIAN_POINT('',(0.00180509202721081,-0.00130946638805867,0.00619490191526757));
#24407=CARTESIAN_POINT('',(0.00041624713709969,-0.00152618017446645,0.00643902427856384));
#24408=CARTESIAN_POINT('',(-0.00223422117598532,-0.00195960774728202,0.00605326040482001));
#24409=CARTESIAN_POINT('',(-0.00349584459895921,-0.00217632153368981,0.00542337416777992));
#24410=CARTESIAN_POINT('',(-0.0053968674416456,-0.00260974910650538,0.00353664138910674));
#24411=CARTESIAN_POINT('',(-0.00603626686135811,-0.00282646289291316,0.00227979484747366));
#24412=CARTESIAN_POINT('',(-0.00644195566580279,-0.00325989046572873,-0.000367683768215259));
#24413=CARTESIAN_POINT('',(-0.00620824505053496,-0.00347660425213652,-0.00175831584227109));
#24414=CARTESIAN_POINT('',(-0.00495941608057806,-0.0039100318249521,-0.00412773130988427));
#24415=CARTESIAN_POINT('',(-0.003944297725889,-0.00412674561135988,-0.00510651470344163));
#24416=CARTESIAN_POINT('',(-0.00153095423081855,-0.00456017318417546,-0.00626818626965384));
#24417=CARTESIAN_POINT('',(-0.000132729090437181,-0.00477688697058323,-0.00645107444230868));
#24418=CARTESIAN_POINT('',(0.00249820728069801,-0.0052103145433988,-0.00594919648812543));
#24419=CARTESIAN_POINT('',(0.00373091851145183,-0.00542702832980658,-0.00526443036128734));
#24420=CARTESIAN_POINT('',(0.00554714871985936,-0.00586045590262214,-0.00329592446009935));
#24421=CARTESIAN_POINT('',(0.00613066769751307,-0.00607716968902991,-0.00201218468574945));
#24422=CARTESIAN_POINT('',(0.00641955949953335,-0.00651059726184545,0.000650566707282241));
#24423=CARTESIAN_POINT('',(0.00612493232389993,-0.00672731104825322,0.00202957832596403));
#24424=CARTESIAN_POINT('',(0.00477313053179474,-0.00716073862106875,0.00434179768005672));
#24425=CARTESIAN_POINT('',(0.00371595591532296,-0.0073774524074765,0.00527500541546762));
#24426=CARTESIAN_POINT('',(0.00125387691687189,-0.00781087998029202,0.00632943200462332));
#24427=CARTESIAN_POINT('',(-0.000151027465107407,-0.00802759376669976,0.00645065085836811));
#24428=CARTESIAN_POINT('',(-0.00275737973266859,-0.00846102133951525,0.00583362257511966));
#24429=CARTESIAN_POINT('',(-0.00395882761825048,-0.008677735125923,0.00509537543812641));
#24430=CARTESIAN_POINT('',(-0.00568664980961529,-0.00911116269873846,0.00304876180318409));
#24431=CARTESIAN_POINT('',(-0.00621302411539821,-0.00932787648514618,0.00174039530523502));
#24432=CARTESIAN_POINT('',(-0.0063664229490903,-0.00971463315675964,-0.000644154363151915));
#24433=CARTESIAN_POINT('',(-0.00616271644222663,-0.00988467604196539,-0.0017096594755033));
#24434=CARTESIAN_POINT('',(-0.0057207606233364,-0.0100547189271711,-0.00266407966842101));
#24435=CARTESIAN_POINT('',(0.00629970494285292,6.37733818485945E-5,-0.000371039548892805));
#24436=CARTESIAN_POINT('',(0.00635927838769681,-0.000106269263185143,0.000679045059853386));
#24437=CARTESIAN_POINT('',(0.00615644245053335,-0.000276311908218883,0.00174470807187195));
#24438=CARTESIAN_POINT('',(0.00513601119402079,-0.000663068339660396,0.00390532232119729));
#24439=CARTESIAN_POINT('',(0.00416496463702334,-0.000879782126068169,0.00492803338824204));
#24440=CARTESIAN_POINT('',(0.00180508138108541,-0.00131320969888372,0.00619486537879094));
#24441=CARTESIAN_POINT('',(0.000416244682144953,-0.0015299234852915,0.00643898630229508));
#24442=CARTESIAN_POINT('',(-0.00223420799892927,-0.00196335105810707,0.00605322470372089));
#24443=CARTESIAN_POINT('',(-0.00349582398106304,-0.00218006484451485,0.00542334218164257));
#24444=CARTESIAN_POINT('',(-0.00539683561184041,-0.00261349241733042,0.00353662053059805));
#24445=CARTESIAN_POINT('',(-0.00603623126048402,-0.00283020620373821,0.00227978140163185));
#24446=CARTESIAN_POINT('',(-0.00644191767224521,-0.00326363377655378,-0.000367681599679004));
#24447=CARTESIAN_POINT('',(-0.00620820843536279,-0.00348034756296157,-0.00175830547202366));
#24448=CARTESIAN_POINT('',(-0.00495938683078651,-0.00391377513577715,-0.00412770696522788));
#24449=CARTESIAN_POINT('',(-0.00394427446309265,-0.00413048892218493,-0.00510648458608745));
#24450=CARTESIAN_POINT('',(-0.00153094520151119,-0.00456391649500051,-0.00626814930095857));
#24451=CARTESIAN_POINT('',(-0.000132728307623607,-0.00478063028140828,-0.00645103639497011));
#24452=CARTESIAN_POINT('',(0.00249819254669687,-0.00521405785422385,-0.00594916140077757));
#24453=CARTESIAN_POINT('',(0.00373089650712975,-0.00543077164063163,-0.0052643993125735));
#24454=CARTESIAN_POINT('',(0.00554711600372078,-0.00586419921344719,-0.00329590502129811));
#24455=CARTESIAN_POINT('',(0.00613063153987892,-0.00608091299985495,-0.00201217281822681));
#24456=CARTESIAN_POINT('',(0.00641952163806455,-0.00651434057267049,0.00065056287035058));
#24457=CARTESIAN_POINT('',(0.00612489620009204,-0.00673105435907826,0.00202956635585666));
#24458=CARTESIAN_POINT('',(0.00477310238068363,-0.0071644819318938,0.00434177207287333));
#24459=CARTESIAN_POINT('',(0.00371593399924772,-0.00738119571830155,0.00527497430438391));
#24460=CARTESIAN_POINT('',(0.00125386952171934,-0.00781462329111707,0.00632939467471113));
#24461=CARTESIAN_POINT('',(-0.000151026574373135,-0.00803133707752481,0.00645061281352777));
#24462=CARTESIAN_POINT('',(-0.00275736347011246,-0.0084647646503403,0.00583358816940706));
#24463=CARTESIAN_POINT('',(-0.0039588042697593,-0.00868147843674805,0.00509534538646972));
#24464=CARTESIAN_POINT('',(-0.00568661627072304,-0.00911490600956351,0.00304874382210612));
#24465=CARTESIAN_POINT('',(-0.00621298747203993,-0.00933161979597122,0.00174038504067986));
#24466=CARTESIAN_POINT('',(-0.00636638540101182,-0.00971837646758469,-0.000644150564039167));
#24467=CARTESIAN_POINT('',(-0.00616268009557444,-0.00988841935279044,-0.00170964939222283));
#24468=CARTESIAN_POINT('',(-0.00572072688326437,-0.0100584622379962,-0.00266406395613276));
#24469=CARTESIAN_POINT('',(0.00629970494285293,-9.58825219423124E-5,-0.000371039548892805));
#24470=CARTESIAN_POINT('',(0.00635927838769681,-0.00026592516697605,0.000679045059853387));
#24471=CARTESIAN_POINT('',(0.00615644245053335,-0.00043596781200979,0.00174470807187195));
#24472=CARTESIAN_POINT('',(0.00513601119402079,-0.000822724243451304,0.00390532232119729));
#24473=CARTESIAN_POINT('',(0.00416496463702333,-0.00103943802985908,0.00492803338824205));
#24474=CARTESIAN_POINT('',(0.00180508138108541,-0.00147286560267463,0.00619486537879095));
#24475=CARTESIAN_POINT('',(0.000416244682144946,-0.00168957938908242,0.0064389863022951));
#24476=CARTESIAN_POINT('',(-0.00223420799892928,-0.00212300696189798,0.00605322470372089));
#24477=CARTESIAN_POINT('',(-0.00349582398106304,-0.00233972074830577,0.00542334218164257));
#24478=CARTESIAN_POINT('',(-0.00539683561184041,-0.00277314832112133,0.00353662053059804));
#24479=CARTESIAN_POINT('',(-0.00603623126048403,-0.00298986210752912,0.00227978140163184));
#24480=CARTESIAN_POINT('',(-0.00644191767224521,-0.00342328968034468,-0.000367681599679018));
#24481=CARTESIAN_POINT('',(-0.00620820843536279,-0.00364000346675248,-0.00175830547202367));
#24482=CARTESIAN_POINT('',(-0.00495938683078651,-0.00407343103956807,-0.0041277069652279));
#24483=CARTESIAN_POINT('',(-0.00394427446309265,-0.00429014482597584,-0.00510648458608746));
#24484=CARTESIAN_POINT('',(-0.00153094520151119,-0.00472357239879141,-0.00626814930095858));
#24485=CARTESIAN_POINT('',(-0.000132728307623605,-0.00494028618519919,-0.00645103639497012));
#24486=CARTESIAN_POINT('',(0.00249819254669687,-0.00537371375801476,-0.00594916140077757));
#24487=CARTESIAN_POINT('',(0.00373089650712976,-0.00559042754442254,-0.00526439931257351));
#24488=CARTESIAN_POINT('',(0.00554711600372077,-0.00602385511723811,-0.00329590502129811));
#24489=CARTESIAN_POINT('',(0.00613063153987892,-0.00624056890364588,-0.00201217281822679));
#24490=CARTESIAN_POINT('',(0.00641952163806455,-0.00667399647646141,0.000650562870350614));
#24491=CARTESIAN_POINT('',(0.00612489620009204,-0.00689071026286918,0.00202956635585669));
#24492=CARTESIAN_POINT('',(0.00477310238068361,-0.00732413783568471,0.00434177207287336));
#24493=CARTESIAN_POINT('',(0.0037159339992477,-0.00754085162209245,0.00527497430438394));
#24494=CARTESIAN_POINT('',(0.00125386952171932,-0.00797427919490799,0.00632939467471114));
#24495=CARTESIAN_POINT('',(-0.000151026574373135,-0.00819099298131572,0.00645061281352778));
#24496=CARTESIAN_POINT('',(-0.00275736347011246,-0.00862442055413122,0.00583358816940704));
#24497=CARTESIAN_POINT('',(-0.00395880426975933,-0.00884113434053896,0.00509534538646969));
#24498=CARTESIAN_POINT('',(-0.00568661627072307,-0.00927456191335442,0.00304874382210608));
#24499=CARTESIAN_POINT('',(-0.00621298747203995,-0.00949127569976213,0.00174038504067985));
#24500=CARTESIAN_POINT('',(-0.00636638540101182,-0.0098780323713756,-0.000644150564039162));
#24501=CARTESIAN_POINT('',(-0.00616268009557445,-0.0100480752565813,-0.00170964939222283));
#24502=CARTESIAN_POINT('',(-0.00572072688326439,-0.0102181181417871,-0.00266406395613277));
#24503=CARTESIAN_POINT('',(0.00636416127792705,-0.00025179511490817,-0.000374835893278158));
#24504=CARTESIAN_POINT('',(0.00642434425702011,-0.000421837759941906,0.00068599280682017));
#24505=CARTESIAN_POINT('',(0.00621943297486042,-0.000591880404975645,0.00176255930285932));
#24506=CARTESIAN_POINT('',(0.0051885610295241,-0.000978636836417156,0.00394528018690546));
#24507=CARTESIAN_POINT('',(0.00420757907034222,-0.00119535062282493,0.00497845526898258));
#24508=CARTESIAN_POINT('',(0.00182355033024902,-0.00162877819564049,0.00625824903282184));
#24509=CARTESIAN_POINT('',(0.00042050354933771,-0.00184549198204827,0.00650486771458397));
#24510=CARTESIAN_POINT('',(-0.00225706761865918,-0.00227891955486382,0.00611515914086064));
#24511=CARTESIAN_POINT('',(-0.00353159200574476,-0.00249563334127161,0.00547883188537516));
#24512=CARTESIAN_POINT('',(-0.00545205410980061,-0.00292906091408718,0.00357280597103028));
#24513=CARTESIAN_POINT('',(-0.00609799182677088,-0.00314577470049497,0.00230310731217089));
#24514=CARTESIAN_POINT('',(-0.00650782907726638,-0.00357920227331054,-0.000371443586725145));
#24515=CARTESIAN_POINT('',(-0.00627172861079161,-0.00379591605971833,-0.00177629582676178));
#24516=CARTESIAN_POINT('',(-0.00501012950877337,-0.0042293436325339,-0.00416994019133164));
#24517=CARTESIAN_POINT('',(-0.0039846308732299,-0.00444605741894169,-0.00515873231586488));
#24518=CARTESIAN_POINT('',(-0.00154660928701741,-0.00487948499175726,-0.0063322827699547));
#24519=CARTESIAN_POINT('',(-0.000134086336348389,-0.00509619877816504,-0.00651704109951128));
#24520=CARTESIAN_POINT('',(0.00252375316220668,-0.00552962635098061,-0.0060100310993011));
#24521=CARTESIAN_POINT('',(0.00376906971009273,-0.00574634013738839,-0.00531826276953433));
#24522=CARTESIAN_POINT('',(0.00560387211707439,-0.00617976771020394,-0.00332962754645642));
#24523=CARTESIAN_POINT('',(0.00619335797617,-0.00639648149661172,-0.0020327606531453));
#24524=CARTESIAN_POINT('',(0.00648520389484837,-0.00682990906942726,0.000657219197708537));
#24525=CARTESIAN_POINT('',(0.00618756395443112,-0.00704662285583503,0.00205033215525125));
#24526=CARTESIAN_POINT('',(0.0048219390625891,-0.00748005042865056,0.00438619553684241));
#24527=CARTESIAN_POINT('',(0.00375395411116432,-0.00769676421505832,0.00532894596089087));
#24528=CARTESIAN_POINT('',(0.00126669866764987,-0.00813019178787383,0.00639415478453699));
#24529=CARTESIAN_POINT('',(-0.000152571824439797,-0.00834690557428157,0.00651661318413464));
#24530=CARTESIAN_POINT('',(-0.00278557583011391,-0.00878033314709707,0.00589327536383009));
#24531=CARTESIAN_POINT('',(-0.00399930934369837,-0.0089970469335048,0.00514747914392788));
#24532=CARTESIAN_POINT('',(-0.00574479970107554,-0.00943047450632027,0.00307993748198947));
#24533=CARTESIAN_POINT('',(-0.00627655654486826,-0.00964718829272799,0.00175819203995327));
#24534=CARTESIAN_POINT('',(-0.00643152398676165,-0.0100339449643414,-0.00065074128296498));
#24535=CARTESIAN_POINT('',(-0.00622573444126181,-0.0102039878495472,-0.00172714191529876));
#24536=CARTESIAN_POINT('',(-0.00577925932124365,-0.0103740307347529,-0.0026913217087693));
#24537=CARTESIAN_POINT('',(0.00658422897131801,-0.000472288818425242,-0.000387797423766075));
#24538=CARTESIAN_POINT('',(0.00664649303051135,-0.000642331463458977,0.000709713898742101));
#24539=CARTESIAN_POINT('',(0.00643449607731892,-0.000812374108492715,0.00182350721780144));
#24540=CARTESIAN_POINT('',(0.00536797739059997,-0.00119913053993422,0.00408170487392976));
#24541=CARTESIAN_POINT('',(0.00435307384653242,-0.001415844326342,0.00515060633804724));
#24542=CARTESIAN_POINT('',(0.00188660726696621,-0.00184927189915755,0.00647465436404686));
#24543=CARTESIAN_POINT('',(0.00043504423146757,-0.00206598568556533,0.00672980092592901));
#24544=CARTESIAN_POINT('',(-0.00233511524237175,-0.0024994132583809,0.00632661653612109));
#24545=CARTESIAN_POINT('',(-0.00365371168071242,-0.00271612704478867,0.00566828558443103));
#24546=CARTESIAN_POINT('',(-0.0056405818544302,-0.00314955461760424,0.00369635079251448));
#24547=CARTESIAN_POINT('',(-0.00630885558980731,-0.00336626840401203,0.00238274695228799));
#24548=CARTESIAN_POINT('',(-0.00673286469020471,-0.0037996959768276,-0.000384287813919532));
#24549=CARTESIAN_POINT('',(-0.00648860005522499,-0.00401640976323539,-0.00183771873990057));
#24550=CARTESIAN_POINT('',(-0.00518337584814724,-0.00444983733605096,-0.0043141334446779));
#24551=CARTESIAN_POINT('',(-0.0041224162760492,-0.00466655112245875,-0.00533711722347419));
#24552=CARTESIAN_POINT('',(-0.00160008982019489,-0.00509997869527432,-0.00655124812960334));
#24553=CARTESIAN_POINT('',(-0.000138722936438618,-0.0053166924816821,-0.0067423952569362));
#24554=CARTESIAN_POINT('',(0.00261102256234292,-0.00575012005449767,-0.00621785324953767));
#24555=CARTESIAN_POINT('',(0.00389940117736819,-0.00596683384090545,-0.00550216411480628));
#24556=CARTESIAN_POINT('',(0.0057976496090339,-0.00640026141372101,-0.00344476344920941));
#24557=CARTESIAN_POINT('',(0.00640751942567434,-0.00661697520012878,-0.00210305191834394));
#24558=CARTESIAN_POINT('',(0.00670945714676693,-0.00705040277294432,0.000679945320849618));
#24559=CARTESIAN_POINT('',(0.00640152505121908,-0.00726711655935209,0.0021212310291777));
#24560=CARTESIAN_POINT('',(0.0049886779242921,-0.00770054413216763,0.00453786673001321));
#24561=CARTESIAN_POINT('',(0.00388376289291296,-0.00791725791857539,0.00551321672252064));
#24562=CARTESIAN_POINT('',(0.00131050011167958,-0.0083506854913909,0.00661525962980517));
#24563=CARTESIAN_POINT('',(-0.000157847638174655,-0.00856739927779865,0.00674195254458227));
#24564=CARTESIAN_POINT('',(-0.00288189885225745,-0.00900082685061413,0.00609706019252922));
#24565=CARTESIAN_POINT('',(-0.004137602316486,-0.00921754063702187,0.00532547492569906));
#24566=CARTESIAN_POINT('',(-0.00594345035809038,-0.00965096820983733,0.00318643929862331));
#24567=CARTESIAN_POINT('',(-0.00649359493546621,-0.00986768199624506,0.00181898893837771));
#24568=CARTESIAN_POINT('',(-0.00665392102966254,-0.0102544386678585,-0.000673243404907283));
#24569=CARTESIAN_POINT('',(-0.00644101544347415,-0.0104244815530643,-0.00178686512482473));
#24570=CARTESIAN_POINT('',(-0.00597910156483126,-0.01059452443827,-0.00278438549750075));
#24571=CARTESIAN_POINT('',(0.00673984032963485,-0.000536869928976456,-0.000396962609868636));
#24572=CARTESIAN_POINT('',(0.00680357593467928,-0.000706912574010191,0.00072648724369725));
#24573=CARTESIAN_POINT('',(0.00658656865545035,-0.00087695521904393,0.00186660390175619));
#24574=CARTESIAN_POINT('',(0.00549484391617253,-0.00126371165048544,0.00417817169524589));
#24575=CARTESIAN_POINT('',(0.00445595418940373,-0.00148042543689321,0.00527233552637138));
#24576=CARTESIAN_POINT('',(0.00193119525451979,-0.00191385300970877,0.00662767604124101));
#24577=CARTESIAN_POINT('',(0.000445326046404667,-0.00213056679611654,0.00688885272498515));
#24578=CARTESIAN_POINT('',(-0.00239030324635441,-0.00256399436893211,0.0064761394942418));
#24579=CARTESIAN_POINT('',(-0.00374006333099836,-0.0027807081553399,0.00580224957975431));
#24580=CARTESIAN_POINT('',(-0.00577389110109959,-0.00321413572815547,0.00378371017356644));
#24581=CARTESIAN_POINT('',(-0.00645795878655688,-0.00343084951456325,0.00243906068186606));
#24582=CARTESIAN_POINT('',(-0.00689198889812187,-0.00386427708737882,-0.000393370054067792));
#24583=CARTESIAN_POINT('',(-0.00664195132422956,-0.00408099087378661,-0.00188115129830126));
#24584=CARTESIAN_POINT('',(-0.00530587950953425,-0.00451441844660218,-0.0044160934719204));
#24585=CARTESIAN_POINT('',(-0.00421984526873124,-0.00473113223300997,-0.00546325440130608));
#24586=CARTESIAN_POINT('',(-0.00163790626786615,-0.00516455980582554,-0.00670608002025585));
#24587=CARTESIAN_POINT('',(-0.000142001507804065,-0.00538127359223332,-0.00690174470981995));
#24588=CARTESIAN_POINT('',(0.00267273134696934,-0.00581470116504889,-0.00636480570125073));
#24589=CARTESIAN_POINT('',(0.00399155944168066,-0.00603141495145667,-0.00563220200311741));
#24590=CARTESIAN_POINT('',(0.00593467098763979,-0.00646484252427222,-0.00352617682680408));
#24591=CARTESIAN_POINT('',(0.0065589544388876,-0.00668155631068,-0.00215275534862407));
#24592=CARTESIAN_POINT('',(0.00686802814190169,-0.00711498388349554,0.000696015116632774));
#24593=CARTESIAN_POINT('',(0.00655281839366796,-0.00733169766990331,0.0021713641037096));
#24594=CARTESIAN_POINT('',(0.0051065801040896,-0.00776512524271884,0.00464511445921495));
#24595=CARTESIAN_POINT('',(0.00397555156274497,-0.0079818390291266,0.00564351582764347));
#24596=CARTESIAN_POINT('',(0.00134147240977875,-0.00841526660194211,0.00677160436524751));
#24597=CARTESIAN_POINT('',(-0.000161578201842847,-0.00863198038834986,0.00690129153442303));
#24598=CARTESIAN_POINT('',(-0.00295000951439953,-0.00906540796116535,0.00624115782680529));
#24599=CARTESIAN_POINT('',(-0.00423539021533461,-0.00928212174757309,0.00545133695001203));
#24600=CARTESIAN_POINT('',(-0.00608391758475277,-0.00971554932038855,0.00326174745537375));
#24601=CARTESIAN_POINT('',(-0.00664706425323585,-0.00993226310679628,0.00186197883752874));
#24602=CARTESIAN_POINT('',(-0.0068111794868136,-0.0103190197784097,-0.00068915480792377));
#24603=CARTESIAN_POINT('',(-0.00659324209999915,-0.0104890626636155,-0.00182909581127476));
#24604=CARTESIAN_POINT('',(-0.00612041137043959,-0.0106591055488212,-0.00285019153359567));
#24605=CARTESIAN_POINT('',(0.00705106304626852,-0.000536869928976456,-0.00041529298207376));
#24606=CARTESIAN_POINT('',(0.00711774174301514,-0.000706912574010191,0.000760033933607546));
#24607=CARTESIAN_POINT('',(0.00689071381171319,-0.00087695521904393,0.0019527972696657));
#24608=CARTESIAN_POINT('',(0.00574857696731765,-0.00126371165048544,0.00437110533787816));
#24609=CARTESIAN_POINT('',(0.00466171487514634,-0.00148042543689321,0.00551579390301966));
#24610=CARTESIAN_POINT('',(0.00202037122962694,-0.00191385300970877,0.00693371939562929));
#24611=CARTESIAN_POINT('',(0.00046588967627886,-0.00213056679611654,0.00720695632309743));
#24612=CARTESIAN_POINT('',(-0.00250067925431972,-0.00256399436893211,0.00677518541048322));
#24613=CARTESIAN_POINT('',(-0.00391276663157022,-0.0027807081553399,0.00607017757040086));
#24614=CARTESIAN_POINT('',(-0.00604050959443837,-0.00321413572815547,0.00395842893567034));
#24615=CARTESIAN_POINT('',(-0.00675616518005603,-0.00343084951456325,0.00255168814102218));
#24616=CARTESIAN_POINT('',(-0.00721023731395619,-0.00386427708737882,-0.000411534534364311));
#24617=CARTESIAN_POINT('',(-0.00694865386223869,-0.00408099087378661,-0.00196801641510262));
#24618=CARTESIAN_POINT('',(-0.00555088683230826,-0.00451441844660218,-0.0046200135264054));
#24619=CARTESIAN_POINT('',(-0.00441470325409532,-0.00473113223300997,-0.00571552875696985));
#24620=CARTESIAN_POINT('',(-0.00171353916320868,-0.00516455980582554,-0.00701574380156088));
#24621=CARTESIAN_POINT('',(-0.000148558650534955,-0.00538127359223332,-0.00722044361558744));
#24622=CARTESIAN_POINT('',(0.00279614891622217,-0.00581470116504889,-0.00665871060467683));
#24623=CARTESIAN_POINT('',(0.0041758759703056,-0.00603141495145667,-0.00589227777973966));
#24624=CARTESIAN_POINT('',(0.00620871374485157,-0.00646484252427223,-0.00368900358199341));
#24625=CARTESIAN_POINT('',(0.00686182446531413,-0.00668155631068,-0.00225216220918432));
#24626=CARTESIAN_POINT('',(0.00718517013217121,-0.00711498388349554,0.000728154708199082));
#24627=CARTESIAN_POINT('',(0.00685540507856572,-0.00733169766990331,0.0022716302527734));
#24628=CARTESIAN_POINT('',(0.00534238446368461,-0.00776512524271884,0.00485960991761842));
#24629=CARTESIAN_POINT('',(0.00415912890240899,-0.0079818390291266,0.00590411403788912));
#24630=CARTESIAN_POINT('',(0.00140341700597708,-0.00841526660194211,0.00708429383613219));
#24631=CARTESIAN_POINT('',(-0.000169039329179231,-0.00863198038834986,0.00721996951410456));
#24632=CARTESIAN_POINT('',(-0.00308623083868367,-0.00906540796116535,0.00652935309535746));
#24633=CARTESIAN_POINT('',(-0.00443096601303181,-0.00928212174757309,0.00570306099863799));
#24634=CARTESIAN_POINT('',(-0.00636485203807753,-0.00971554932038855,0.00341236376887466));
#24635=CARTESIAN_POINT('',(-0.00695400288877511,-0.00993226310679628,0.00194795863583079));
#24636=CARTESIAN_POINT('',(-0.0071256964011157,-0.0103190197784097,-0.000720977613956743));
#24637=CARTESIAN_POINT('',(-0.00689769541304913,-0.0104890626636155,-0.00191355718417482));
#24638=CARTESIAN_POINT('',(-0.00640303098165626,-0.0106591055488212,-0.00298180360578551));
#24639=CARTESIAN_POINT('',(0.00720667440458535,-0.000472288818425242,-0.000424458168176322));
#24640=CARTESIAN_POINT('',(0.00727482464718306,-0.000642331463458977,0.000776807278562694));
#24641=CARTESIAN_POINT('',(0.00704278638984461,-0.000812374108492715,0.00199589395362046));
#24642=CARTESIAN_POINT('',(0.00587544349289021,-0.00119913053993422,0.00446757215919429));
#24643=CARTESIAN_POINT('',(0.00476459521801765,-0.001415844326342,0.0056375230913438));
#24644=CARTESIAN_POINT('',(0.00206495921718051,-0.00184927189915755,0.00708674107282344));
#24645=CARTESIAN_POINT('',(0.000476171491215956,-0.00206598568556533,0.00736600812215358));
#24646=CARTESIAN_POINT('',(-0.00255586725830238,-0.0024994132583809,0.00692470836860393));
#24647=CARTESIAN_POINT('',(-0.00399911828185615,-0.00271612704478868,0.00620414156572414));
#24648=CARTESIAN_POINT('',(-0.00617381884110776,-0.00314955461760424,0.00404578831672229));
#24649=CARTESIAN_POINT('',(-0.0069052683768056,-0.00336626840401203,0.00260800187060023));
#24650=CARTESIAN_POINT('',(-0.00736936152187335,-0.0037996959768276,-0.000420616774512571));
#24651=CARTESIAN_POINT('',(-0.00710200513124325,-0.00401640976323539,-0.00201144897350331));
#24652=CARTESIAN_POINT('',(-0.00567339049369526,-0.00444983733605097,-0.0047219735536479));
#24653=CARTESIAN_POINT('',(-0.00451213224677736,-0.00466655112245875,-0.00584166593480174));
#24654=CARTESIAN_POINT('',(-0.00175135561087993,-0.00509997869527433,-0.00717057569221338));
#24655=CARTESIAN_POINT('',(-0.0001518372219004,-0.00531669248168211,-0.00737979306847118));
#24656=CARTESIAN_POINT('',(0.00285785770084859,-0.00575012005449767,-0.00680566305638988));
#24657=CARTESIAN_POINT('',(0.00426803423461806,-0.00596683384090546,-0.00602231566805078));
#24658=CARTESIAN_POINT('',(0.00634573512345746,-0.00640026141372101,-0.00377041695958807));
#24659=CARTESIAN_POINT('',(0.00701325947852739,-0.00661697520012879,-0.00230186563946444));
#24660=CARTESIAN_POINT('',(0.00734374112730596,-0.00705040277294433,0.000744224503982235));
#24661=CARTESIAN_POINT('',(0.00700669842101459,-0.00726711655935209,0.00232176332730529));
#24662=CARTESIAN_POINT('',(0.00546028664348212,-0.00770054413216762,0.00496685764682015));
#24663=CARTESIAN_POINT('',(0.00425091757224101,-0.00791725791857539,0.00603441314301195));
#24664=CARTESIAN_POINT('',(0.00143438930407624,-0.0083506854913909,0.00724063857157453));
#24665=CARTESIAN_POINT('',(-0.000172769892847422,-0.00856739927779865,0.00737930850394532));
#24666=CARTESIAN_POINT('',(-0.00315434150082575,-0.00900082685061413,0.00667345072963354));
#24667=CARTESIAN_POINT('',(-0.00452875391188042,-0.00921754063702187,0.00582892302295097));
#24668=CARTESIAN_POINT('',(-0.00650531926473991,-0.00965096820983733,0.00348767192562511));
#24669=CARTESIAN_POINT('',(-0.00710747220654474,-0.00986768199624506,0.00199094853498182));
#24670=CARTESIAN_POINT('',(-0.00728295485826675,-0.0102544386678585,-0.000736889016973229));
#24671=CARTESIAN_POINT('',(-0.00704992206957412,-0.0104244815530643,-0.00195578787062486));
#24672=CARTESIAN_POINT('',(-0.00654434078726459,-0.01059452443827,-0.00304760964188044));
#24673=CARTESIAN_POINT('',(0.00742674209797632,-0.00025179511490817,-0.000437419698664237));
#24674=CARTESIAN_POINT('',(0.0074969734206743,-0.000421837759941906,0.000800528370484627));
#24675=CARTESIAN_POINT('',(0.00725784949230312,-0.000591880404975645,0.00205684186856258));
#24676=CARTESIAN_POINT('',(0.00605485985396608,-0.000978636836417156,0.00460399684621859));
#24677=CARTESIAN_POINT('',(0.00491008999420785,-0.00119535062282493,0.00580967416040847));
#24678=CARTESIAN_POINT('',(0.00212801615389771,-0.00162877819564049,0.00730314640404848));
#24679=CARTESIAN_POINT('',(0.00049071217334581,-0.00184549198204827,0.00759094133349861));
#24680=CARTESIAN_POINT('',(-0.00263391488201495,-0.00227891955486382,0.00713616576386438));
#24681=CARTESIAN_POINT('',(-0.00412123795682381,-0.00249563334127161,0.00639359526478001));
#24682=CARTESIAN_POINT('',(-0.00636234658573735,-0.00292906091408718,0.00416933313820649));
#24683=CARTESIAN_POINT('',(-0.00711613213984203,-0.00314577470049497,0.00268764151071733));
#24684=CARTESIAN_POINT('',(-0.00759439713481168,-0.00357920227331054,-0.000433461001706966));
#24685=CARTESIAN_POINT('',(-0.00731887657567664,-0.00379591605971833,-0.00207287188664212));
#24686=CARTESIAN_POINT('',(-0.00584663683306913,-0.0042293436325339,-0.00486616680699417));
#24687=CARTESIAN_POINT('',(-0.00464991764959665,-0.00444605741894168,-0.00602005084241107));
#24688=CARTESIAN_POINT('',(-0.0018048361440574,-0.00487948499175726,-0.00738954105186204));
#24689=CARTESIAN_POINT('',(-0.00015647382199062,-0.00509619877816504,-0.00760514722589611));
#24690=CARTESIAN_POINT('',(0.00294512710098484,-0.0055296263509806,-0.00701348520662647));
#24691=CARTESIAN_POINT('',(0.00439836570189353,-0.00574634013738838,-0.00620621701332274));
#24692=CARTESIAN_POINT('',(0.00653951261541697,-0.00617976771020394,-0.00388555286234104));
#24693=CARTESIAN_POINT('',(0.00722742092803174,-0.00639648149661171,-0.00237215690466308));
#24694=CARTESIAN_POINT('',(0.00756799437922453,-0.00682990906942726,0.000766950627123331));
#24695=CARTESIAN_POINT('',(0.00722065951780256,-0.00704662285583503,0.00239266220123176));
#24696=CARTESIAN_POINT('',(0.00562702550518511,-0.00748005042865056,0.00511852883999096));
#24697=CARTESIAN_POINT('',(0.00438072635398964,-0.00769676421505832,0.00621868390464172));
#24698=CARTESIAN_POINT('',(0.00147819074810594,-0.00813019178787383,0.00746174341684272));
#24699=CARTESIAN_POINT('',(-0.000178045706582277,-0.00834690557428157,0.00760464786439295));
#24700=CARTESIAN_POINT('',(-0.00325066452296929,-0.00878033314709707,0.00687723555833265));
#24701=CARTESIAN_POINT('',(-0.00466704688466808,-0.00899704693350481,0.00600691880472212));
#24702=CARTESIAN_POINT('',(-0.00670396992175478,-0.00943047450632027,0.00359417374225892));
#24703=CARTESIAN_POINT('',(-0.0073245105971427,-0.00964718829272799,0.00205174543340626));
#24704=CARTESIAN_POINT('',(-0.00750535190116764,-0.0100339449643414,-0.00075939113891553));
#24705=CARTESIAN_POINT('',(-0.00726520307178647,-0.0102039878495472,-0.00201551108015082));
#24706=CARTESIAN_POINT('',(-0.0067441830308522,-0.0103740307347529,-0.00314067343061189));
#24707=CARTESIAN_POINT('',(0.00749119843305045,-9.58825219423123E-5,-0.000441216043049591));
#24708=CARTESIAN_POINT('',(0.00756203928999761,-0.00026592516697605,0.000807476117451413));
#24709=CARTESIAN_POINT('',(0.00732084001663019,-0.00043596781200979,0.00207469309954995));
#24710=CARTESIAN_POINT('',(0.00610740968946939,-0.000822724243451302,0.00464395471192676));
#24711=CARTESIAN_POINT('',(0.00495270442752674,-0.00103943802985908,0.005860096041149));
#24712=CARTESIAN_POINT('',(0.00214648510306132,-0.00147286560267463,0.00736653005807937));
#24713=CARTESIAN_POINT('',(0.000494971040538567,-0.00168957938908242,0.00765682274578751));
#24714=CARTESIAN_POINT('',(-0.00265677450174487,-0.00212300696189798,0.00719810020100412));
#24715=CARTESIAN_POINT('',(-0.00415700598150554,-0.00233972074830576,0.0064490849685126));
#24716=CARTESIAN_POINT('',(-0.00641756508369755,-0.00277314832112133,0.00420551857863874));
#24717=CARTESIAN_POINT('',(-0.00717789270612889,-0.00298986210752912,0.00271096742125639));
#24718=CARTESIAN_POINT('',(-0.00766030853983284,-0.0034232896803447,-0.000437222988753104));
#24719=CARTESIAN_POINT('',(-0.00738239675110546,-0.00364000346675248,-0.00209086224138024));
#24720=CARTESIAN_POINT('',(-0.00589737951105599,-0.00407343103956805,-0.00490840003309794));
#24721=CARTESIAN_POINT('',(-0.00469027405973391,-0.00429014482597584,-0.0060722985721885));
#24722=CARTESIAN_POINT('',(-0.00182050022956361,-0.0047235723987914,-0.00745367452085818));
#24723=CARTESIAN_POINT('',(-0.000157831850715397,-0.00494028618519919,-0.0076711519304373));
#24724=CARTESIAN_POINT('',(0.00297068771649466,-0.00537371375801475,-0.00707435490515));
#24725=CARTESIAN_POINT('',(0.00443653890485652,-0.00559042754442253,-0.00626008047028358));
#24726=CARTESIAN_POINT('',(0.00659626872877059,-0.00602385511723809,-0.00391927538749937));
#24727=CARTESIAN_POINT('',(0.00729014736432282,-0.00624056890364586,-0.00239274473958158));
#24728=CARTESIAN_POINT('',(0.00763367663600835,-0.00667399647646141,0.000773606954481276));
#24729=CARTESIAN_POINT('',(0.00728332727214165,-0.00689071026286918,0.00241342800062633));
#24730=CARTESIAN_POINT('',(0.0056758621870906,-0.00732413783568471,0.00516295230396004));
#24731=CARTESIAN_POINT('',(0.00441874646590625,-0.00754085162209247,0.00627265556114868));
#24732=CARTESIAN_POINT('',(0.00149101989403648,-0.00797427919490797,0.00752650352666857));
#24733=CARTESIAN_POINT('',(-0.00017959095664894,-0.00819099298131572,0.00767064823499982));
#24734=CARTESIAN_POINT('',(-0.00327887688297075,-0.00862442055413122,0.00693692275275568));
#24735=CARTESIAN_POINT('',(-0.00470755195860714,-0.00884113434053896,0.00605905256218029));
#24736=CARTESIAN_POINT('',(-0.00676215335210728,-0.00927456191335442,0.00362536740214229));
#24737=CARTESIAN_POINT('',(-0.00738807966997103,-0.00949127569976214,0.00206955243267967));
#24738=CARTESIAN_POINT('',(-0.00757049048691747,-0.0098780323713756,-0.000765981857841343));
#24739=CARTESIAN_POINT('',(-0.00732825741747383,-0.0100480752565813,-0.00203300360322675));
#24740=CARTESIAN_POINT('',(-0.00680271546883148,-0.0102181181417871,-0.00316793118324842));
#24741=CARTESIAN_POINT('',(0.00749119843305045,6.37733790118039E-5,-0.000441216043049592));
#24742=CARTESIAN_POINT('',(0.00756203928999761,-0.000106269266021933,0.00080747611745141));
#24743=CARTESIAN_POINT('',(0.00732084001663019,-0.000276311911055674,0.00207469309954994));
#24744=CARTESIAN_POINT('',(0.00610740968946939,-0.000663068342497186,0.00464395471192676));
#24745=CARTESIAN_POINT('',(0.00495270442752674,-0.00087978212890496,0.00586009604114899));
#24746=CARTESIAN_POINT('',(0.00214648510306132,-0.00131320970172052,0.00736653005807937));
#24747=CARTESIAN_POINT('',(0.000494971040538567,-0.0015299234881283,0.00765682274578751));
#24748=CARTESIAN_POINT('',(-0.00265677450174487,-0.00196335106094386,0.00719810020100412));
#24749=CARTESIAN_POINT('',(-0.00415700598150554,-0.00218006484735165,0.00644908496851259));
#24750=CARTESIAN_POINT('',(-0.00641756508369755,-0.00261349242016722,0.00420551857863873));
#24751=CARTESIAN_POINT('',(-0.00717789270612889,-0.002830206206575,0.00271096742125639));
#24752=CARTESIAN_POINT('',(-0.00766030853983284,-0.00326363377939058,-0.000437222988753101));
#24753=CARTESIAN_POINT('',(-0.00738239675110545,-0.00348034756579837,-0.00209086224138024));
#24754=CARTESIAN_POINT('',(-0.00589737951105599,-0.00391377513861393,-0.00490840003309794));
#24755=CARTESIAN_POINT('',(-0.00469027405973391,-0.00413048892502172,-0.0060722985721885));
#24756=CARTESIAN_POINT('',(-0.00182050022956361,-0.0045639164978373,-0.00745367452085817));
#24757=CARTESIAN_POINT('',(-0.000157831850715396,-0.00478063028424508,-0.00767115193043729));
#24758=CARTESIAN_POINT('',(0.00297068771649466,-0.00521405785706064,-0.00707435490514999));
#24759=CARTESIAN_POINT('',(0.00443653890485651,-0.00543077164346842,-0.00626008047028358));
#24760=CARTESIAN_POINT('',(0.00659626872877058,-0.00586419921628398,-0.00391927538749937));
#24761=CARTESIAN_POINT('',(0.00729014736432282,-0.00608091300269175,-0.00239274473958158));
#24762=CARTESIAN_POINT('',(0.00763367663600835,-0.00651434057550729,0.000773606954481275));
#24763=CARTESIAN_POINT('',(0.00728332727214164,-0.00673105436191506,0.00241342800062633));
#24764=CARTESIAN_POINT('',(0.00567586218709059,-0.00716448193473059,0.00516295230396004));
#24765=CARTESIAN_POINT('',(0.00441874646590625,-0.00738119572113835,0.00627265556114868));
#24766=CARTESIAN_POINT('',(0.00149101989403648,-0.00781462329395386,0.00752650352666857));
#24767=CARTESIAN_POINT('',(-0.000179590956648939,-0.00803133708036161,0.00767064823499982));
#24768=CARTESIAN_POINT('',(-0.00327887688297075,-0.0084647646531771,0.00693692275275568));
#24769=CARTESIAN_POINT('',(-0.00470755195860714,-0.00868147843958484,0.00605905256218029));
#24770=CARTESIAN_POINT('',(-0.00676215335210728,-0.0091149060124003,0.00362536740214228));
#24771=CARTESIAN_POINT('',(-0.00738807966997102,-0.00933161979880802,0.00206955243267967));
#24772=CARTESIAN_POINT('',(-0.00757049048691747,-0.00971837647042148,-0.000765981857841343));
#24773=CARTESIAN_POINT('',(-0.00732825741747383,-0.00988841935562723,-0.00203300360322675));
#24774=CARTESIAN_POINT('',(-0.00680271546883148,-0.010058462240833,-0.00316793118324842));
#24775=CARTESIAN_POINT('',(0.0074911612783006,6.75166870000634E-5,-0.000441213854711924));
#24776=CARTESIAN_POINT('',(0.00756200178389218,-0.000102525958033674,0.000807472112541725));
#24777=CARTESIAN_POINT('',(0.00732080370682183,-0.000272568603067414,0.00207468280951373));
#24778=CARTESIAN_POINT('',(0.00610737939801719,-0.000659325034508927,0.00464393167889977));
#24779=CARTESIAN_POINT('',(0.00495267986316688,-0.000876038820916701,0.00586006697631985));
#24780=CARTESIAN_POINT('',(0.00214647445695205,-0.00130946639373226,0.00736649352165812));
#24781=CARTESIAN_POINT('',(0.000494968585587552,-0.00152618018014004,0.00765678476957631));
#24782=CARTESIAN_POINT('',(-0.00265676132470878,-0.0019596077529556,0.00719806449995911));
#24783=CARTESIAN_POINT('',(-0.00415698536364062,-0.00217632153936339,0.00644905298242372));
#24784=CARTESIAN_POINT('',(-0.0064175332539406,-0.00260974911217896,0.00420549772016165));
#24785=CARTESIAN_POINT('',(-0.00717785710530876,-0.00282646289858674,0.00271095397543496));
#24786=CARTESIAN_POINT('',(-0.00766027054633285,-0.00325989047140232,-0.000437220820220132));
#24787=CARTESIAN_POINT('',(-0.00738236013598878,-0.00347660425781011,-0.00209085187114853));
#24788=CARTESIAN_POINT('',(-0.00589735026130877,-0.00391003183062568,-0.00490837568847844));
#24789=CARTESIAN_POINT('',(-0.00469025079697282,-0.00412674561703346,-0.00607226845487996));
#24790=CARTESIAN_POINT('',(-0.00182049120026993,-0.00456017318984904,-0.00745363755221893));
#24791=CARTESIAN_POINT('',(-0.000157831067903008,-0.00477688697625682,-0.00767111388315639));
#24792=CARTESIAN_POINT('',(0.00297067298251585,-0.00521031454907239,-0.00707431981785531));
#24793=CARTESIAN_POINT('',(0.00443651690056778,-0.00542702833548016,-0.0062600494216168));
#24794=CARTESIAN_POINT('',(0.00659623601268159,-0.00586045590829572,-0.0039192559487276));
#24795=CARTESIAN_POINT('',(0.00729011120674347,-0.00607716969470349,-0.00239273287207692));
#24796=CARTESIAN_POINT('',(0.00763363877459693,-0.00651059726751903,0.00077360311755543));
#24797=CARTESIAN_POINT('',(0.0072832911483885,-0.0067273110539268,0.00241341603053711));
#24798=CARTESIAN_POINT('',(0.00567583403602215,-0.00716073862674233,0.00516292669681546));
#24799=CARTESIAN_POINT('',(0.00441872454986423,-0.00737745241315009,0.00627262445011212));
#24800=CARTESIAN_POINT('',(0.00149101249889514,-0.0078108799859656,0.00752646619681296));
#24801=CARTESIAN_POINT('',(-0.000179590065916016,-0.00802759377237335,0.00767061019021714));
#24802=CARTESIAN_POINT('',(-0.00327886062043926,-0.00846102134518883,0.00693688834709523));
#24803=CARTESIAN_POINT('',(-0.00470752861015135,-0.00867773513159658,0.00605902251056914));
#24804=CARTESIAN_POINT('',(-0.00676211981326586,-0.00911116270441204,0.00362534942109156));
#24805=CARTESIAN_POINT('',(-0.00738804302666828,-0.00932787649081976,0.00206954216814007));
#24806=CARTESIAN_POINT('',(-0.00757045293889591,-0.00971463316243323,-0.000765978058734354));
#24807=CARTESIAN_POINT('',(-0.00732822107087673,-0.00988467604763897,-0.00203299351996157));
#24808=CARTESIAN_POINT('',(-0.00680268172881059,-0.0100547189328447,-0.00316791547098399));
#24809=CARTESIAN_POINT('',(0.00749108723007599,7.12593629933681E-5,-0.000441209493425148));
#24810=CARTESIAN_POINT('',(0.00756192703542718,-9.87832820403692E-5,0.000807464130885192));
#24811=CARTESIAN_POINT('',(0.0073207313425385,-0.000268825927074109,0.00207466230180165));
#24812=CARTESIAN_POINT('',(0.00610731902812464,-0.000655582358515622,0.00464388577481585));
#24813=CARTESIAN_POINT('',(0.00495263090718565,-0.000872296144923396,0.00586000905104771));
#24814=CARTESIAN_POINT('',(0.00214645323959778,-0.00130572371773895,0.00736642070574259));
#24815=CARTESIAN_POINT('',(0.000494963692948929,-0.00152243750414673,0.0076567090842056));
#24816=CARTESIAN_POINT('',(-0.00265673506329857,-0.0019558650769623,0.00719799334892164));
#24817=CARTESIAN_POINT('',(-0.00415694427289721,-0.00217257886337008,0.00644898923517466));
#24818=CARTESIAN_POINT('',(-0.00641746981825604,-0.00260600643618565,0.00420545614988593));
#24819=CARTESIAN_POINT('',(-0.00717778615401624,-0.00282272022259344,0.00271092717834417));
#24820=CARTESIAN_POINT('',(-0.00766019482650612,-0.00325614779540901,-0.000437216498403487));
#24821=CARTESIAN_POINT('',(-0.0073822871632358,-0.0034728615818168,-0.00209083120360938));
#24822=CARTESIAN_POINT('',(-0.00589729196750083,-0.00390628915463237,-0.00490832717043271));
#24823=CARTESIAN_POINT('',(-0.00469020443503618,-0.00412300294104016,-0.00607220843205016));
#24824=CARTESIAN_POINT('',(-0.00182047320517728,-0.00455643051385573,-0.00745356387490681));
#24825=CARTESIAN_POINT('',(-0.000157829507783031,-0.00477314430026351,-0.00767103805614603));
#24826=CARTESIAN_POINT('',(0.0029706436181687,-0.00520657187307908,-0.00707424989000256));
#24827=CARTESIAN_POINT('',(0.0044364730467262,-0.00542328565948686,-0.00625998754261988));
#24828=CARTESIAN_POINT('',(0.00659617081056569,-0.00585671323230241,-0.00391921720787901));
#24829=CARTESIAN_POINT('',(0.0072900391458477,-0.00607342701871018,-0.00239270922052083));
#24830=CARTESIAN_POINT('',(0.00763356331801849,-0.00650685459152572,0.000773595470685301));
#24831=CARTESIAN_POINT('',(0.00728321915490727,-0.00672356837793349,0.00241339217453326));
#24832=CARTESIAN_POINT('',(0.00567577793184578,-0.00715699595074902,0.00516287566259773));
#24833=CARTESIAN_POINT('',(0.00441868087189551,-0.00737370973715678,0.00627256244681424));
#24834=CARTESIAN_POINT('',(0.00149099776061568,-0.00780713730997229,0.00752639179960821));
#24835=CARTESIAN_POINT('',(-0.000179588290713876,-0.00802385109638004,0.00767053436818566));
#24836=CARTESIAN_POINT('',(-0.00327882820973568,-0.00845727866919553,0.00693681977771762));
#24837=CARTESIAN_POINT('',(-0.00470748207742792,-0.00867399245560327,0.00605896261867213));
#24838=CARTESIAN_POINT('',(-0.00676205297143077,-0.00910742002841873,0.00362531358543428));
#24839=CARTESIAN_POINT('',(-0.00738796999774137,-0.00932413381482645,0.00206952171124192));
#24840=CARTESIAN_POINT('',(-0.00757037810689339,-0.00971089048643992,-0.000765970487235993));
#24841=CARTESIAN_POINT('',(-0.00732814863327465,-0.00988093337164566,-0.00203297342433751));
#24842=CARTESIAN_POINT('',(-0.00680261448603128,-0.0100509762568514,-0.003167884156945));
#24843=CARTESIAN_POINT('',(0.00750327656949163,-8.53080491936399E-9,5.83924182010614E-10));
#24844=CARTESIAN_POINT('',(0.00750045193429679,-0.000208387270651741,0.00153290805400538));
#24845=CARTESIAN_POINT('',(0.00653694841133434,-0.00062514475034539,0.00459055487999984));
#24846=CARTESIAN_POINT('',(0.00270641832097577,-0.00125028096988588,0.00751610457455796));
#24847=CARTESIAN_POINT('',(-0.00210705546339051,-0.00187541718942638,0.00770553350902045));
#24848=CARTESIAN_POINT('',(-0.00615519750508701,-0.00250055340896689,0.0050930536775311));
#24849=CARTESIAN_POINT('',(-0.00796476961812452,-0.00312568962850741,0.000627460647780618));
#24850=CARTESIAN_POINT('',(-0.00687737551287545,-0.00375082584804793,-0.00406674126964439));
#24851=CARTESIAN_POINT('',(-0.00328822051990866,-0.00437596206758845,-0.00728203064254025));
#24852=CARTESIAN_POINT('',(0.00149719851208568,-0.00500109828712896,-0.00784857616360702));
#24853=CARTESIAN_POINT('',(0.00573800786308136,-0.00562623450666946,-0.00556018257780444));
#24854=CARTESIAN_POINT('',(0.00789149013387365,-0.00625137072620993,-0.00124942470180139));
#24855=CARTESIAN_POINT('',(0.00717446965196578,-0.00687650694575041,0.00351542988874914));
#24856=CARTESIAN_POINT('',(0.00384807543662403,-0.00750164316529085,0.00700128328974673));
#24857=CARTESIAN_POINT('',(-0.000877510408965592,-0.00812677938483126,0.00794008218231011));
#24858=CARTESIAN_POINT('',(-0.00528323049698942,-0.00875191560437166,0.00599199497594793));
#24859=CARTESIAN_POINT('',(-0.00776779806369973,-0.009377051823912,0.00186177392815872));
#24860=CARTESIAN_POINT('',(-0.00753804409837646,-0.00979380930360554,-0.00133584335935025));
#24861=CARTESIAN_POINT('',(-0.00697636861983814,-0.0100021880434523,-0.00276214414835674));
#24862=CARTESIAN_POINT('',(0.00750327646842837,-8.5308003845869E-9,5.83738566996586E-10));
#24863=CARTESIAN_POINT('',(-0.00586675988532295,-0.0100021881184342,-0.00232281882532306));
#24864=CARTESIAN_POINT('',(-0.00633909957834279,-0.0097938093874645,-0.00112337476477271));
#24865=CARTESIAN_POINT('',(-0.00653231086002425,-0.00937705192552518,0.00156565350772152));
#24866=CARTESIAN_POINT('',(-0.00444292037225485,-0.00875191573261618,0.00503895285821675));
#24867=CARTESIAN_POINT('',(-0.000737941280445877,-0.00812677953970714,0.00667719248116907));
#24868=CARTESIAN_POINT('',(0.00323602849815479,-0.00750164334679806,0.00588771257234701));
#24869=CARTESIAN_POINT('',(0.00603335200295941,-0.00687650715388895,0.00295629339011012));
#24870=CARTESIAN_POINT('',(0.00663632948134336,-0.00625137096097982,-0.00105069907242596));
#24871=CARTESIAN_POINT('',(0.00482536482892095,-0.0056262347680707,-0.00467582061643415));
#24872=CARTESIAN_POINT('',(0.00125906729727915,-0.00500109857516152,-0.00660024047415044));
#24873=CARTESIAN_POINT('',(-0.00276521905501561,-0.00437596238225236,-0.0061238066311924));
#24874=CARTESIAN_POINT('',(-0.00578351087799506,-0.00375082618934319,-0.00341991802437042));
#24875=CARTESIAN_POINT('',(-0.00669795362144113,-0.003125689996434,0.000527659058564769));
#24876=CARTESIAN_POINT('',(-0.00517619987335009,-0.00250055380352483,0.00428298895775701));
#24877=CARTESIAN_POINT('',(-0.00177192579579772,-0.00187541761061565,0.00647994872559159));
#24878=CARTESIAN_POINT('',(0.00227595305361633,-0.00125028141770649,0.00632065066437801));
#24879=CARTESIAN_POINT('',(0.00549722889407064,-0.000625145224797345,0.00386041839750601));
#24880=CARTESIAN_POINT('',(0.0063074860203521,-0.000208387762857922,0.00128909831370986));
#24881=CARTESIAN_POINT('',(0.006309862017394,-9.03188821431785E-9,3.59097525483689E-9));
#24882=CARTESIAN_POINT('',(0.006309861940649,-9.03189165685046E-9,3.59083324543894E-9));
#24883=CARTESIAN_POINT('',(0.006309862017394,-9.03188821431785E-9,3.59097525483689E-9));
#24884=CARTESIAN_POINT('',(0.00630986901478792,-0.000155917358435469,3.33265209946742E-9));
#24885=CARTESIAN_POINT('',(0.00643899489450502,-0.000467728700051866,2.8884814458691E-9));
#24886=CARTESIAN_POINT('',(0.00690656929312651,-0.000661460863890071,2.25531077613276E-9));
#24887=CARTESIAN_POINT('',(0.00737414369198757,-0.000467728449513883,1.49442951234317E-9));
#24888=CARTESIAN_POINT('',(0.00750326957200423,-0.000155916940868211,8.91109424662301E-10));
#24889=CARTESIAN_POINT('',(0.00750327656949163,-8.53080492228456E-9,5.83924176101713E-10));
#24890=CARTESIAN_POINT('',(0.00749108680181898,4.8779357875437E-5,-0.000441209536398754));
#24891=CARTESIAN_POINT('',(0.00756192661576567,-0.000121263290243651,0.000807464039153491));
#24892=CARTESIAN_POINT('',(0.00732073093746893,-0.000291305938362742,0.0020746621637675));
#24893=CARTESIAN_POINT('',(0.00610731868211987,-0.000678062372889606,0.0046438855117206));
#24894=CARTESIAN_POINT('',(0.00495263062659871,-0.00089477615929738,0.00586000871905406));
#24895=CARTESIAN_POINT('',(0.00214645311799237,-0.00132820373211294,0.00736642028840452));
#24896=CARTESIAN_POINT('',(0.000494963664907198,-0.00154491751852072,0.0076567086504215));
#24897=CARTESIAN_POINT('',(-0.00265673491278359,-0.00197834509133628,0.00719799294112568));
#24898=CARTESIAN_POINT('',(-0.00415694403738921,-0.00219505887774407,0.00644898886981287));
#24899=CARTESIAN_POINT('',(-0.00641746945467996,-0.00262848645055964,0.00420545591162953));
#24900=CARTESIAN_POINT('',(-0.0071777857473651,-0.00284520023696742,0.00271092702475898));
#24901=CARTESIAN_POINT('',(-0.00766019439252454,-0.003278627809783,-0.000437216473633373));
#24902=CARTESIAN_POINT('',(-0.00738228674499883,-0.00349534159619078,-0.00209083108515518));
#24903=CARTESIAN_POINT('',(-0.00589729163339495,-0.00392876916900636,-0.00490832689235577));
#24904=CARTESIAN_POINT('',(-0.00469020416931679,-0.00414548295541414,-0.00607220808803455));
#24905=CARTESIAN_POINT('',(-0.00182047310203998,-0.00457891052822971,-0.00745356345263173));
#24906=CARTESIAN_POINT('',(-0.000157829498841341,-0.0047956243146375,-0.00767103762155014));
#24907=CARTESIAN_POINT('',(0.00297064344986951,-0.00522905188745306,-0.00707424948921717));
#24908=CARTESIAN_POINT('',(0.00443647279538173,-0.00544576567386084,-0.00625998718796581));
#24909=CARTESIAN_POINT('',(0.00659617043686546,-0.0058791932466764,-0.00391921698583922));
#24910=CARTESIAN_POINT('',(0.00729003873283697,-0.00609590703308417,-0.002392709084964));
#24911=CARTESIAN_POINT('',(0.0076335628855457,-0.00652933460589971,0.000773595426857932));
#24912=CARTESIAN_POINT('',(0.00728321874228292,-0.00674604839230748,0.00241339203780465));
#24913=CARTESIAN_POINT('',(0.00567577761028959,-0.00717947596512301,0.00516287537009956));
#24914=CARTESIAN_POINT('',(0.00441868062155905,-0.00739618975153077,0.00627256209144775));
#24915=CARTESIAN_POINT('',(0.00149099767614452,-0.00782961732434628,0.00752639137320712));
#24916=CARTESIAN_POINT('',(-0.000179588280539459,-0.00804633111075403,0.0076705339336183));
#24917=CARTESIAN_POINT('',(-0.00327882802397656,-0.00847975868356952,0.00693681938471822));
#24918=CARTESIAN_POINT('',(-0.00470748181072968,-0.00869647246997725,0.00605896227540695));
#24919=CARTESIAN_POINT('',(-0.00676205258833262,-0.00912990004279271,0.00362531338004534));
#24920=CARTESIAN_POINT('',(-0.00738796957918245,-0.00934661382920044,0.002069521593995));
#24921=CARTESIAN_POINT('',(-0.00756094313073936,-0.00971336659681803,-0.000619312571671788));
#24922=CARTESIAN_POINT('',(-0.00738067797570845,-0.0098634055780279,-0.00173515348405907));
#24923=CARTESIAN_POINT('',(-0.00697626028083462,-0.0100134445592378,-0.0027621141197859));
#24924=CARTESIAN_POINT('',(0.00749116113247787,5.25291749297248E-5,-0.000441213914320999));
#24925=CARTESIAN_POINT('',(0.00756200164933592,-0.000117513473189364,0.000807472051253157));
#24926=CARTESIAN_POINT('',(0.00732080357776379,-0.000287556121308455,0.00207468274969978));
#24927=CARTESIAN_POINT('',(0.00610737928227492,-0.000674312555835319,0.00464393159089162));
#24928=CARTESIAN_POINT('',(0.00495267976930757,-0.000891026342243092,0.00586006686526445));
#24929=CARTESIAN_POINT('',(0.00214647441627375,-0.00132445391505865,0.00736649338205411));
#24930=CARTESIAN_POINT('',(0.000494968576207295,-0.00154116770146643,0.00765678462447093));
#24931=CARTESIAN_POINT('',(-0.00265676127435993,-0.00197459527428199,0.00719806436354704));
#24932=CARTESIAN_POINT('',(-0.0041569852848607,-0.00219130906068978,0.00644905286020633));
#24933=CARTESIAN_POINT('',(-0.00641753313232054,-0.00262473663350535,0.00420549764046236));
#24934=CARTESIAN_POINT('',(-0.00717785696927964,-0.00284145041991313,0.00271095392405908));
#24935=CARTESIAN_POINT('',(-0.0076602704011614,-0.00327487799272871,-0.000437220811934266));
#24936=CARTESIAN_POINT('',(-0.00738235999608408,-0.00349159177913649,-0.00209085183152434));
#24937=CARTESIAN_POINT('',(-0.0058973501495468,-0.00392501935195207,-0.00490837559545876));
#24938=CARTESIAN_POINT('',(-0.00469025070808686,-0.00414173313835985,-0.00607226833980309));
#24939=CARTESIAN_POINT('',(-0.00182049116576941,-0.00457516071117542,-0.00745363741096344));
#24940=CARTESIAN_POINT('',(-0.000157831064911919,-0.00479187449758321,-0.00767111373777945));
#24941=CARTESIAN_POINT('',(0.00297067292621798,-0.00522530207039877,-0.00707431968378835));
#24942=CARTESIAN_POINT('',(0.00443651681649039,-0.00544201585680655,-0.00626004930298125));
#24943=CARTESIAN_POINT('',(0.00659623588767489,-0.00587544342962211,-0.00391925587445293));
#24944=CARTESIAN_POINT('',(0.007290111068587,-0.00609215721602988,-0.00239273282673172));
#24945=CARTESIAN_POINT('',(0.00763363862993019,-0.00652558478884542,0.00077360310289471));
#24946=CARTESIAN_POINT('',(0.00728329101036128,-0.00674229857525319,0.00241341598479994));
#24947=CARTESIAN_POINT('',(0.00567583392845819,-0.00717572614806872,0.00516292659897171));
#24948=CARTESIAN_POINT('',(0.00441872446612402,-0.00739243993447648,0.00627262433123825));
#24949=CARTESIAN_POINT('',(0.00149101247063865,-0.00782586750729199,0.00752646605417728));
#24950=CARTESIAN_POINT('',(-0.000179590062512566,-0.00804258129369974,0.00767061004484975));
#24951=CARTESIAN_POINT('',(-0.00327886055830087,-0.00847600886651523,0.00693688821563276));
#24952=CARTESIAN_POINT('',(-0.00470752852093795,-0.00869272265292296,0.0060590223957433));
#24953=CARTESIAN_POINT('',(-0.00676211968511546,-0.00912615022573842,0.00362534935238679));
#24954=CARTESIAN_POINT('',(-0.00738804288665588,-0.00934286401214615,0.00206954212891973));
#24955=CARTESIAN_POINT('',(-0.00756101815455094,-0.00970961677976375,-0.000619318716829726));
#24956=CARTESIAN_POINT('',(-0.00738075121083061,-0.00985965576097361,-0.00173517070120062));
#24957=CARTESIAN_POINT('',(-0.0069763295031033,-0.0100096947421835,-0.00276214152699234));
#24958=CARTESIAN_POINT('',(0.00749119842919432,5.62796276046614E-5,-0.000441216111020545));
#24959=CARTESIAN_POINT('',(0.00756203929875053,-0.000113763020514427,0.000807476071465192));
#24960=CARTESIAN_POINT('',(0.00732084002631034,-0.000283805668633518,0.00207469307905365));
#24961=CARTESIAN_POINT('',(0.00610740968946939,-0.000670562103160382,0.00464395471192676));
#24962=CARTESIAN_POINT('',(0.00495270442752674,-0.000887275889568156,0.00586009604114899));
#24963=CARTESIAN_POINT('',(0.00214648510306132,-0.00132070346238371,0.00736653005807937));
#24964=CARTESIAN_POINT('',(0.000494971040538567,-0.00153741724879149,0.00765682274578751));
#24965=CARTESIAN_POINT('',(-0.00265677450174487,-0.00197084482160706,0.00719810020100412));
#24966=CARTESIAN_POINT('',(-0.00415700598150554,-0.00218755860801484,0.00644908496851259));
#24967=CARTESIAN_POINT('',(-0.00641756508369755,-0.00262098618083041,0.00420551857863873));
#24968=CARTESIAN_POINT('',(-0.00717789270612889,-0.0028376999672382,0.00271096742125639));
#24969=CARTESIAN_POINT('',(-0.00766030853983284,-0.00327112754005377,-0.000437222988753101));
#24970=CARTESIAN_POINT('',(-0.00738239675110545,-0.00348784132646156,-0.00209086224138024));
#24971=CARTESIAN_POINT('',(-0.00589737951105598,-0.00392126889927713,-0.00490840003309794));
#24972=CARTESIAN_POINT('',(-0.00469027405973391,-0.00413798268568492,-0.0060722985721885));
#24973=CARTESIAN_POINT('',(-0.00182050022956361,-0.00457141025850048,-0.00745367452085817));
#24974=CARTESIAN_POINT('',(-0.000157831850715397,-0.00478812404490827,-0.00767115193043729));
#24975=CARTESIAN_POINT('',(0.00297068771649466,-0.00522155161772383,-0.00707435490514999));
#24976=CARTESIAN_POINT('',(0.00443653890485651,-0.00543826540413161,-0.00626008047028358));
#24977=CARTESIAN_POINT('',(0.00659626872877058,-0.00587169297694717,-0.00391927538749937));
#24978=CARTESIAN_POINT('',(0.00729014736432282,-0.00608840676335494,-0.00239274473958158));
#24979=CARTESIAN_POINT('',(0.00763367663600835,-0.00652183433617048,0.000773606954481275));
#24980=CARTESIAN_POINT('',(0.00728332727214164,-0.00673854812257825,0.00241342800062633));
#24981=CARTESIAN_POINT('',(0.00567586218709059,-0.00717197569539378,0.00516295230396003));
#24982=CARTESIAN_POINT('',(0.00441874646590624,-0.00738868948180154,0.00627265556114867));
#24983=CARTESIAN_POINT('',(0.00149101989403648,-0.00782211705461705,0.00752650352666857));
#24984=CARTESIAN_POINT('',(-0.000179590956648939,-0.0080388308410248,0.00767064823499982));
#24985=CARTESIAN_POINT('',(-0.00327887688297075,-0.00847225841384029,0.00693692275275568));
#24986=CARTESIAN_POINT('',(-0.00470755195860714,-0.00868897220024802,0.00605905256218029));
#24987=CARTESIAN_POINT('',(-0.00676215335210727,-0.00912239977306348,0.00362536740214228));
#24988=CARTESIAN_POINT('',(-0.00738807966997102,-0.00933911355947121,0.00206955243267967));
#24989=CARTESIAN_POINT('',(-0.00756105579906895,-0.00970586632708881,-0.000619321800270888));
#24990=CARTESIAN_POINT('',(-0.00738078795784222,-0.00985590530829868,-0.00173517934020444));
#24991=CARTESIAN_POINT('',(-0.00697636423659504,-0.0100059442895085,-0.00276215527904059));
#24992=CARTESIAN_POINT('',(0.00749119842919431,0.000215942673245456,-0.000441216111020545));
#24993=CARTESIAN_POINT('',(0.00756203929875052,4.59000251263681E-5,0.000807476071465192));
#24994=CARTESIAN_POINT('',(0.00732084002631033,-0.000124142622992723,0.00207469307905365));
#24995=CARTESIAN_POINT('',(0.00610740968946938,-0.000510899057519587,0.00464395471192676));
#24996=CARTESIAN_POINT('',(0.00495270442752674,-0.000727612843927361,0.005860096041149));
#24997=CARTESIAN_POINT('',(0.00214648510306132,-0.00116104041674292,0.00736653005807936));
#24998=CARTESIAN_POINT('',(0.000494971040538565,-0.0013777542031507,0.00765682274578749));
#24999=CARTESIAN_POINT('',(-0.00265677450174487,-0.00181118177596626,0.00719810020100411));
#25000=CARTESIAN_POINT('',(-0.00415700598150554,-0.00202789556237405,0.0064490849685126));
#25001=CARTESIAN_POINT('',(-0.00641756508369755,-0.00246132313518961,0.00420551857863873));
#25002=CARTESIAN_POINT('',(-0.00717789270612888,-0.00267803692159741,0.00271096742125639));
#25003=CARTESIAN_POINT('',(-0.00766030853983282,-0.00311146449441299,-0.000437222988753105));
#25004=CARTESIAN_POINT('',(-0.00738239675110542,-0.00332817828082076,-0.00209086224138025));
#25005=CARTESIAN_POINT('',(-0.00589737951105598,-0.00376160585363634,-0.00490840003309796));
#25006=CARTESIAN_POINT('',(-0.00469027405973391,-0.00397831964004412,-0.0060722985721885));
#25007=CARTESIAN_POINT('',(-0.0018205002295636,-0.00441174721285969,-0.00745367452085817));
#25008=CARTESIAN_POINT('',(-0.000157831850715366,-0.00462846099926748,-0.00767115193043729));
#25009=CARTESIAN_POINT('',(0.00297068771649469,-0.00506188857208304,-0.00707435490514999));
#25010=CARTESIAN_POINT('',(0.00443653890485652,-0.00527860235849082,-0.00626008047028357));
#25011=CARTESIAN_POINT('',(0.00659626872877058,-0.00571202993130638,-0.00391927538749938));
#25012=CARTESIAN_POINT('',(0.0072901473643228,-0.00592874371771416,-0.00239274473958159));
#25013=CARTESIAN_POINT('',(0.00763367663600834,-0.0063621712905297,0.000773606954481287));
#25014=CARTESIAN_POINT('',(0.00728332727214164,-0.00657888507693747,0.00241342800062636));
#25015=CARTESIAN_POINT('',(0.00567586218709056,-0.00701231264975299,0.00516295230396007));
#25016=CARTESIAN_POINT('',(0.00441874646590621,-0.00722902643616075,0.00627265556114869));
#25017=CARTESIAN_POINT('',(0.00149101989403646,-0.00766245400897627,0.00752650352666855));
#25018=CARTESIAN_POINT('',(-0.000179590956648946,-0.00787916779538399,0.00767064823499983));
#25019=CARTESIAN_POINT('',(-0.00327887688297074,-0.00831259536819949,0.00693692275275569));
#25020=CARTESIAN_POINT('',(-0.00470755195860713,-0.00852930915460724,0.00605905256218031));
#25021=CARTESIAN_POINT('',(-0.00676215335210728,-0.0089627367274227,0.00362536740214226));
#25022=CARTESIAN_POINT('',(-0.00738807966997103,-0.00917945051383042,0.00206955243267961));
#25023=CARTESIAN_POINT('',(-0.00756105579906895,-0.00954620328144802,-0.000619321800270949));
#25024=CARTESIAN_POINT('',(-0.00738078795784222,-0.0096962422626579,-0.00173517934020447));
#25025=CARTESIAN_POINT('',(-0.00697636423659504,-0.00984628124386777,-0.00276215527904061));
#25026=CARTESIAN_POINT('',(0.00742674209415336,0.000371855266211312,-0.00043741976605035));
#25027=CARTESIAN_POINT('',(0.0074969734293519,0.000201812618092225,0.000800528324894085));
#25028=CARTESIAN_POINT('',(0.00725784950189997,3.17699699731351E-5,0.00205684184824264));
#25029=CARTESIAN_POINT('',(0.00605485985396608,-0.000354986464553727,0.00460399684621859));
#25030=CARTESIAN_POINT('',(0.00491008999420785,-0.0005717002509615,0.00580967416040846));
#25031=CARTESIAN_POINT('',(0.00212801615389771,-0.00100512782377705,0.00730314640404847));
#25032=CARTESIAN_POINT('',(0.00049071217334581,-0.00122184161018483,0.00759094133349861));
#25033=CARTESIAN_POINT('',(-0.00263391488201495,-0.0016552691830004,0.00713616576386437));
#25034=CARTESIAN_POINT('',(-0.00412123795682381,-0.00187198296940818,0.00639359526478));
#25035=CARTESIAN_POINT('',(-0.00636234658573735,-0.00230541054222375,0.00416933313820649));
#25036=CARTESIAN_POINT('',(-0.00711613213984203,-0.00252212432863154,0.00268764151071733));
#25037=CARTESIAN_POINT('',(-0.00759439713481167,-0.00295555190144711,-0.000433461001706967));
#25038=CARTESIAN_POINT('',(-0.00731887657567663,-0.0031722656878549,-0.00207287188664212));
#25039=CARTESIAN_POINT('',(-0.00584663683306912,-0.00360569326067047,-0.00486616680699417));
#25040=CARTESIAN_POINT('',(-0.00464991764959665,-0.00382240704707826,-0.00602005084241106));
#25041=CARTESIAN_POINT('',(-0.0018048361440574,-0.00425583461989383,-0.00738954105186203));
#25042=CARTESIAN_POINT('',(-0.000156473821990613,-0.00447254840630161,-0.00760514722589611));
#25043=CARTESIAN_POINT('',(0.00294512710098485,-0.00490597597911718,-0.00701348520662646));
#25044=CARTESIAN_POINT('',(0.00439836570189353,-0.00512268976552496,-0.00620621701332274));
#25045=CARTESIAN_POINT('',(0.00653951261541697,-0.00555611733834051,-0.00388555286234104));
#25046=CARTESIAN_POINT('',(0.00722742092803173,-0.00577283112474829,-0.00237215690466308));
#25047=CARTESIAN_POINT('',(0.00756799437922453,-0.00620625869756383,0.000766950627123334));
#25048=CARTESIAN_POINT('',(0.00722065951780256,-0.0064229724839716,0.00239266220123177));
#25049=CARTESIAN_POINT('',(0.00562702550518511,-0.00685640005678713,0.00511852883999097));
#25050=CARTESIAN_POINT('',(0.00438072635398963,-0.00707311384319489,0.00621868390464173));
#25051=CARTESIAN_POINT('',(0.00147819074810594,-0.0075065414160104,0.00746174341684272));
#25052=CARTESIAN_POINT('',(-0.000178045706582278,-0.00772325520241815,0.00760464786439295));
#25053=CARTESIAN_POINT('',(-0.00325066452296928,-0.00815668277523364,0.00687723555833265));
#25054=CARTESIAN_POINT('',(-0.00466704688466808,-0.00837339656164138,0.00600691880472212));
#25055=CARTESIAN_POINT('',(-0.00670396992175478,-0.00880682413445684,0.00359417374225892));
#25056=CARTESIAN_POINT('',(-0.0073245105971427,-0.00902353792086456,0.00205174543340624));
#25057=CARTESIAN_POINT('',(-0.00749599839197253,-0.00939029068848216,-0.000613992984883923));
#25058=CARTESIAN_POINT('',(-0.00731728162491385,-0.00954032966969203,-0.0017202493791354));
#25059=CARTESIAN_POINT('',(-0.0069163376767793,-0.0096903686509019,-0.00273838893407139));
#25060=CARTESIAN_POINT('',(0.00720667440087568,0.000592348969728383,-0.000424458233565662));
#25061=CARTESIAN_POINT('',(0.00727482465560353,0.000422306321609296,0.000776807234323083));
#25062=CARTESIAN_POINT('',(0.0070427863991571,0.000252263673490207,0.00199589393390264));
#25063=CARTESIAN_POINT('',(0.00587544349289022,-0.000134492761036654,0.00446757215919429));
#25064=CARTESIAN_POINT('',(0.00476459521801765,-0.000351206547444426,0.0056375230913438));
#25065=CARTESIAN_POINT('',(0.00206495921718051,-0.000784634120259979,0.00708674107282344));
#25066=CARTESIAN_POINT('',(0.000476171491215957,-0.00100134790666776,0.00736600812215358));
#25067=CARTESIAN_POINT('',(-0.00255586725830238,-0.00143477547948332,0.00692470836860393));
#25068=CARTESIAN_POINT('',(-0.00399911828185615,-0.0016514892658911,0.00620414156572414));
#25069=CARTESIAN_POINT('',(-0.00617381884110776,-0.00208491683870668,0.00404578831672229));
#25070=CARTESIAN_POINT('',(-0.0069052683768056,-0.00230163062511446,0.00260800187060023));
#25071=CARTESIAN_POINT('',(-0.00736936152187336,-0.00273505819793004,-0.000420616774512569));
#25072=CARTESIAN_POINT('',(-0.00710200513124326,-0.00295177198433782,-0.0020114489735033));
#25073=CARTESIAN_POINT('',(-0.00567339049369526,-0.0033851995571534,-0.00472197355364789));
#25074=CARTESIAN_POINT('',(-0.00451213224677736,-0.00360191334356118,-0.00584166593480174));
#25075=CARTESIAN_POINT('',(-0.00175135561087993,-0.00403534091637675,-0.00717057569221339));
#25076=CARTESIAN_POINT('',(-0.000151837221900407,-0.00425205470278453,-0.00737979306847119));
#25077=CARTESIAN_POINT('',(0.00285785770084859,-0.0046854822756001,-0.00680566305638989));
#25078=CARTESIAN_POINT('',(0.00426803423461806,-0.00490219606200788,-0.00602231566805079));
#25079=CARTESIAN_POINT('',(0.00634573512345747,-0.00533562363482344,-0.00377041695958807));
#25080=CARTESIAN_POINT('',(0.0070132594785274,-0.00555233742123121,-0.00230186563946444));
#25081=CARTESIAN_POINT('',(0.00734374112730596,-0.00598576499404675,0.000744224503982232));
#25082=CARTESIAN_POINT('',(0.0070066984210146,-0.00620247878045452,0.00232176332730528));
#25083=CARTESIAN_POINT('',(0.00546028664348213,-0.00663590635327005,0.00496685764682014));
#25084=CARTESIAN_POINT('',(0.00425091757224103,-0.00685262013967781,0.00603441314301194));
#25085=CARTESIAN_POINT('',(0.00143438930407625,-0.00728604771249332,0.00724063857157453));
#25086=CARTESIAN_POINT('',(-0.000172769892847421,-0.00750276149890108,0.00737930850394532));
#25087=CARTESIAN_POINT('',(-0.00315434150082575,-0.00793618907171656,0.00667345072963354));
#25088=CARTESIAN_POINT('',(-0.00452875391188042,-0.0081529028581243,0.00582892302295097));
#25089=CARTESIAN_POINT('',(-0.00650531926473991,-0.00858633043093976,0.00348767192562512));
#25090=CARTESIAN_POINT('',(-0.00710747220654474,-0.00880304421734749,0.00199094853498184));
#25091=CARTESIAN_POINT('',(-0.00727387851033112,-0.00916979698496509,-0.000595799271118275));
#25092=CARTESIAN_POINT('',(-0.00710045744173322,-0.00931983596617496,-0.00166927530356775));
#25093=CARTESIAN_POINT('',(-0.00671139418215376,-0.00946987494738482,-0.0026572455567495));
#25094=CARTESIAN_POINT('',(0.00705106304263895,0.000656930080279598,-0.00041529304605117));
#25095=CARTESIAN_POINT('',(0.00711774175125379,0.000486887432160511,0.000760033890323187));
#25096=CARTESIAN_POINT('',(0.0068907138208246,0.000316844784041421,0.00195279725037364));
#25097=CARTESIAN_POINT('',(0.00574857696731766,-6.99116504854405E-5,0.00437110533787815));
#25098=CARTESIAN_POINT('',(0.00466171487514634,-0.000286625436893213,0.00551579390301966));
#25099=CARTESIAN_POINT('',(0.00202037122962695,-0.000720053009708766,0.00693371939562929));
#25100=CARTESIAN_POINT('',(0.000465889676278861,-0.000936766796116546,0.00720695632309743));
#25101=CARTESIAN_POINT('',(-0.00250067925431972,-0.00137019436893211,0.00677518541048322));
#25102=CARTESIAN_POINT('',(-0.00391276663157022,-0.00158690815533989,0.00607017757040086));
#25103=CARTESIAN_POINT('',(-0.00604050959443837,-0.00202033572815547,0.00395842893567034));
#25104=CARTESIAN_POINT('',(-0.00675616518005603,-0.00223704951456325,0.00255168814102218));
#25105=CARTESIAN_POINT('',(-0.00721023731395619,-0.00267047708737882,-0.000411534534364309));
#25106=CARTESIAN_POINT('',(-0.00694865386223869,-0.00288719087378661,-0.00196801641510262));
#25107=CARTESIAN_POINT('',(-0.00555088683230826,-0.00332061844660218,-0.0046200135264054));
#25108=CARTESIAN_POINT('',(-0.00441470325409532,-0.00353733223300997,-0.00571552875696985));
#25109=CARTESIAN_POINT('',(-0.00171353916320867,-0.00397075980582554,-0.00701574380156087));
#25110=CARTESIAN_POINT('',(-0.000148558650534957,-0.00418747359223332,-0.00722044361558744));
#25111=CARTESIAN_POINT('',(0.00279614891622217,-0.00462090116504889,-0.00665871060467684));
#25112=CARTESIAN_POINT('',(0.00417587597030559,-0.00483761495145667,-0.00589227777973966));
#25113=CARTESIAN_POINT('',(0.00620871374485157,-0.00527104252427223,-0.00368900358199341));
#25114=CARTESIAN_POINT('',(0.00686182446531413,-0.00548775631068,-0.00225216220918432));
#25115=CARTESIAN_POINT('',(0.00718517013217121,-0.00592118388349554,0.000728154708199079));
#25116=CARTESIAN_POINT('',(0.00685540507856572,-0.00613789766990331,0.00227163025277339));
#25117=CARTESIAN_POINT('',(0.00534238446368462,-0.00657132524271884,0.00485960991761841));
#25118=CARTESIAN_POINT('',(0.004159128902409,-0.0067880390291266,0.00590411403788912));
#25119=CARTESIAN_POINT('',(0.00140341700597708,-0.00722146660194211,0.00708429383613219));
#25120=CARTESIAN_POINT('',(-0.000169039329179231,-0.00743818038834986,0.00721996951410456));
#25121=CARTESIAN_POINT('',(-0.00308623083868367,-0.00787160796116534,0.00652935309535745));
#25122=CARTESIAN_POINT('',(-0.00443096601303181,-0.00808832174757308,0.00570306099863799));
#25123=CARTESIAN_POINT('',(-0.00636485203807753,-0.00852174932038855,0.00341236376887466));
#25124=CARTESIAN_POINT('',(-0.00695400288877511,-0.00873846310679627,0.0019479586358308));
#25125=CARTESIAN_POINT('',(-0.00711681603578613,-0.00910521587441387,-0.000582934372739653));
#25126=CARTESIAN_POINT('',(-0.00694713959148096,-0.00925525485562374,-0.00163323118906917));
#25127=CARTESIAN_POINT('',(-0.00656647724734397,-0.00940529383683361,-0.00259986852439682));
#25128=CARTESIAN_POINT('',(0.00673984032616548,0.000656930080279598,-0.000396962671022186));
#25129=CARTESIAN_POINT('',(0.00680357594255429,0.000486887432160511,0.000726487202323393));
#25130=CARTESIAN_POINT('',(0.00658656866415959,0.000316844784041421,0.00186660388331565));
#25131=CARTESIAN_POINT('',(0.00549484391617253,-6.99116504854403E-5,0.00417817169524589));
#25132=CARTESIAN_POINT('',(0.00445595418940373,-0.000286625436893212,0.00527233552637138));
#25133=CARTESIAN_POINT('',(0.00193119525451979,-0.000720053009708766,0.00662767604124101));
#25134=CARTESIAN_POINT('',(0.000445326046404666,-0.000936766796116546,0.00688885272498515));
#25135=CARTESIAN_POINT('',(-0.00239030324635441,-0.00137019436893211,0.0064761394942418));
#25136=CARTESIAN_POINT('',(-0.00374006333099836,-0.00158690815533989,0.00580224957975431));
#25137=CARTESIAN_POINT('',(-0.00577389110109959,-0.00202033572815547,0.00378371017356644));
#25138=CARTESIAN_POINT('',(-0.00645795878655688,-0.00223704951456325,0.00243906068186606));
#25139=CARTESIAN_POINT('',(-0.00689198889812187,-0.00267047708737883,-0.000393370054067794));
#25140=CARTESIAN_POINT('',(-0.00664195132422956,-0.00288719087378661,-0.00188115129830126));
#25141=CARTESIAN_POINT('',(-0.00530587950953425,-0.00332061844660218,-0.0044160934719204));
#25142=CARTESIAN_POINT('',(-0.00421984526873124,-0.00353733223300997,-0.00546325440130608));
#25143=CARTESIAN_POINT('',(-0.00163790626786615,-0.00397075980582554,-0.00670608002025585));
#25144=CARTESIAN_POINT('',(-0.000142001507804063,-0.00418747359223332,-0.00690174470981995));
#25145=CARTESIAN_POINT('',(0.00267273134696934,-0.00462090116504889,-0.00636480570125073));
#25146=CARTESIAN_POINT('',(0.00399155944168066,-0.00483761495145667,-0.00563220200311741));
#25147=CARTESIAN_POINT('',(0.00593467098763978,-0.00527104252427223,-0.00352617682680408));
#25148=CARTESIAN_POINT('',(0.0065589544388876,-0.00548775631068,-0.00215275534862407));
#25149=CARTESIAN_POINT('',(0.00686802814190169,-0.00592118388349554,0.000696015116632777));
#25150=CARTESIAN_POINT('',(0.00655281839366796,-0.00613789766990331,0.0021713641037096));
#25151=CARTESIAN_POINT('',(0.0051065801040896,-0.00657132524271884,0.00464511445921495));
#25152=CARTESIAN_POINT('',(0.00397555156274497,-0.0067880390291266,0.00564351582764347));
#25153=CARTESIAN_POINT('',(0.00134147240977874,-0.00722146660194211,0.00677160436524751));
#25154=CARTESIAN_POINT('',(-0.000161578201842847,-0.00743818038834986,0.00690129153442303));
#25155=CARTESIAN_POINT('',(-0.00295000951439953,-0.00787160796116534,0.0062411578268053));
#25156=CARTESIAN_POINT('',(-0.00423539021533461,-0.00808832174757308,0.00545133695001203));
#25157=CARTESIAN_POINT('',(-0.00608391758475277,-0.00852174932038855,0.00326174745537375));
#25158=CARTESIAN_POINT('',(-0.00664706425323584,-0.00873846310679627,0.00186197883752873));
#25159=CARTESIAN_POINT('',(-0.00680269108669614,-0.00910521587441387,-0.000557204575982392));
#25160=CARTESIAN_POINT('',(-0.00664050389097645,-0.00925525485562374,-0.00156114296007199));
#25161=CARTESIAN_POINT('',(-0.0062766433777244,-0.00940529383683361,-0.00248511445969145));
#25162=CARTESIAN_POINT('',(0.00658422896792875,0.000592348969728383,-0.000387797483507693));
#25163=CARTESIAN_POINT('',(0.00664649303820454,0.000422306321609297,0.000709713858323498));
#25164=CARTESIAN_POINT('',(0.00643449608582708,0.000252263673490207,0.00182350719978666));
#25165=CARTESIAN_POINT('',(0.00536797739059997,-0.000134492761036653,0.00408170487392976));
#25166=CARTESIAN_POINT('',(0.00435307384653242,-0.000351206547444425,0.00515060633804724));
#25167=CARTESIAN_POINT('',(0.00188660726696621,-0.000784634120259978,0.00647465436404687));
#25168=CARTESIAN_POINT('',(0.000435044231467567,-0.00100134790666776,0.00672980092592901));
#25169=CARTESIAN_POINT('',(-0.00233511524237175,-0.00143477547948332,0.00632661653612109));
#25170=CARTESIAN_POINT('',(-0.00365371168071242,-0.0016514892658911,0.00566828558443103));
#25171=CARTESIAN_POINT('',(-0.0056405818544302,-0.00208491683870668,0.00369635079251449));
#25172=CARTESIAN_POINT('',(-0.00630885558980731,-0.00230163062511446,0.00238274695228799));
#25173=CARTESIAN_POINT('',(-0.00673286469020471,-0.00273505819793004,-0.000384287813919537));
#25174=CARTESIAN_POINT('',(-0.00648860005522499,-0.00295177198433782,-0.00183771873990058));
#25175=CARTESIAN_POINT('',(-0.00518337584814724,-0.0033851995571534,-0.00431413344467791));
#25176=CARTESIAN_POINT('',(-0.00412241627604921,-0.00360191334356118,-0.00533711722347419));
#25177=CARTESIAN_POINT('',(-0.0016000898201949,-0.00403534091637675,-0.00655124812960334));
#25178=CARTESIAN_POINT('',(-0.000138722936438619,-0.00425205470278453,-0.00674239525693621));
#25179=CARTESIAN_POINT('',(0.00261102256234292,-0.0046854822756001,-0.00621785324953768));
#25180=CARTESIAN_POINT('',(0.00389940117736819,-0.00490219606200788,-0.00550216411480628));
#25181=CARTESIAN_POINT('',(0.0057976496090339,-0.00533562363482344,-0.00344476344920941));
#25182=CARTESIAN_POINT('',(0.00640751942567434,-0.00555233742123121,-0.00210305191834393));
#25183=CARTESIAN_POINT('',(0.00670945714676693,-0.00598576499404675,0.000679945320849626));
#25184=CARTESIAN_POINT('',(0.00640152505121908,-0.00620247878045452,0.00212123102917771));
#25185=CARTESIAN_POINT('',(0.00498867792429209,-0.00663590635327005,0.00453786673001321));
#25186=CARTESIAN_POINT('',(0.00388376289291295,-0.00685262013967781,0.00551321672252064));
#25187=CARTESIAN_POINT('',(0.00131050011167958,-0.00728604771249332,0.00661525962980517));
#25188=CARTESIAN_POINT('',(-0.000157847638174654,-0.00750276149890107,0.00674195254458227));
#25189=CARTESIAN_POINT('',(-0.00288189885225745,-0.00793618907171656,0.00609706019252921));
#25190=CARTESIAN_POINT('',(-0.00413760231648601,-0.0081529028581243,0.00532547492569905));
#25191=CARTESIAN_POINT('',(-0.00594345035809039,-0.00858633043093976,0.0031864392986233));
#25192=CARTESIAN_POINT('',(-0.00649359493546621,-0.00880304421734749,0.00181898893837771));
#25193=CARTESIAN_POINT('',(-0.00664562861215114,-0.00916979698496509,-0.000544339677603755));
#25194=CARTESIAN_POINT('',(-0.0064871860407242,-0.00931983596617496,-0.0015250988455734));
#25195=CARTESIAN_POINT('',(-0.00613172644291462,-0.00946987494738482,-0.00242773742733876));
#25196=CARTESIAN_POINT('',(0.00636416127465107,0.000371855266211312,-0.000374835951023005));
#25197=CARTESIAN_POINT('',(0.00642434426445617,0.000201812618092225,0.000685992767752494));
#25198=CARTESIAN_POINT('',(0.00621943298308421,3.17699699731348E-5,0.00176255928544665));
#25199=CARTESIAN_POINT('',(0.0051885610295241,-0.000354986464553727,0.00394528018690546));
#25200=CARTESIAN_POINT('',(0.00420757907034223,-0.0005717002509615,0.00497845526898257));
#25201=CARTESIAN_POINT('',(0.00182355033024902,-0.00100512782377705,0.00625824903282183));
#25202=CARTESIAN_POINT('',(0.000420503549337712,-0.00122184161018483,0.00650486771458397));
#25203=CARTESIAN_POINT('',(-0.00225706761865918,-0.0016552691830004,0.00611515914086064));
#25204=CARTESIAN_POINT('',(-0.00353159200574477,-0.00187198296940818,0.00547883188537516));
#25205=CARTESIAN_POINT('',(-0.00545205410980061,-0.00230541054222375,0.00357280597103028));
#25206=CARTESIAN_POINT('',(-0.00609799182677088,-0.00252212432863154,0.00230310731217089));
#25207=CARTESIAN_POINT('',(-0.00650782907726638,-0.00295555190144711,-0.00037144358672514));
#25208=CARTESIAN_POINT('',(-0.00627172861079161,-0.0031722656878549,-0.00177629582676177));
#25209=CARTESIAN_POINT('',(-0.00501012950877337,-0.00360569326067047,-0.00416994019133164));
#25210=CARTESIAN_POINT('',(-0.00398463087322989,-0.00382240704707826,-0.00515873231586488));
#25211=CARTESIAN_POINT('',(-0.0015466092870174,-0.00425583461989383,-0.0063322827699547));
#25212=CARTESIAN_POINT('',(-0.000134086336348388,-0.00447254840630161,-0.00651704109951128));
#25213=CARTESIAN_POINT('',(0.00252375316220668,-0.00490597597911718,-0.0060100310993011));
#25214=CARTESIAN_POINT('',(0.00376906971009273,-0.00512268976552496,-0.00531826276953433));
#25215=CARTESIAN_POINT('',(0.00560387211707439,-0.00555611733834051,-0.00332962754645643));
#25216=CARTESIAN_POINT('',(0.00619335797617,-0.00577283112474829,-0.00203276065314531));
#25217=CARTESIAN_POINT('',(0.00648520389484837,-0.00620625869756383,0.000657219197708529));
#25218=CARTESIAN_POINT('',(0.00618756395443112,-0.0064229724839716,0.00205033215525123));
#25219=CARTESIAN_POINT('',(0.0048219390625891,-0.00685640005678713,0.00438619553684241));
#25220=CARTESIAN_POINT('',(0.00375395411116433,-0.00707311384319489,0.00532894596089087));
#25221=CARTESIAN_POINT('',(0.00126669866764988,-0.0075065414160104,0.00639415478453698));
#25222=CARTESIAN_POINT('',(-0.000152571824439798,-0.00772325520241815,0.00651661318413464));
#25223=CARTESIAN_POINT('',(-0.00278557583011391,-0.00815668277523364,0.0058932753638301));
#25224=CARTESIAN_POINT('',(-0.00399930934369835,-0.00837339656164138,0.00514747914392789));
#25225=CARTESIAN_POINT('',(-0.00574479970107553,-0.00880682413445684,0.00307993748198948));
#25226=CARTESIAN_POINT('',(-0.00627655654486826,-0.00902353792086456,0.00175819203995327));
#25227=CARTESIAN_POINT('',(-0.00642350873050973,-0.00939029068848216,-0.000526145963838135));
#25228=CARTESIAN_POINT('',(-0.00627036185754357,-0.00954032966969203,-0.00147412477000577));
#25229=CARTESIAN_POINT('',(-0.00592678294828908,-0.0096903686509019,-0.00234659405001688));
#25230=CARTESIAN_POINT('',(0.00629970493961011,0.000215942673245455,-0.00037103960605281));
#25231=CARTESIAN_POINT('',(0.00635927839505755,4.59000251263669E-5,0.000679045021181388));
#25232=CARTESIAN_POINT('',(0.00615644245867384,-0.000124142622992724,0.00174470805463564));
#25233=CARTESIAN_POINT('',(0.00513601119402079,-0.000510899057519587,0.00390532232119729));
#25234=CARTESIAN_POINT('',(0.00416496463702333,-0.000727612843927361,0.00492803338824205));
#25235=CARTESIAN_POINT('',(0.00180508138108541,-0.00116104041674292,0.00619486537879095));
#25236=CARTESIAN_POINT('',(0.000416244682144955,-0.0013777542031507,0.00643898630229508));
#25237=CARTESIAN_POINT('',(-0.00223420799892928,-0.00181118177596627,0.00605322470372089));
#25238=CARTESIAN_POINT('',(-0.00349582398106305,-0.00202789556237404,0.00542334218164256));
#25239=CARTESIAN_POINT('',(-0.00539683561184042,-0.00246132313518961,0.00353662053059804));
#25240=CARTESIAN_POINT('',(-0.00603623126048403,-0.0026780369215974,0.00227978140163184));
#25241=CARTESIAN_POINT('',(-0.00644191767224522,-0.00311146449441298,-0.000367681599679002));
#25242=CARTESIAN_POINT('',(-0.0062082084353628,-0.00332817828082076,-0.00175830547202365));
#25243=CARTESIAN_POINT('',(-0.0049593868307865,-0.00376160585363634,-0.00412770696522788));
#25244=CARTESIAN_POINT('',(-0.00394427446309262,-0.00397831964004412,-0.00510648458608746));
#25245=CARTESIAN_POINT('',(-0.00153094520151117,-0.00441174721285968,-0.00626814930095857));
#25246=CARTESIAN_POINT('',(-0.0001327283076236,-0.00462846099926747,-0.00645103639497011));
#25247=CARTESIAN_POINT('',(0.00249819254669685,-0.00506188857208303,-0.00594916140077757));
#25248=CARTESIAN_POINT('',(0.00373089650712975,-0.00527860235849082,-0.0052643993125735));
#25249=CARTESIAN_POINT('',(0.00554711600372078,-0.00571202993130638,-0.00329590502129811));
#25250=CARTESIAN_POINT('',(0.00613063153987892,-0.00592874371771416,-0.00201217281822681));
#25251=CARTESIAN_POINT('',(0.00641952163806455,-0.0063621712905297,0.000650562870350582));
#25252=CARTESIAN_POINT('',(0.00612489620009204,-0.00657888507693745,0.00202956635585666));
#25253=CARTESIAN_POINT('',(0.00477310238068363,-0.00701231264975299,0.00434177207287334));
#25254=CARTESIAN_POINT('',(0.00371593399924772,-0.00722902643616076,0.00527497430438392));
#25255=CARTESIAN_POINT('',(0.00125386952171934,-0.00766245400897627,0.00632939467471113));
#25256=CARTESIAN_POINT('',(-0.000151026574373135,-0.00787916779538401,0.00645061281352776));
#25257=CARTESIAN_POINT('',(-0.00275736347011246,-0.0083125953681995,0.00583358816940705));
#25258=CARTESIAN_POINT('',(-0.0039588042697593,-0.00852930915460724,0.00509534538646971));
#25259=CARTESIAN_POINT('',(-0.00568661627072304,-0.0089627367274227,0.00304874382210612));
#25260=CARTESIAN_POINT('',(-0.00621298747203994,-0.00917945051383042,0.00174038504067986));
#25261=CARTESIAN_POINT('',(-0.00635845132341332,-0.00954620328144802,-0.000520817148451154));
#25262=CARTESIAN_POINT('',(-0.0062068555246152,-0.00969624226265789,-0.00145919480893673));
#25263=CARTESIAN_POINT('',(-0.00586675638847333,-0.00984628124386776,-0.00232282770504767));
#25264=CARTESIAN_POINT('',(0.00629970493961011,5.62796276089674E-5,-0.000371039606052811));
#25265=CARTESIAN_POINT('',(0.00635927839505755,-0.000113763020510121,0.000679045021181388));
#25266=CARTESIAN_POINT('',(0.00615644245867384,-0.000283805668629212,0.00174470805463564));
#25267=CARTESIAN_POINT('',(0.00513601119402079,-0.000670562103156075,0.00390532232119729));
#25268=CARTESIAN_POINT('',(0.00416496463702333,-0.000887275889563849,0.00492803338824204));
#25269=CARTESIAN_POINT('',(0.00180508138108541,-0.00132070346237941,0.00619486537879094));
#25270=CARTESIAN_POINT('',(0.000416244682144954,-0.00153741724878719,0.00643898630229508));
#25271=CARTESIAN_POINT('',(-0.00223420799892927,-0.00197084482160275,0.0060532247037209));
#25272=CARTESIAN_POINT('',(-0.00349582398106304,-0.00218755860801054,0.00542334218164257));
#25273=CARTESIAN_POINT('',(-0.00539683561184041,-0.00262098618082611,0.00353662053059805));
#25274=CARTESIAN_POINT('',(-0.00603623126048402,-0.00283769996723389,0.00227978140163185));
#25275=CARTESIAN_POINT('',(-0.00644191767224522,-0.00327112754004947,-0.000367681599679004));
#25276=CARTESIAN_POINT('',(-0.00620820843536279,-0.00348784132645725,-0.00175830547202365));
#25277=CARTESIAN_POINT('',(-0.00495938683078651,-0.00392126889927283,-0.00412770696522788));
#25278=CARTESIAN_POINT('',(-0.00394427446309264,-0.00413798268568061,-0.00510648458608745));
#25279=CARTESIAN_POINT('',(-0.00153094520151119,-0.00457141025849618,-0.00626814930095856));
#25280=CARTESIAN_POINT('',(-0.000132728307623607,-0.00478812404490397,-0.00645103639497011));
#25281=CARTESIAN_POINT('',(0.00249819254669686,-0.00522155161771953,-0.00594916140077758));
#25282=CARTESIAN_POINT('',(0.00373089650712975,-0.00543826540412731,-0.0052643993125735));
#25283=CARTESIAN_POINT('',(0.00554711600372077,-0.00587169297694287,-0.00329590502129811));
#25284=CARTESIAN_POINT('',(0.00613063153987892,-0.00608840676335064,-0.00201217281822681));
#25285=CARTESIAN_POINT('',(0.00641952163806455,-0.00652183433616618,0.000650562870350582));
#25286=CARTESIAN_POINT('',(0.00612489620009204,-0.00673854812257395,0.00202956635585666));
#25287=CARTESIAN_POINT('',(0.00477310238068363,-0.00717197569538948,0.00434177207287333));
#25288=CARTESIAN_POINT('',(0.00371593399924772,-0.00738868948179724,0.00527497430438391));
#25289=CARTESIAN_POINT('',(0.00125386952171934,-0.00782211705461275,0.00632939467471113));
#25290=CARTESIAN_POINT('',(-0.000151026574373135,-0.0080388308410205,0.00645061281352777));
#25291=CARTESIAN_POINT('',(-0.00275736347011246,-0.00847225841383599,0.00583358816940706));
#25292=CARTESIAN_POINT('',(-0.0039588042697593,-0.00868897220024372,0.00509534538646972));
#25293=CARTESIAN_POINT('',(-0.00568661627072304,-0.00912239977305918,0.00304874382210612));
#25294=CARTESIAN_POINT('',(-0.00621298747203993,-0.00933911355946691,0.00174038504067986));
#25295=CARTESIAN_POINT('',(-0.00635845132341332,-0.0097058663270845,-0.000520817148451154));
#25296=CARTESIAN_POINT('',(-0.00620685552461521,-0.00985590530829437,-0.00145919480893672));
#25297=CARTESIAN_POINT('',(-0.00586675638847333,-0.0100059442895042,-0.00232282770504767));
#25298=CARTESIAN_POINT('',(0.00629974223632648,5.25291749383375E-5,-0.000371041802752352));
#25299=CARTESIAN_POINT('',(0.00635931604447206,-0.000117513473180751,0.000679049041393414));
#25300=CARTESIAN_POINT('',(0.0061564789072203,-0.000287556121299842,0.00174471838398949));
#25301=CARTESIAN_POINT('',(0.00513604160121519,-0.000674312555826705,0.00390534544223238));
#25302=CARTESIAN_POINT('',(0.00416498929524245,-0.000891026342234479,0.00492806256412651));
#25303=CARTESIAN_POINT('',(0.00180509206787296,-0.00132445391505004,0.00619490205481612));
#25304=CARTESIAN_POINT('',(0.00041624714647622,-0.00154116770145782,0.00643902442361157));
#25305=CARTESIAN_POINT('',(-0.00223422122631418,-0.00197459527427338,0.0060532605411779));
#25306=CARTESIAN_POINT('',(-0.00349584467770784,-0.00219130906068117,0.00542337428994876));
#25307=CARTESIAN_POINT('',(-0.00539686756321734,-0.00262473663349674,0.00353664146877437));
#25308=CARTESIAN_POINT('',(-0.00603626699733319,-0.00284145041990452,0.00227979489882912));
#25309=CARTESIAN_POINT('',(-0.00644195581091657,-0.0032748779927201,-0.000367683776497834));
#25310=CARTESIAN_POINT('',(-0.00620824519038408,-0.00349159177912788,-0.00175831588187953));
#25311=CARTESIAN_POINT('',(-0.00495941619229562,-0.00392501935194346,-0.004127731402867));
#25312=CARTESIAN_POINT('',(-0.00394429781473964,-0.00414173313835124,-0.00510651481847279));
#25313=CARTESIAN_POINT('',(-0.00153095426530537,-0.00457516071116681,-0.00626818641085321));
#25314=CARTESIAN_POINT('',(-0.000132729093427084,-0.0047918744975746,-0.00645107458762786));
#25315=CARTESIAN_POINT('',(0.00249820733697351,-0.00522530207039016,-0.00594919662213914));
#25316=CARTESIAN_POINT('',(0.00373091859549582,-0.00544201585679794,-0.00526443047987576));
#25317=CARTESIAN_POINT('',(0.00554714884481638,-0.0058754434296135,-0.00329592453434451));
#25318=CARTESIAN_POINT('',(0.00613066783561465,-0.00609215721602127,-0.00201218473107663));
#25319=CARTESIAN_POINT('',(0.00641955964414262,-0.00652558478883681,0.000650566721937138));
#25320=CARTESIAN_POINT('',(0.00612493246187232,-0.00674229857524458,0.00202957837168303));
#25321=CARTESIAN_POINT('',(0.00477313063931596,-0.00717572614806011,0.00434179777786159));
#25322=CARTESIAN_POINT('',(0.00371595599902989,-0.00739243993446787,0.00527500553429426));
#25323=CARTESIAN_POINT('',(0.00125387694511716,-0.00782586750728338,0.00632943214720234));
#25324=CARTESIAN_POINT('',(-0.000151027468509505,-0.00804258129369113,0.00645065100367775));
#25325=CARTESIAN_POINT('',(-0.0027573797947823,-0.00847600886650662,0.0058336227065299));
#25326=CARTESIAN_POINT('',(-0.00395882770742843,-0.00869272265291435,0.00509537555290664));
#25327=CARTESIAN_POINT('',(-0.00568664993771477,-0.00912615022572981,0.00304876187186157));
#25328=CARTESIAN_POINT('',(-0.00621302425535498,-0.00934286401213754,0.00174039534443977));
#25329=CARTESIAN_POINT('',(-0.00635848896793125,-0.00970961677975513,-0.000520820231892307));
#25330=CARTESIAN_POINT('',(-0.00620689227162673,-0.009859655760965,-0.00145920344794052));
#25331=CARTESIAN_POINT('',(-0.005866791121965,-0.0100096947421749,-0.00232284145709589));
#25332=CARTESIAN_POINT('',(0.0062998165669852,4.87793578883542E-5,-0.000371046180674587));
#25333=CARTESIAN_POINT('',(0.00635939107804215,-0.000121263290230734,0.000679057053493061));
#25334=CARTESIAN_POINT('',(0.00615655154751501,-0.000291305938349825,0.00174473896992172));
#25335=CARTESIAN_POINT('',(0.0051361022013701,-0.000678062372876689,0.0039053915214033));
#25336=CARTESIAN_POINT('',(0.00416503843795119,-0.000894776159284463,0.00492812071033677));
#25337=CARTESIAN_POINT('',(0.00180511336615429,-0.00132820373210002,0.00619497514846554));
#25338=CARTESIAN_POINT('',(0.000416252057776306,-0.0015449175185078,0.00643910039766082));
#25339=CARTESIAN_POINT('',(-0.00223424758789045,-0.00197834509132337,0.0060533319635991));
#25340=CARTESIAN_POINT('',(-0.00349588592517923,-0.00219505887773115,0.00542343828034207));
#25341=CARTESIAN_POINT('',(-0.00539693124085779,-0.00262848645054672,0.00353668319760711));
#25342=CARTESIAN_POINT('',(-0.00603633821924757,-0.0028452002369545,0.00227982179812916));
#25343=CARTESIAN_POINT('',(-0.00644203181955326,-0.00327862780977008,-0.000367688114798717));
#25344=CARTESIAN_POINT('',(-0.00620831844146915,-0.00349534159617787,-0.00175833662824864));
#25345=CARTESIAN_POINT('',(-0.00495947470844733,-0.00392876916899344,-0.00412778010596988));
#25346=CARTESIAN_POINT('',(-0.0039443443535096,-0.00414548295540122,-0.00510657507024119));
#25347=CARTESIAN_POINT('',(-0.00153097232903477,-0.00457891052821679,-0.00626826036918475));
#25348=CARTESIAN_POINT('',(-0.000132730659497659,-0.00479562431462458,-0.006451150703857));
#25349=CARTESIAN_POINT('',(0.00249823681332191,-0.00522905188744014,-0.00594926681671015));
#25350=CARTESIAN_POINT('',(0.00373096261660437,-0.00544576567384792,-0.00526449259489105));
#25351=CARTESIAN_POINT('',(0.00554721429562567,-0.00587919324666348,-0.00329596342295813));
#25352=CARTESIAN_POINT('',(0.00613074017136452,-0.00609590703307125,-0.0020122084728443));
#25353=CARTESIAN_POINT('',(0.00641963538852694,-0.00652933460588679,0.000650574397973898));
#25354=CARTESIAN_POINT('',(0.00612500472995051,-0.00674604839229456,0.00202960231867826));
#25355=CARTESIAN_POINT('',(0.00477318695748443,-0.00717947596511009,0.00434184900673363));
#25356=CARTESIAN_POINT('',(0.00371599984359477,-0.00739618975151785,0.00527506777408462));
#25357=CARTESIAN_POINT('',(0.00125389173961125,-0.00782961732433336,0.00632950682817232));
#25358=CARTESIAN_POINT('',(-0.000151029250482608,-0.00804633111074111,0.00645072711490902));
#25359=CARTESIAN_POINT('',(-0.00275741232910654,-0.0084797586835566,0.00583369153744429));
#25360=CARTESIAN_POINT('',(-0.0039588744176366,-0.00869647246996433,0.00509543567324285));
#25361=CARTESIAN_POINT('',(-0.00568671703449746,-0.00912990004277979,0.00304879784420294));
#25362=CARTESIAN_POINT('',(-0.00621309756282825,-0.00934661382918752,0.00174041587936446));
#25363=CARTESIAN_POINT('',(-0.00635856399174266,-0.00971336659680511,-0.000520826377050229));
#25364=CARTESIAN_POINT('',(-0.00620696550674872,-0.00986340557801498,-0.00145922066508202));
#25365=CARTESIAN_POINT('',(-0.00586686034423352,-0.0100134445592248,-0.00232286886430227));
#25366=CARTESIAN_POINT('',(0.00750327656949163,-8.53080492016359E-9,5.83924176101713E-10));
#25367=CARTESIAN_POINT('',(0.00750328356622613,0.000155908244795296,8.91110510665626E-10));
#25368=CARTESIAN_POINT('',(0.00737416840995134,0.000467747108013051,1.49443482527523E-9));
#25369=CARTESIAN_POINT('',(0.00690656929314086,0.000661501357346462,2.2553121146952E-9));
#25370=CARTESIAN_POINT('',(0.0064389701765613,0.000467746857475072,2.88847076502633E-9));
#25371=CARTESIAN_POINT('',(0.00630985502057318,0.000155907827228039,3.33264413512018E-9));
#25372=CARTESIAN_POINT('',(0.006309862017394,-9.03188821051637E-9,3.5909752516927E-9));
#25373=CARTESIAN_POINT('',(-0.00600466497160202,0.00989161658584234,0.00195123602046633));
#25374=CARTESIAN_POINT('',(-0.00574414092335559,0.010028972165006,0.00275296354617664));
#25375=CARTESIAN_POINT('',(-0.00532095763677864,0.0101627934786023,0.00350161061675348));
#25376=CARTESIAN_POINT('',(-0.00421610368672497,0.0104233675746601,0.00477472643696357));
#25377=CARTESIAN_POINT('',(-0.00353443302324826,0.0105501203571216,0.00529919518659681));
#25378=CARTESIAN_POINT('',(-0.00202056207538,0.0107965573909099,0.00604079260745369));
#25379=CARTESIAN_POINT('',(-0.00118836179098845,0.0109162416422367,0.00625792127867733));
#25380=CARTESIAN_POINT('',(0.000494835703082955,0.0111485416137555,0.00635050111591244));
#25381=CARTESIAN_POINT('',(0.00134583291276282,0.0112611573339475,0.00622595228192391));
#25382=CARTESIAN_POINT('',(0.0029319010653021,0.0114793202431967,0.00565488463000731));
#25383=CARTESIAN_POINT('',(0.00366697200816151,0.0115848674322539,0.00520836581207923));
#25384=CARTESIAN_POINT('',(0.00490482050632797,0.0117888932792336,0.00406404847997765));
#25385=CARTESIAN_POINT('',(0.00540759806163502,0.0118873719371561,0.00336624996580416));
#25386=CARTESIAN_POINT('',(0.00610126561429382,0.0120772607218663,0.00182983996835635));
#25387=CARTESIAN_POINT('',(0.00629215561164556,0.012168670848654,0.000991228485082042));
#25388=CARTESIAN_POINT('',(0.00633182860310908,0.0123444225710946,-0.000694047966501003));
#25389=CARTESIAN_POINT('',(0.00618061159722085,0.0124287641667475,-0.00154071293480974));
#25390=CARTESIAN_POINT('',(0.00556000950518228,0.0125903788269186,-0.00310806215598619));
#25391=CARTESIAN_POINT('',(0.00509062441903194,0.0126676518914367,-0.00382874640885392));
#25392=CARTESIAN_POINT('',(0.00390799378434807,0.0128151294893382,-0.00503004381017692));
#25393=CARTESIAN_POINT('',(0.00319474823581453,0.0128853340227216,-0.00551065695863221));
#25394=CARTESIAN_POINT('',(0.00163730957094308,0.0130186745583536,-0.00615572684557856));
#25395=CARTESIAN_POINT('',(0.000793116454605152,0.0130818105606022,-0.00632018358406963));
#25396=CARTESIAN_POINT('',(-0.000892574732320377,0.0132010140339646,-0.00630690641188717));
#25397=CARTESIAN_POINT('',(-0.00173407280290798,0.0132570815050784,-0.00612917250121364));
#25398=CARTESIAN_POINT('',(-0.0032811564713131,0.0133621479161712,-0.0054596483638267));
#25399=CARTESIAN_POINT('',(-0.00398674206913061,0.0134111468561502,-0.00496785813711329));
#25400=CARTESIAN_POINT('',(-0.0051503049186267,0.0135020762049735,-0.00374808507395191));
#25401=CARTESIAN_POINT('',(-0.00560828217030528,0.0135440066138177,-0.00302010223750393));
#25402=CARTESIAN_POINT('',(-0.00620411058405509,0.0136207989003714,-0.00144315566807725));
#25403=CARTESIAN_POINT('',(-0.00634196174612631,0.0136556607780809,-0.000594191935098553));
#25404=CARTESIAN_POINT('',(-0.00627577492760283,0.013718316002365,0.00109019087403818));
#25405=CARTESIAN_POINT('',(-0.00607173694700813,0.0137461093489396,0.00192560995019621));
#25406=CARTESIAN_POINT('',(-0.00571279299028783,0.0137703684299469,0.0026883674746708));
#25407=CARTESIAN_POINT('',(-0.00600350244213178,0.00990699069817707,0.00195085825261618));
#25408=CARTESIAN_POINT('',(-0.00574302883248355,0.0100443462773407,0.00275243056036176));
#25409=CARTESIAN_POINT('',(-0.00531992747604663,0.010178167590937,0.00350093268958277));
#25410=CARTESIAN_POINT('',(-0.00421528743056271,0.0104387416869948,0.00477380202898718));
#25411=CARTESIAN_POINT('',(-0.00353374874151571,0.0105654944694564,0.00529816923917059));
#25412=CARTESIAN_POINT('',(-0.0020201708857016,0.0108119315032447,0.00603962308351473));
#25413=CARTESIAN_POINT('',(-0.0011881317189345,0.0109316157545714,0.00625670971767546));
#25414=CARTESIAN_POINT('',(0.000494739900720878,0.0111639157260902,0.0063492716310481));
#25415=CARTESIAN_POINT('',(0.00134557235360914,0.0112765314462822,0.00622474691026));
#25416=CARTESIAN_POINT('',(0.00293133343639884,0.0114946943555314,0.00565378981954506));
#25417=CARTESIAN_POINT('',(0.00366626206630027,0.0116002415445887,0.00520735744961822));
#25418=CARTESIAN_POINT('',(0.00490387091156926,0.0118042673915684,0.00406326166237021));
#25419=CARTESIAN_POINT('',(0.00540655112693682,0.0119027460494908,0.00336559824504905));
#25420=CARTESIAN_POINT('',(0.00610008438251554,0.012092634834201,0.00182948570331425));
#25421=CARTESIAN_POINT('',(0.0062909374227267,0.0121840449609887,0.000991036578900582));
#25422=CARTESIAN_POINT('',(0.0063306027333251,0.0123597966834293,-0.00069391359577114));
#25423=CARTESIAN_POINT('',(0.00617941500371233,0.0124441382790822,-0.0015404146460292));
#25424=CARTESIAN_POINT('',(0.00555893306296025,0.0126057529392533,-0.00310746042152328));
#25425=CARTESIAN_POINT('',(0.00508963885182094,0.0126830260037714,-0.0038280051467593));
#25426=CARTESIAN_POINT('',(0.00390723717961403,0.012830503601673,-0.00502906997163746));
#25427=CARTESIAN_POINT('',(0.00319412971854643,0.0129007081350563,-0.00550959007127961));
#25428=CARTESIAN_POINT('',(0.00163699258063019,0.0130340486706883,-0.00615453506986708));
#25429=CARTESIAN_POINT('',(0.000792962903781556,0.0130971846729369,-0.0063189599688124));
#25430=CARTESIAN_POINT('',(-0.000892401925938069,0.0132163881462993,-0.0063056853671487));
#25431=CARTESIAN_POINT('',(-0.00173373707880906,0.0132724556174131,-0.00612798586653968));
#25432=CARTESIAN_POINT('',(-0.00328052122503168,0.0133775220285059,-0.00545859135196174));
#25433=CARTESIAN_POINT('',(-0.00398597021838331,0.013426520968485,-0.00496689633799283));
#25434=CARTESIAN_POINT('',(-0.00514930779700927,0.0135174503173082,-0.00374735942824544));
#25435=CARTESIAN_POINT('',(-0.0056071963822836,0.0135593807261525,-0.00301951753246696));
#25436=CARTESIAN_POINT('',(-0.00620290944103967,0.0136361730127061,-0.00144287626681137));
#25437=CARTESIAN_POINT('',(-0.0063407339145214,0.0136710348904156,-0.00059407689693426));
#25438=CARTESIAN_POINT('',(-0.00627455991005623,0.0137336901146997,0.00108997980830424));
#25439=CARTESIAN_POINT('',(-0.00607056143210933,0.0137614834612744,0.00192523714366564));
#25440=CARTESIAN_POINT('',(-0.00571168696851309,0.0137857425422816,0.00268784699493865));
#25441=CARTESIAN_POINT('',(-0.00600291424347733,0.00992240968822442,0.00195066711549076));
#25442=CARTESIAN_POINT('',(-0.00574246615396974,0.0100597652673881,0.00275216088845479));
#25443=CARTESIAN_POINT('',(-0.00531940625127602,0.0101935865809844,0.00350058968249362));
#25444=CARTESIAN_POINT('',(-0.00421487443391306,0.0104541606770422,0.00477333431135781));
#25445=CARTESIAN_POINT('',(-0.0035334025192438,0.0105809134595037,0.00529765014618318));
#25446=CARTESIAN_POINT('',(-0.00201997295760744,0.010827350493292,0.00603903134590732));
#25447=CARTESIAN_POINT('',(-0.00118801531064032,0.0109470347446188,0.00625609671080609));
#25448=CARTESIAN_POINT('',(0.000494691428125635,0.0111793347161375,0.00634864955534043));
#25449=CARTESIAN_POINT('',(0.00134544051992447,0.0112919504363295,0.00622413703497599));
#25450=CARTESIAN_POINT('',(0.0029310462363186,0.0115101133455788,0.00565323588430534));
#25451=CARTESIAN_POINT('',(0.0036659028609139,0.011615660534636,0.00520684725399913));
#25452=CARTESIAN_POINT('',(0.0049033904503219,0.0118196863816157,0.00406286356058454));
#25453=CARTESIAN_POINT('',(0.00540602141513462,0.0119181650395382,0.00336526849747616));
#25454=CARTESIAN_POINT('',(0.00609948672115694,0.0121080538242483,0.00182930645777559));
#25455=CARTESIAN_POINT('',(0.00629032106236656,0.012199463951036,0.000990939481183401));
#25456=CARTESIAN_POINT('',(0.0063299824867198,0.0123752156734767,-0.000693845608950566));
#25457=CARTESIAN_POINT('',(0.00617880956986341,0.0124595572691296,-0.00154026372249235));
#25458=CARTESIAN_POINT('',(0.0055583884213982,0.0126211719293006,-0.00310715596524024));
#25459=CARTESIAN_POINT('',(0.00508914018978937,0.0126984449938188,-0.00382763009444637));
#25460=CARTESIAN_POINT('',(0.00390685436447006,0.0128459225917203,-0.00502857724389744));
#25461=CARTESIAN_POINT('',(0.00319381677075958,0.0129161271251037,-0.00550905026414239));
#25462=CARTESIAN_POINT('',(0.00163683219478167,0.0130494676607356,-0.00615393207365249));
#25463=CARTESIAN_POINT('',(0.000792885212514244,0.0131126036629842,-0.00631834086291762));
#25464=CARTESIAN_POINT('',(-0.000892314492041417,0.0132318071363466,-0.00630506756184519));
#25465=CARTESIAN_POINT('',(-0.00173356721432965,0.0132878746074604,-0.00612738547150761));
#25466=CARTESIAN_POINT('',(-0.00328019981295779,0.0133929410185533,-0.0054580565414708));
#25467=CARTESIAN_POINT('',(-0.0039855796892977,0.0134419399585323,-0.00496640970177156));
#25468=CARTESIAN_POINT('',(-0.00514880328885811,0.0135328693073556,-0.0037469922772707));
#25469=CARTESIAN_POINT('',(-0.0056066470120786,0.0135747997161998,-0.00301922169246908));
#25470=CARTESIAN_POINT('',(-0.00620230170530172,0.0136515920027535,-0.00144273489968662));
#25471=CARTESIAN_POINT('',(-0.00634011267530433,0.0136864538804629,-0.000594018691705766));
#25472=CARTESIAN_POINT('',(-0.00627394515429791,0.013749109104747,0.00108987301653347));
#25473=CARTESIAN_POINT('',(-0.00606996666328886,0.0137769024513217,0.00192504851679185));
#25474=CARTESIAN_POINT('',(-0.00571112736074713,0.013801161532329,0.00268758365066568));
#25475=CARTESIAN_POINT('',(-0.00600291424347733,0.0100627296731023,0.00195066711549077));
#25476=CARTESIAN_POINT('',(-0.00574246615396974,0.010200085252266,0.00275216088845479));
#25477=CARTESIAN_POINT('',(-0.00531940625127601,0.0103339065658623,0.00350058968249363));
#25478=CARTESIAN_POINT('',(-0.00421487443391307,0.0105944806619201,0.00477333431135782));
#25479=CARTESIAN_POINT('',(-0.00353340251924381,0.0107212334443816,0.00529765014618319));
#25480=CARTESIAN_POINT('',(-0.00201997295760744,0.0109676704781699,0.00603903134590733));
#25481=CARTESIAN_POINT('',(-0.00118801531064032,0.0110873547294967,0.0062560967108061));
#25482=CARTESIAN_POINT('',(0.000494691428125638,0.0113196547010155,0.00634864955534044));
#25483=CARTESIAN_POINT('',(0.00134544051992447,0.0114322704212074,0.006224137034976));
#25484=CARTESIAN_POINT('',(0.0029310462363186,0.0116504333304567,0.00565323588430534));
#25485=CARTESIAN_POINT('',(0.0036659028609139,0.0117559805195139,0.00520684725399913));
#25486=CARTESIAN_POINT('',(0.00490339045032191,0.0119600063664936,0.00406286356058454));
#25487=CARTESIAN_POINT('',(0.0054060214151346,0.0120584850244161,0.00336526849747616));
#25488=CARTESIAN_POINT('',(0.00609948672115694,0.0122483738091262,0.00182930645777561));
#25489=CARTESIAN_POINT('',(0.00629032106236657,0.012339783935914,0.000990939481183417));
#25490=CARTESIAN_POINT('',(0.00632998248671981,0.0125155356583546,-0.000693845608950559));
#25491=CARTESIAN_POINT('',(0.00617880956986342,0.0125998772540075,-0.00154026372249234));
#25492=CARTESIAN_POINT('',(0.0055583884213982,0.0127614919141786,-0.00310715596524025));
#25493=CARTESIAN_POINT('',(0.00508914018978937,0.0128387649786967,-0.00382763009444637));
#25494=CARTESIAN_POINT('',(0.00390685436447006,0.0129862425765982,-0.00502857724389744));
#25495=CARTESIAN_POINT('',(0.00319381677075959,0.0130564471099816,-0.00550905026414239));
#25496=CARTESIAN_POINT('',(0.00163683219478168,0.0131897876456135,-0.00615393207365249));
#25497=CARTESIAN_POINT('',(0.000792885212514246,0.0132529236478621,-0.00631834086291763));
#25498=CARTESIAN_POINT('',(-0.000892314492041417,0.0133721271212245,-0.00630506756184518));
#25499=CARTESIAN_POINT('',(-0.00173356721432965,0.0134281945923383,-0.00612738547150761));
#25500=CARTESIAN_POINT('',(-0.00328019981295779,0.0135332610034312,-0.00545805654147079));
#25501=CARTESIAN_POINT('',(-0.00398557968929771,0.0135822599434102,-0.00496640970177156));
#25502=CARTESIAN_POINT('',(-0.00514880328885811,0.0136731892922335,-0.0037469922772707));
#25503=CARTESIAN_POINT('',(-0.0056066470120786,0.0137151197010777,-0.00301922169246908));
#25504=CARTESIAN_POINT('',(-0.00620230170530172,0.0137919119876314,-0.00144273489968662));
#25505=CARTESIAN_POINT('',(-0.00634011267530434,0.0138267738653408,-0.000594018691705788));
#25506=CARTESIAN_POINT('',(-0.00627394515429791,0.0138894290896249,0.00108987301653344));
#25507=CARTESIAN_POINT('',(-0.00606996666328888,0.0139172224361996,0.00192504851679183));
#25508=CARTESIAN_POINT('',(-0.00571112736074714,0.0139414815172069,0.00268758365066566));
#25509=CARTESIAN_POINT('',(-0.00604151039169543,0.0101876306679329,0.00196320906329477));
#25510=CARTESIAN_POINT('',(-0.00577938773336043,0.0103249862470965,0.00276985609535972));
#25511=CARTESIAN_POINT('',(-0.00535360773805049,0.0104588075606928,0.00352309696358349));
#25512=CARTESIAN_POINT('',(-0.00424197425772759,0.0107193816567506,0.00480402479119866));
#25513=CARTESIAN_POINT('',(-0.00355612077271463,0.0108461344392122,0.00533171175059006));
#25514=CARTESIAN_POINT('',(-0.00203296051206952,0.0110925714730005,0.00607785971150886));
#25515=CARTESIAN_POINT('',(-0.00119565373643737,0.0112122557243272,0.00629632071303625));
#25516=CARTESIAN_POINT('',(0.000497872080540071,0.011444555695846,0.0063894686324227));
#25517=CARTESIAN_POINT('',(0.00135409112188536,0.011557171416038,0.00626415555028175));
#25518=CARTESIAN_POINT('',(0.00294989159881799,0.0117753343252872,0.00568958375156659));
#25519=CARTESIAN_POINT('',(0.00368947303440534,0.0118808815143445,0.00524032503499238));
#25520=CARTESIAN_POINT('',(0.00493491713501468,0.0120849073613242,0.00408898602007905));
#25521=CARTESIAN_POINT('',(0.00544077980003667,0.0121833860192466,0.00338690572173993));
#25522=CARTESIAN_POINT('',(0.00613870378873374,0.0123732748039568,0.00184106810891984));
#25523=CARTESIAN_POINT('',(0.00633076511240882,0.0124646849307445,0.000997310794438878));
#25524=CARTESIAN_POINT('',(0.00637068154260601,0.0126404366531851,-0.000698306736809025));
#25525=CARTESIAN_POINT('',(0.00621853664912812,0.012724778248838,-0.00155016695357596));
#25526=CARTESIAN_POINT('',(0.00559412646040137,0.0128863929090091,-0.00312713363730202));
#25527=CARTESIAN_POINT('',(0.0051218611651525,0.0129636659735273,-0.00385224010426115));
#25528=CARTESIAN_POINT('',(0.00393197375215438,0.0131111435714288,-0.00506090882565251));
#25529=CARTESIAN_POINT('',(0.00321435163440513,0.0131813481048121,-0.00554447108008473));
#25530=CARTESIAN_POINT('',(0.00164735631947105,0.0133146886404441,-0.00619349920135166));
#25531=CARTESIAN_POINT('',(0.00079798312228622,0.0133778246426927,-0.00635896506818637));
#25532=CARTESIAN_POINT('',(-0.000898051689175196,0.0134970281160551,-0.00634560642551571));
#25533=CARTESIAN_POINT('',(-0.00174471330345179,0.0135530955871689,-0.00616678191601034));
#25534=CARTESIAN_POINT('',(-0.0033012900822888,0.0136581619982617,-0.00549314948978108));
#25535=CARTESIAN_POINT('',(-0.00401120524684925,0.0137071609382408,-0.00499834157305719));
#25536=CARTESIAN_POINT('',(-0.00518190787220253,0.013798090287064,-0.00377108382071775));
#25537=CARTESIAN_POINT('',(-0.00564269533299538,0.0138400206959083,-0.0030386339851022));
#25538=CARTESIAN_POINT('',(-0.00624217982886001,0.0139168129824619,-0.00145201106252507));
#25539=CARTESIAN_POINT('',(-0.00638087686393179,0.0139516748601714,-0.000597837975563495));
#25540=CARTESIAN_POINT('',(-0.00631428391431779,0.0140143300844555,0.0010968804297296));
#25541=CARTESIAN_POINT('',(-0.00610899392963201,0.0140421234310302,0.00193742574806112));
#25542=CARTESIAN_POINT('',(-0.00574784744522067,0.0140663825120374,0.00270486365379789));
#25543=CARTESIAN_POINT('',(-0.00618115256778337,0.0103897247227974,0.00200858625673483));
#25544=CARTESIAN_POINT('',(-0.00591297126251429,0.0105270803019611,0.00283387795537971));
#25545=CARTESIAN_POINT('',(-0.0054773498796663,0.0106609016155573,0.00360452907156096));
#25546=CARTESIAN_POINT('',(-0.00434002234137772,0.0109214757116152,0.00491506399039386));
#25547=CARTESIAN_POINT('',(-0.00363831618593712,0.0110482284940767,0.00545494779304551));
#25548=CARTESIAN_POINT('',(-0.00207994992554408,0.011294665527865,0.00621834205798284));
#25549=CARTESIAN_POINT('',(-0.00122328982059163,0.0114143497791917,0.00644185252026851));
#25550=CARTESIAN_POINT('',(0.000509379789081899,0.0116466497507105,0.00653715344069573));
#25551=CARTESIAN_POINT('',(0.00138538929380299,0.0117592654709025,0.00640894389883727));
#25552=CARTESIAN_POINT('',(0.0030180747608711,0.0119774283801518,0.00582109157073635));
#25553=CARTESIAN_POINT('',(0.00377475072321812,0.012082975569209,0.00536144878449388));
#25554=CARTESIAN_POINT('',(0.00504898175178574,0.0122870014161887,0.00418349796639993));
#25555=CARTESIAN_POINT('',(0.00556653681800634,0.0123854800741112,0.00346518993454846));
#25556=CARTESIAN_POINT('',(0.00628059247216568,0.0125753688588213,0.00188362216252356));
#25557=CARTESIAN_POINT('',(0.00647709306010441,0.012666778985609,0.00102036242235014));
#25558=CARTESIAN_POINT('',(0.00651793211011238,0.0128425307080496,-0.000714447249029106));
#25559=CARTESIAN_POINT('',(0.00636227057218162,0.0129268723037026,-0.00158599718023493));
#25560=CARTESIAN_POINT('',(0.00572342790020611,0.0130884869638736,-0.00319941353383765));
#25561=CARTESIAN_POINT('',(0.00524024676616137,0.0131657600283918,-0.00394127995623455));
#25562=CARTESIAN_POINT('',(0.00402285655057284,0.0133132376262933,-0.0051778855873524));
#25563=CARTESIAN_POINT('',(0.00328864746902905,0.0133834421596767,-0.00567262479607335));
#25564=CARTESIAN_POINT('',(0.00168543296029903,0.0135167826953086,-0.00633665441420447));
#25565=CARTESIAN_POINT('',(0.000816427533112797,0.0135799186975572,-0.00650594482361463));
#25566=CARTESIAN_POINT('',(-0.000918809063405364,0.0136991221709196,-0.00649227741214095));
#25567=CARTESIAN_POINT('',(-0.0017850402327373,0.0137551896420334,-0.0063093195912571));
#25568=CARTESIAN_POINT('',(-0.00337759539356031,0.0138602560531262,-0.00562011696953312));
#25569=CARTESIAN_POINT('',(-0.0041039193850514,0.0139092549931053,-0.005113872168693));
#25570=CARTESIAN_POINT('',(-0.00530168137992607,0.0140001843419285,-0.00385824784375061));
#25571=CARTESIAN_POINT('',(-0.00577311938330966,0.0140421147507728,-0.00310886831964835));
#25572=CARTESIAN_POINT('',(-0.00638646023530149,0.0141189070373265,-0.00148557253495975));
#25573=CARTESIAN_POINT('',(-0.00652836308390973,0.0141537689150359,-0.000611656274373407));
#25574=CARTESIAN_POINT('',(-0.00646023091913374,0.01421642413932,0.00112223348884646));
#25575=CARTESIAN_POINT('',(-0.00625019590574951,0.0142442174858947,0.00198220699147998));
#25576=CARTESIAN_POINT('',(-0.00588070195891569,0.0142684765669019,0.00276738329245592));
#25577=CARTESIAN_POINT('',(-0.0062821985956532,0.0104669177828314,0.00204142150237086));
#25578=CARTESIAN_POINT('',(-0.00600963321227745,0.010604273361995,0.00288020460849478));
#25579=CARTESIAN_POINT('',(-0.00556689053450765,0.0107380946755913,0.00366345389844858));
#25580=CARTESIAN_POINT('',(-0.00441097060121332,0.0109986687716491,0.00499541270974823));
#25581=CARTESIAN_POINT('',(-0.00369779334568878,0.0111254215541106,0.00554412223109408));
#25582=CARTESIAN_POINT('',(-0.00211395178455655,0.0113718585878989,0.00631999603885528));
#25583=CARTESIAN_POINT('',(-0.00124328747894885,0.0114915428392257,0.00654716032527062));
#25584=CARTESIAN_POINT('',(0.000517706845209291,0.0117238428107445,0.00664401917188651));
#25585=CARTESIAN_POINT('',(0.00140803686375974,0.0118364585309365,0.00651371373208705));
#25586=CARTESIAN_POINT('',(0.00306741256042482,0.0120546214401857,0.00591625152264486));
#25587=CARTESIAN_POINT('',(0.00383645823853945,0.012160168629243,0.00544909475300213));
#25588=CARTESIAN_POINT('',(0.00513151968386402,0.0123641944762227,0.0042518874532263));
#25589=CARTESIAN_POINT('',(0.00565753545107396,0.0124626731341451,0.00352183692309322));
#25590=CARTESIAN_POINT('',(0.00638326408802082,0.0126525619188553,0.00191441456498304));
#25591=CARTESIAN_POINT('',(0.00658297695775774,0.012743972045643,0.00103704273700594));
#25592=CARTESIAN_POINT('',(0.00662448362173253,0.0129197237680836,-0.00072612663339072));
#25593=CARTESIAN_POINT('',(0.0064662774159704,0.0130040653637365,-0.00161192417581028));
#25594=CARTESIAN_POINT('',(0.00581699130100769,0.0131656800239076,-0.0032517157583115));
#25595=CARTESIAN_POINT('',(0.0053259113918071,0.0132429530884257,-0.00400570979839314));
#25596=CARTESIAN_POINT('',(0.00408861996130697,0.0133904306863273,-0.00526253076729722));
#25597=CARTESIAN_POINT('',(0.00334240844000743,0.0134606352197106,-0.00576535769611964));
#25598=CARTESIAN_POINT('',(0.00171298547643764,0.0135939757553426,-0.00644024249935811));
#25599=CARTESIAN_POINT('',(0.000829774034167402,0.0136571117575912,-0.00661230037377415));
#25600=CARTESIAN_POINT('',(-0.000933829240501756,0.0137763152309536,-0.00659840953509567));
#25601=CARTESIAN_POINT('',(-0.00181422107290067,0.0138323827020674,-0.00641246082200114));
#25602=CARTESIAN_POINT('',(-0.0034328104355008,0.0139374491131602,-0.00571199150097489));
#25603=CARTESIAN_POINT('',(-0.004171007965702,0.0139864480531392,-0.00519747089304317));
#25604=CARTESIAN_POINT('',(-0.00538835030430519,0.0140773774019625,-0.00392132032333643));
#25605=CARTESIAN_POINT('',(-0.00586749511270716,0.0141193078108067,-0.0031596903615614));
#25606=CARTESIAN_POINT('',(-0.00649086251818467,0.0141961000973604,-0.00150985784455599));
#25607=CARTESIAN_POINT('',(-0.00663508511526021,0.0142309619750699,-0.00062165528932561));
#25608=CARTESIAN_POINT('',(-0.00656583916392981,0.014293617199354,0.00114057913476716));
#25609=CARTESIAN_POINT('',(-0.00635237061552386,0.0143214105459286,0.00201461100362956));
#25610=CARTESIAN_POINT('',(-0.00597683638813717,0.0143456696269359,0.00281262292798174));
#25611=CARTESIAN_POINT('',(-0.00650814438282647,0.0105441108428653,0.00211484334367094));
#25612=CARTESIAN_POINT('',(-0.00622577590278555,0.010681466422029,0.00298379415403012));
#25613=CARTESIAN_POINT('',(-0.00576710952548274,0.0108152877356253,0.00379521381693169));
#25614=CARTESIAN_POINT('',(-0.00456961573309102,0.0110758618316831,0.00517507790812964));
#25615=CARTESIAN_POINT('',(-0.00383078831800211,0.0112026146141446,0.00574352233642602));
#25616=CARTESIAN_POINT('',(-0.0021899822526698,0.0114490516479329,0.00654730125026951));
#25617=CARTESIAN_POINT('',(-0.00128800360242641,0.0115687358992597,0.00678263573581662));
#25618=CARTESIAN_POINT('',(0.000536326708762601,0.0118010358707784,0.0068829782112943));
#25619=CARTESIAN_POINT('',(0.0014586783697082,0.0119136515909704,0.00674798620122487));
#25620=CARTESIAN_POINT('',(0.00317773523408718,0.0121318145002197,0.00612903564384791));
#25621=CARTESIAN_POINT('',(0.00397444043752055,0.0122373616892769,0.00564507709654037));
#25622=CARTESIAN_POINT('',(0.00531608011071332,0.0124413875362566,0.00440481099471639));
#25623=CARTESIAN_POINT('',(0.00586101458047273,0.0125398661941791,0.00364850344019995));
#25624=CARTESIAN_POINT('',(0.00661284480043267,0.0127297549788892,0.00198326847007294));
#25625=CARTESIAN_POINT('',(0.00681974055063322,0.0128211651056769,0.00107434105446238));
#25626=CARTESIAN_POINT('',(0.00686274004482053,0.0129969168281176,-0.000752242530758643));
#25627=CARTESIAN_POINT('',(0.00669884378880731,0.0130812584237705,-0.00166989870036911));
#25628=CARTESIAN_POINT('',(0.00602620542540606,0.0132428730839416,-0.00336866708760947));
#25629=CARTESIAN_POINT('',(0.00551746331801803,0.0133201461484597,-0.00414977930523935));
#25630=CARTESIAN_POINT('',(0.00423567141814074,0.0134676237463612,-0.00545180314362154));
#25631=CARTESIAN_POINT('',(0.00346262162565148,0.0135378282797446,-0.00597271476437384));
#25632=CARTESIAN_POINT('',(0.00177459477547475,0.0136711688153765,-0.00667187249942069));
#25633=CARTESIAN_POINT('',(0.000859617717787273,0.0137343048176251,-0.00685011861371523));
#25634=CARTESIAN_POINT('',(-0.000967415377523374,0.0138535082909875,-0.00683572817661878));
#25635=CARTESIAN_POINT('',(-0.00187947141514655,0.0139095757621013,-0.00664309162522779));
#25636=CARTESIAN_POINT('',(-0.00355627502266023,0.0140146421731942,-0.00591742919867961));
#25637=CARTESIAN_POINT('',(-0.00432102259255075,0.0140636411131732,-0.00538440332352243));
#25638=CARTESIAN_POINT('',(-0.00558214791075367,0.0141545704619965,-0.00406235467519978));
#25639=CARTESIAN_POINT('',(-0.00607852565906609,0.0141965008708407,-0.00327333190203431));
#25640=CARTESIAN_POINT('',(-0.00672431311971763,0.0142732931573944,-0.00156416144766781));
#25641=CARTESIAN_POINT('',(-0.00687372283205676,0.0143081550351038,-0.000644013766466768));
#25642=CARTESIAN_POINT('',(-0.00680198637827826,0.0143708102593879,0.00118160124613701));
#25643=CARTESIAN_POINT('',(-0.00658084021216063,0.0143986036059626,0.00208706857753974));
#25644=CARTESIAN_POINT('',(-0.00619179950685455,0.0144228626869699,0.00291378182829478));
#25645=CARTESIAN_POINT('',(-0.00663304414212992,0.0105441108428653,0.00215542993933499));
#25646=CARTESIAN_POINT('',(-0.00634525664353049,0.010681466422029,0.00304105704645039));
#25647=CARTESIAN_POINT('',(-0.00587778786161648,0.0108152877356253,0.00386804890852719));
#25648=CARTESIAN_POINT('',(-0.00465731260513313,0.0110758618316831,0.00527439438715669));
#25649=CARTESIAN_POINT('',(-0.00390430613056378,0.0112026146141446,0.0058537480037094));
#25650=CARTESIAN_POINT('',(-0.00223201086177059,0.0114490516479329,0.00667295248081131));
#25651=CARTESIAN_POINT('',(-0.00131272206754674,0.0115687358992597,0.00691280334136051));
#25652=CARTESIAN_POINT('',(0.000546619516188517,0.0118010358707784,0.00701507151951131));
#25653=CARTESIAN_POINT('',(0.00148667230569993,0.0119136515909704,0.00687748883711291));
#25654=CARTESIAN_POINT('',(0.00323872010819583,0.0121318145002197,0.00624665981314244));
#25655=CARTESIAN_POINT('',(0.00405071512118033,0.0122373616892769,0.00575341347157038));
#25656=CARTESIAN_POINT('',(0.00541810260548434,0.0124413875362566,0.00448934504938012));
#25657=CARTESIAN_POINT('',(0.00597349507680387,0.0125398661941791,0.00371852296876192));
#25658=CARTESIAN_POINT('',(0.00673975389698938,0.0127297549788892,0.00202132997270337));
#25659=CARTESIAN_POINT('',(0.00695062024585536,0.0128211651056769,0.00109495905726303));
#25660=CARTESIAN_POINT('',(0.00699444495628839,0.0129969168281176,-0.000766679043764951));
#25661=CARTESIAN_POINT('',(0.00682740331785544,0.0130812584237705,-0.00170194622935258));
#25662=CARTESIAN_POINT('',(0.00614185614900286,0.0132428730839416,-0.00343331619243359));
#25663=CARTESIAN_POINT('',(0.00562335061858323,0.0133201461484597,-0.00422941896992696));
#25664=CARTESIAN_POINT('',(0.00431695946424038,0.0134676237463612,-0.00555643034000104));
#25665=CARTESIAN_POINT('',(0.00352907384031716,0.0135378282797446,-0.00608733893258175));
#25666=CARTESIAN_POINT('',(0.00180865155837324,0.0136711688153765,-0.00679991441432962));
#25667=CARTESIAN_POINT('',(0.000876114900352538,0.0137343048176251,-0.00698158130349679));
#25668=CARTESIAN_POINT('',(-0.0009859813374486,0.0138535082909875,-0.00696691469518718));
#25669=CARTESIAN_POINT('',(-0.00191554091722904,0.0139095757621013,-0.0067705811977104));
#25670=CARTESIAN_POINT('',(-0.00362452456787917,0.0140146421731942,-0.00603099236494257));
#25671=CARTESIAN_POINT('',(-0.00440394863874886,0.0140636411131732,-0.00548773702965151));
#25672=CARTESIAN_POINT('',(-0.00568927659282304,0.0141545704619965,-0.00414031654747732));
#25673=CARTESIAN_POINT('',(-0.00619518047602752,0.0141965008708407,-0.00333615140059418));
#25674=CARTESIAN_POINT('',(-0.00685336143836741,0.0142732931573944,-0.00159417974118338));
#25675=CARTESIAN_POINT('',(-0.00700563851750283,0.0143081550351038,-0.000656373228655721));
#25676=CARTESIAN_POINT('',(-0.00693252534783064,0.0143708102593879,0.00120427771158615));
#25677=CARTESIAN_POINT('',(-0.00670713509902304,0.0143986036059626,0.00212712213930035));
#25678=CARTESIAN_POINT('',(-0.00631062819635044,0.0144228626869699,0.00296970109308201));
#25679=CARTESIAN_POINT('',(-0.0068589899293032,0.0104669177828314,0.00222885178063507));
#25680=CARTESIAN_POINT('',(-0.00656139933403859,0.010604273361995,0.00314464659198573));
#25681=CARTESIAN_POINT('',(-0.00607800685259157,0.0107380946755913,0.0039998088270103));
#25682=CARTESIAN_POINT('',(-0.00481595773701083,0.0109986687716491,0.00545405958553811));
#25683=CARTESIAN_POINT('',(-0.00403730110287711,0.0111254215541107,0.00605314810904135));
#25684=CARTESIAN_POINT('',(-0.00230804132988384,0.0113718585878989,0.00690025769222555));
#25685=CARTESIAN_POINT('',(-0.00135743819102429,0.0114915428392257,0.00714827875190651));
#25686=CARTESIAN_POINT('',(0.000565239379741828,0.0117238428107445,0.0072540305589191));
#25687=CARTESIAN_POINT('',(0.00153731381164839,0.0118364585309365,0.00711176130625072));
#25688=CARTESIAN_POINT('',(0.0033490427818582,0.0120546214401857,0.00645944393434549));
#25689=CARTESIAN_POINT('',(0.00418869732016144,0.012160168629243,0.00594939581510862));
#25690=CARTESIAN_POINT('',(0.00560266303233365,0.0123641944762227,0.0046422685908702));
#25691=CARTESIAN_POINT('',(0.00617697420620264,0.0124626731341451,0.00384518948586864));
#25692=CARTESIAN_POINT('',(0.00696933460940123,0.0126525619188553,0.00209018387779328));
#25693=CARTESIAN_POINT('',(0.00718738383873084,0.012743972045643,0.00113225737471947));
#25694=CARTESIAN_POINT('',(0.0072327013793764,0.0129197237680836,-0.000792794941132875));
#25695=CARTESIAN_POINT('',(0.00705996969069235,0.0130040653637365,-0.00175992075391141));
#25696=CARTESIAN_POINT('',(0.00635107027340123,0.0131656800239076,-0.00355026752173156));
#25697=CARTESIAN_POINT('',(0.00581490254479415,0.0132429530884257,-0.00437348847677317));
#25698=CARTESIAN_POINT('',(0.00446401092107414,0.0133904306863273,-0.00574570271632536));
#25699=CARTESIAN_POINT('',(0.00364928702596121,0.0134606352197106,-0.00629469600083594));
#25700=CARTESIAN_POINT('',(0.00187026085741034,0.0135939757553426,-0.0070315444143922));
#25701=CARTESIAN_POINT('',(0.000905958583972411,0.0136571117575912,-0.00721939954343787));
#25702=CARTESIAN_POINT('',(-0.00101956747447021,0.0137763152309536,-0.0072042333367103));
#25703=CARTESIAN_POINT('',(-0.00198079125947491,0.0138323827020674,-0.00700121200093705));
#25704=CARTESIAN_POINT('',(-0.0037479891550386,0.0139374491131602,-0.00623643006264729));
#25705=CARTESIAN_POINT('',(-0.0045539632655976,0.0139864480531392,-0.00567466946013077));
#25706=CARTESIAN_POINT('',(-0.00588307419927152,0.0140773774019625,-0.00428135089934067));
#25707=CARTESIAN_POINT('',(-0.00640621102238644,0.0141193078108067,-0.0034497929410671));
#25708=CARTESIAN_POINT('',(-0.00708681203990037,0.0141961000973604,-0.0016484833442952));
#25709=CARTESIAN_POINT('',(-0.00724427623429938,0.0142309619750699,-0.000678731705796876));
#25710=CARTESIAN_POINT('',(-0.0071686725621791,0.014293617199354,0.00124529982295599));
#25711=CARTESIAN_POINT('',(-0.00693560469565981,0.0143214105459286,0.00219957971321054));
#25712=CARTESIAN_POINT('',(-0.00652559131506782,0.0143456696269359,0.00307085999339506));
#25713=CARTESIAN_POINT('',(-0.00696003595717303,0.0103897247227974,0.00226168702627111));
#25714=CARTESIAN_POINT('',(-0.00665806128380176,0.0105270803019611,0.0031909732451008));
#25715=CARTESIAN_POINT('',(-0.00616754750743291,0.0106609016155573,0.00405873365389792));
#25716=CARTESIAN_POINT('',(-0.00488690599684642,0.0109214757116152,0.00553440830489247));
#25717=CARTESIAN_POINT('',(-0.00409677826262877,0.0110482284940767,0.00614232254708991));
#25718=CARTESIAN_POINT('',(-0.00234204318889632,0.011294665527865,0.00700191167309799));
#25719=CARTESIAN_POINT('',(-0.00137743584938151,0.0114143497791917,0.00725358655690862));
#25720=CARTESIAN_POINT('',(0.000573566435869221,0.0116466497507105,0.00736089629010987));
#25721=CARTESIAN_POINT('',(0.00155996138160514,0.0117592654709025,0.0072165311395005));
#25722=CARTESIAN_POINT('',(0.00339838058141192,0.0119774283801518,0.006554603886254));
#25723=CARTESIAN_POINT('',(0.00425040483548277,0.012082975569209,0.00603704178361687));
#25724=CARTESIAN_POINT('',(0.00568520096441194,0.0122870014161887,0.00471065807769657));
#25725=CARTESIAN_POINT('',(0.00626797283927026,0.0123854800741112,0.0039018364744134));
#25726=CARTESIAN_POINT('',(0.00707200622525638,0.0125753688588213,0.00212097628025274));
#25727=CARTESIAN_POINT('',(0.00729326773638417,0.012666778985609,0.00114893768937527));
#25728=CARTESIAN_POINT('',(0.00733925289099655,0.0128425307080496,-0.00080447432549449));
#25729=CARTESIAN_POINT('',(0.00716397653448113,0.0129268723037026,-0.00178584774948676));
#25730=CARTESIAN_POINT('',(0.0064446336742028,0.0130884869638736,-0.00360256974620541));
#25731=CARTESIAN_POINT('',(0.00590056717043989,0.0131657600283918,-0.00443791831893177));
#25732=CARTESIAN_POINT('',(0.00452977433180828,0.0133132376262933,-0.00583034789627018));
#25733=CARTESIAN_POINT('',(0.00370304799693959,0.0133834421596767,-0.00638742890088223));
#25734=CARTESIAN_POINT('',(0.00189781337354896,0.0135167826953086,-0.00713513249954584));
#25735=CARTESIAN_POINT('',(0.000919305085027019,0.0135799186975572,-0.00732575509359739));
#25736=CARTESIAN_POINT('',(-0.0010345876515666,0.0136991221709196,-0.00731036545966502));
#25737=CARTESIAN_POINT('',(-0.00200997209963829,0.0137551896420334,-0.00710435323168109));
#25738=CARTESIAN_POINT('',(-0.00380320419697909,0.0138602560531262,-0.00632830459408906));
#25739=CARTESIAN_POINT('',(-0.00462105184624821,0.0139092549931053,-0.00575826818448095));
#25740=CARTESIAN_POINT('',(-0.00596974312365063,0.0140001843419285,-0.00434442337892649));
#25741=CARTESIAN_POINT('',(-0.00650058675178394,0.0140421147507728,-0.00350061498298014));
#25742=CARTESIAN_POINT('',(-0.00719121432278355,0.0141189070373265,-0.00167276865389143));
#25743=CARTESIAN_POINT('',(-0.00735099826564986,0.0141537689150359,-0.000688730720749077));
#25744=CARTESIAN_POINT('',(-0.00727428080697517,0.01421642413932,0.0012636454688767));
#25745=CARTESIAN_POINT('',(-0.00703777940543416,0.0142442174858947,0.00223198372536013));
#25746=CARTESIAN_POINT('',(-0.00662172574428931,0.0142684765669019,0.00311609962892087));
#25747=CARTESIAN_POINT('',(-0.00709967813326097,0.0101876306679329,0.00230706421971116));
#25748=CARTESIAN_POINT('',(-0.00679164481295561,0.0103249862470965,0.00325499510512079));
#25749=CARTESIAN_POINT('',(-0.00629128964904872,0.0104588075606928,0.00414016576187539));
#25750=CARTESIAN_POINT('',(-0.00498495408049655,0.0107193816567506,0.00564544750408768));
#25751=CARTESIAN_POINT('',(-0.00417897367585126,0.0108461344392122,0.00626555858954536));
#25752=CARTESIAN_POINT('',(-0.00238903260237088,0.0110925714730005,0.00714239401957196));
#25753=CARTESIAN_POINT('',(-0.00140507193353578,0.0112122557243272,0.00739911836414088));
#25754=CARTESIAN_POINT('',(0.000585074144411049,0.011444555695846,0.00750858109838291));
#25755=CARTESIAN_POINT('',(0.00159125955352277,0.011557171416038,0.00736131948805603));
#25756=CARTESIAN_POINT('',(0.00346656374346502,0.0117753343252872,0.00668611170542376));
#25757=CARTESIAN_POINT('',(0.00433568252429554,0.0118808815143445,0.00615816553311837));
#25758=CARTESIAN_POINT('',(0.00579926558118299,0.0120849073613242,0.00480517002401746));
#25759=CARTESIAN_POINT('',(0.00639372985723993,0.0121833860192466,0.00398012068722193));
#25760=CARTESIAN_POINT('',(0.00721389490868831,0.0123732748039568,0.00216353033385647));
#25761=CARTESIAN_POINT('',(0.00743959568407976,0.0124646849307445,0.00117198931728653));
#25762=CARTESIAN_POINT('',(0.00748650345850291,0.0126404366531851,-0.00082061483771457));
#25763=CARTESIAN_POINT('',(0.00730771045753463,0.012724778248838,-0.00182167797614574));
#25764=CARTESIAN_POINT('',(0.00657393511400755,0.0128863929090091,-0.00367484964274103));
#25765=CARTESIAN_POINT('',(0.00601895277144875,0.0129636659735273,-0.00452695817090515));
#25766=CARTESIAN_POINT('',(0.00462065713022674,0.0131111435714288,-0.00594732465797007));
#25767=CARTESIAN_POINT('',(0.00377734383156351,0.0131813481048121,-0.00651558261687087));
#25768=CARTESIAN_POINT('',(0.00193589001437694,0.0133146886404441,-0.00727828771239866));
#25769=CARTESIAN_POINT('',(0.0009377494958536,0.0133778246426927,-0.00747273484902566));
#25770=CARTESIAN_POINT('',(-0.00105534502579677,0.0134970281160551,-0.00745703644629025));
#25771=CARTESIAN_POINT('',(-0.0020502990289238,0.0135530955871689,-0.00724689090692786));
#25772=CARTESIAN_POINT('',(-0.00387950950825059,0.0136581619982617,-0.00645527207384111));
#25773=CARTESIAN_POINT('',(-0.00471376598445036,0.0137071609382408,-0.00587379878011676));
#25774=CARTESIAN_POINT('',(-0.00608951663137417,0.013798090287064,-0.00443158740195936));
#25775=CARTESIAN_POINT('',(-0.00663101080209822,0.0138400206959083,-0.0035708493175263));
#25776=CARTESIAN_POINT('',(-0.00733549472922503,0.013916812982462,-0.00170633012632612));
#25777=CARTESIAN_POINT('',(-0.0074984844856278,0.0139516748601714,-0.000702549019558997));
#25778=CARTESIAN_POINT('',(-0.00742022781179112,0.0140143300844555,0.00128899852799355));
#25779=CARTESIAN_POINT('',(-0.00717898138155166,0.0140421234310302,0.00227676496877898));
#25780=CARTESIAN_POINT('',(-0.00675458025798432,0.0140663825120374,0.00317861926757889));
#25781=CARTESIAN_POINT('',(-0.00713827428147907,0.0100627296731023,0.00231960616751517));
#25782=CARTESIAN_POINT('',(-0.0068285663923463,0.010200085252266,0.00327269031202572));
#25783=CARTESIAN_POINT('',(-0.00632549113582319,0.0103339065658623,0.00416267304296526));
#25784=CARTESIAN_POINT('',(-0.00501205390431109,0.0105944806619201,0.00567613798392852));
#25785=CARTESIAN_POINT('',(-0.0042016919293221,0.0107212334443816,0.00629962019395224));
#25786=CARTESIAN_POINT('',(-0.00240202015683297,0.0109676704781699,0.0071812223851735));
#25787=CARTESIAN_POINT('',(-0.00141271035933283,0.0110873547294967,0.00743934236637103));
#25788=CARTESIAN_POINT('',(0.000588254796825484,0.0113196547010154,0.00754940017546517));
#25789=CARTESIAN_POINT('',(0.00159991015548366,0.0114322704212074,0.00740133800336178));
#25790=CARTESIAN_POINT('',(0.00348540910596441,0.0116504333304567,0.00672245957268501));
#25791=CARTESIAN_POINT('',(0.00435925269778697,0.0117559805195139,0.00619164331411162));
#25792=CARTESIAN_POINT('',(0.00583079226587576,0.0119600063664936,0.00483129248351197));
#25793=CARTESIAN_POINT('',(0.00642848824214198,0.0120584850244161,0.00400175791148571));
#25794=CARTESIAN_POINT('',(0.0072531119762651,0.0122483738091262,0.00217529198500073));
#25795=CARTESIAN_POINT('',(0.00748003973412201,0.0123397839359139,0.001178360630542));
#25796=CARTESIAN_POINT('',(0.00752720251438913,0.0125155356583546,-0.000825075965573034));
#25797=CARTESIAN_POINT('',(0.00734743753679934,0.0125998772540075,-0.00183158120722935));
#25798=CARTESIAN_POINT('',(0.00660967315301072,0.0127614919141786,-0.0036948273148028));
#25799=CARTESIAN_POINT('',(0.00605167374681188,0.0128387649786967,-0.00455156818071994));
#25800=CARTESIAN_POINT('',(0.00464577651791105,0.0129862425765982,-0.00597965623972514));
#25801=CARTESIAN_POINT('',(0.00379787869520906,0.0130564471099816,-0.0065510034328132));
#25802=CARTESIAN_POINT('',(0.00194641413906631,0.0131897876456136,-0.00731785484009783));
#25803=CARTESIAN_POINT('',(0.000942847405625574,0.0132529236478621,-0.0075133590542944));
#25804=CARTESIAN_POINT('',(-0.00106108222293055,0.0133721271212245,-0.00749757530996077));
#25805=CARTESIAN_POINT('',(-0.00206144511804592,0.0134281945923384,-0.00728628735143058));
#25806=CARTESIAN_POINT('',(-0.0039005997775816,0.0135332610034312,-0.00649036502215139));
#25807=CARTESIAN_POINT('',(-0.0047393915420019,0.0135822599434102,-0.00590573065140239));
#25808=CARTESIAN_POINT('',(-0.0061226212147186,0.0136731892922335,-0.0044556789454064));
#25809=CARTESIAN_POINT('',(-0.006667059123015,0.0137151197010777,-0.00359026161015942));
#25810=CARTESIAN_POINT('',(-0.00737537285278333,0.0137919119876314,-0.00171560628916458));
#25811=CARTESIAN_POINT('',(-0.00753924867425526,0.0138267738653408,-0.000706368303416717));
#25812=CARTESIAN_POINT('',(-0.00746056657181099,0.0138894290896249,0.00129600594118969));
#25813=CARTESIAN_POINT('',(-0.0072180086478948,0.0139172224361996,0.00228914220004824));
#25814=CARTESIAN_POINT('',(-0.00679130034245786,0.0139414815172069,0.0031958992707111));
#25815=CARTESIAN_POINT('',(-0.00713827428147907,0.00992240968822442,0.00231960616751517));
#25816=CARTESIAN_POINT('',(-0.00682856639234631,0.0100597652673881,0.00327269031202572));
#25817=CARTESIAN_POINT('',(-0.0063254911358232,0.0101935865809844,0.00416267304296526));
#25818=CARTESIAN_POINT('',(-0.00501205390431109,0.0104541606770422,0.00567613798392852));
#25819=CARTESIAN_POINT('',(-0.0042016919293221,0.0105809134595037,0.00629962019395224));
#25820=CARTESIAN_POINT('',(-0.00240202015683297,0.010827350493292,0.0071812223851735));
#25821=CARTESIAN_POINT('',(-0.00141271035933283,0.0109470347446188,0.00743934236637104));
#25822=CARTESIAN_POINT('',(0.000588254796825481,0.0111793347161375,0.00754940017546518));
#25823=CARTESIAN_POINT('',(0.00159991015548366,0.0112919504363295,0.00740133800336179));
#25824=CARTESIAN_POINT('',(0.00348540910596441,0.0115101133455788,0.00672245957268501));
#25825=CARTESIAN_POINT('',(0.00435925269778697,0.011615660534636,0.00619164331411162));
#25826=CARTESIAN_POINT('',(0.00583079226587576,0.0118196863816157,0.00483129248351197));
#25827=CARTESIAN_POINT('',(0.00642848824214198,0.0119181650395382,0.00400175791148571));
#25828=CARTESIAN_POINT('',(0.00725311197626511,0.0121080538242483,0.00217529198500073));
#25829=CARTESIAN_POINT('',(0.00748003973412201,0.012199463951036,0.00117836063054201));
#25830=CARTESIAN_POINT('',(0.00752720251438913,0.0123752156734767,-0.000825075965573031));
#25831=CARTESIAN_POINT('',(0.00734743753679934,0.0124595572691296,-0.00183158120722935));
#25832=CARTESIAN_POINT('',(0.00660967315301072,0.0126211719293006,-0.00369482731480281));
#25833=CARTESIAN_POINT('',(0.00605167374681189,0.0126984449938188,-0.00455156818071995));
#25834=CARTESIAN_POINT('',(0.00464577651791106,0.0128459225917203,-0.00597965623972514));
#25835=CARTESIAN_POINT('',(0.00379787869520906,0.0129161271251037,-0.0065510034328132));
#25836=CARTESIAN_POINT('',(0.00194641413906631,0.0130494676607356,-0.00731785484009783));
#25837=CARTESIAN_POINT('',(0.000942847405625573,0.0131126036629842,-0.0075133590542944));
#25838=CARTESIAN_POINT('',(-0.00106108222293055,0.0132318071363466,-0.00749757530996077));
#25839=CARTESIAN_POINT('',(-0.00206144511804593,0.0132878746074604,-0.00728628735143058));
#25840=CARTESIAN_POINT('',(-0.00390059977758161,0.0133929410185533,-0.00649036502215139));
#25841=CARTESIAN_POINT('',(-0.0047393915420019,0.0134419399585323,-0.00590573065140239));
#25842=CARTESIAN_POINT('',(-0.0061226212147186,0.0135328693073556,-0.0044556789454064));
#25843=CARTESIAN_POINT('',(-0.006667059123015,0.0135747997161998,-0.00359026161015942));
#25844=CARTESIAN_POINT('',(-0.00737537285278333,0.0136515920027535,-0.00171560628916457));
#25845=CARTESIAN_POINT('',(-0.00753924867425526,0.0136864538804629,-0.000706368303416719));
#25846=CARTESIAN_POINT('',(-0.007460566571811,0.013749109104747,0.00129600594118969));
#25847=CARTESIAN_POINT('',(-0.0072180086478948,0.0137769024513217,0.00228914220004825));
#25848=CARTESIAN_POINT('',(-0.00679130034245786,0.013801161532329,0.0031958992707111));
#25849=CARTESIAN_POINT('',(-0.00713768608282461,0.00990699069817707,0.00231941503038975));
#25850=CARTESIAN_POINT('',(-0.0068280037138325,0.0100443462773407,0.00327242064011874));
#25851=CARTESIAN_POINT('',(-0.00632496991105259,0.010178167590937,0.00416233003587611));
#25852=CARTESIAN_POINT('',(-0.00501164090766143,0.0104387416869948,0.00567567026629915));
#25853=CARTESIAN_POINT('',(-0.00420134570705017,0.0105654944694564,0.00629910110096484));
#25854=CARTESIAN_POINT('',(-0.00240182222873878,0.0108119315032447,0.00718063064756609));
#25855=CARTESIAN_POINT('',(-0.00141259395103865,0.0109316157545714,0.00743872935950167));
#25856=CARTESIAN_POINT('',(0.000588206324230238,0.0111639157260902,0.00754877809975751));
#25857=CARTESIAN_POINT('',(0.00159977832179899,0.0112765314462822,0.00740072812807777));
#25858=CARTESIAN_POINT('',(0.00348512190588417,0.0114946943555314,0.00672190563744528));
#25859=CARTESIAN_POINT('',(0.0043588934924006,0.0116002415445887,0.00619113311849253));
#25860=CARTESIAN_POINT('',(0.00583031180462841,0.0118042673915684,0.00483089438172629));
#25861=CARTESIAN_POINT('',(0.00642795853033978,0.0119027460494908,0.0040014281639128));
#25862=CARTESIAN_POINT('',(0.00725251431490651,0.012092634834201,0.00217511273946207));
#25863=CARTESIAN_POINT('',(0.00747942337376187,0.0121840449609887,0.00117826353282482));
#25864=CARTESIAN_POINT('',(0.00752658226778383,0.0123597966834293,-0.000825007978752457));
#25865=CARTESIAN_POINT('',(0.00734683210295042,0.0124441382790822,-0.00183143028369249));
#25866=CARTESIAN_POINT('',(0.00660912851144867,0.0126057529392533,-0.00369452285851977));
#25867=CARTESIAN_POINT('',(0.00605117508478032,0.0126830260037714,-0.00455119312840702));
#25868=CARTESIAN_POINT('',(0.00464539370276709,0.012830503601673,-0.00597916351198512));
#25869=CARTESIAN_POINT('',(0.00379756574742221,0.0129007081350563,-0.00655046362567598));
#25870=CARTESIAN_POINT('',(0.00194625375321779,0.0130340486706883,-0.00731725184388323));
#25871=CARTESIAN_POINT('',(0.000942769714358262,0.0130971846729369,-0.00751273994839962));
#25872=CARTESIAN_POINT('',(-0.0010609947890339,0.0132163881462993,-0.00749695750465726));
#25873=CARTESIAN_POINT('',(-0.00206127525356652,0.0132724556174131,-0.00728568695639851));
#25874=CARTESIAN_POINT('',(-0.00390027836550772,0.0133775220285059,-0.00648983021166044));
#25875=CARTESIAN_POINT('',(-0.00473900101291629,0.013426520968485,-0.00590524401518111));
#25876=CARTESIAN_POINT('',(-0.00612211670656743,0.0135174503173082,-0.00445531179443167));
#25877=CARTESIAN_POINT('',(-0.00666650975281,0.0135593807261525,-0.00358996577016154));
#25878=CARTESIAN_POINT('',(-0.00737476511704538,0.0136361730127061,-0.00171546492203982));
#25879=CARTESIAN_POINT('',(-0.00753862743503819,0.0136710348904156,-0.000706310098188223));
#25880=CARTESIAN_POINT('',(-0.00745995181605267,0.0137336901146997,0.00129589914941892));
#25881=CARTESIAN_POINT('',(-0.00721741387907434,0.0137614834612743,0.00228895357317447));
#25882=CARTESIAN_POINT('',(-0.0067907407346919,0.0137857425422816,0.00319563592643815));
#25883=CARTESIAN_POINT('',(-0.00713652355335438,0.00989161658584234,0.0023190372625396));
#25884=CARTESIAN_POINT('',(-0.00682689162296045,0.010028972165006,0.00327188765430387));
#25885=CARTESIAN_POINT('',(-0.00632393975032057,0.0101627934786023,0.00416165210870539));
#25886=CARTESIAN_POINT('',(-0.00501082465149917,0.0104233675746601,0.00567474585832276));
#25887=CARTESIAN_POINT('',(-0.00420066142531763,0.0105501203571216,0.00629807515353861));
#25888=CARTESIAN_POINT('',(-0.0024014310390604,0.0107965573909099,0.00717946112362713));
#25889=CARTESIAN_POINT('',(-0.00141236387898469,0.0109162416422367,0.0074375177984998));
#25890=CARTESIAN_POINT('',(0.000588110521868161,0.0111485416137555,0.00754754861489316));
#25891=CARTESIAN_POINT('',(0.00159951776264531,0.0112611573339475,0.00739952275641386));
#25892=CARTESIAN_POINT('',(0.00348455427698092,0.0114793202431967,0.00672081082698304));
#25893=CARTESIAN_POINT('',(0.00435818355053937,0.0115848674322539,0.00619012475603152));
#25894=CARTESIAN_POINT('',(0.0058293622098697,0.0117888932792336,0.00483010756411885));
#25895=CARTESIAN_POINT('',(0.00642691159564158,0.0118873719371561,0.00400077644315771));
#25896=CARTESIAN_POINT('',(0.00725133308312823,0.0120772607218663,0.00217475847441996));
#25897=CARTESIAN_POINT('',(0.00747820518484301,0.012168670848654,0.00117807162664336));
#25898=CARTESIAN_POINT('',(0.00752535639799984,0.0123444225710946,-0.000824873608022594));
#25899=CARTESIAN_POINT('',(0.0073456355094419,0.0124287641667475,-0.00183113199491196));
#25900=CARTESIAN_POINT('',(0.00660805206922664,0.0125903788269186,-0.00369392112405686));
#25901=CARTESIAN_POINT('',(0.00605018951756932,0.0126676518914367,-0.00455045186631239));
#25902=CARTESIAN_POINT('',(0.00464463709803305,0.0128151294893382,-0.00597818967344566));
#25903=CARTESIAN_POINT('',(0.0037969472301541,0.0128853340227216,-0.00654939673832338));
#25904=CARTESIAN_POINT('',(0.00194593676290491,0.0130186745583536,-0.00731606006817175));
#25905=CARTESIAN_POINT('',(0.000942616163534665,0.0130818105606022,-0.00751151633314239));
#25906=CARTESIAN_POINT('',(-0.00106082198265159,0.0132010140339646,-0.00749573645991879));
#25907=CARTESIAN_POINT('',(-0.0020609395294676,0.0132570815050784,-0.00728450032172455));
#25908=CARTESIAN_POINT('',(-0.0038996431192263,0.0133621479161712,-0.00648877319979548));
#25909=CARTESIAN_POINT('',(-0.00473822916216899,0.0134111468561502,-0.00590428221606065));
#25910=CARTESIAN_POINT('',(-0.00612111958495,0.0135020762049735,-0.0044545861487252));
#25911=CARTESIAN_POINT('',(-0.00666542396478831,0.0135440066138177,-0.00358938106512457));
#25912=CARTESIAN_POINT('',(-0.00737356397402995,0.0136207989003714,-0.00171518552077393));
#25913=CARTESIAN_POINT('',(-0.00753739960343328,0.0136556607780809,-0.000706195060023929));
#25914=CARTESIAN_POINT('',(-0.00745873679850607,0.013718316002365,0.00129568808368499));
#25915=CARTESIAN_POINT('',(-0.00721623836417553,0.0137461093489396,0.0022885807666439));
#25916=CARTESIAN_POINT('',(-0.00678963471291716,0.0137703684299469,0.00319511544670599));
#25917=CARTESIAN_POINT('',(-0.00586854359428379,0.0100021880658147,0.00232352468558585));
#25918=CARTESIAN_POINT('',(-0.00586854666444476,0.0101583123241833,0.00232352584836629));
#25919=CARTESIAN_POINT('',(-0.00598875051569713,0.0104696625508096,0.00237111789406724));
#25920=CARTESIAN_POINT('',(-0.00642351691599961,0.0106633822281906,0.00254325419483785));
#25921=CARTESIAN_POINT('',(-0.00685828316600545,0.0104696620957779,0.00271539041001652));
#25922=CARTESIAN_POINT('',(-0.00697848678069458,0.0101583117238101,0.00276298232952899));
#25923=CARTESIAN_POINT('',(-0.00697848972311123,0.0100021874495698,0.00276298343174812));
#25924=CARTESIAN_POINT('',(0.00749108874705881,-4.87817538710732E-5,0.000441214548496381));
#25925=CARTESIAN_POINT('',(0.00756192879546182,0.000121259456510575,-0.000807448822781952));
#25926=CARTESIAN_POINT('',(0.00732073880436713,0.000291300666892227,-0.0020746366380809));
#25927=CARTESIAN_POINT('',(0.00610734286898242,0.000678055776640972,-0.00464385789087092));
#25928=CARTESIAN_POINT('',(0.00495265952689379,0.000894769676008066,-0.00585998761368964));
#25929=CARTESIAN_POINT('',(0.00214648654660137,0.00132819747474226,-0.00736641318963322));
#25930=CARTESIAN_POINT('',(0.00049499690839756,0.00154491137410936,-0.00765670904275807));
#25931=CARTESIAN_POINT('',(-0.00265670621037452,0.00197833917284356,-0.00719800623814542));
#25932=CARTESIAN_POINT('',(-0.00415691969094279,0.00219505307221066,-0.00644900758040792));
#25933=CARTESIAN_POINT('',(-0.00641745568980185,0.00262848087094487,-0.00420548154343388));
#25934=CARTESIAN_POINT('',(-0.00717777820809264,0.00284519477031198,-0.00271095416419734));
#25935=CARTESIAN_POINT('',(-0.00766019843077886,0.00327862256904619,0.000437190225863992));
#25936=CARTESIAN_POINT('',(-0.00738229613517428,0.0034953364684133,0.00209080723668879));
#25937=CARTESIAN_POINT('',(-0.0058973088636481,0.00392876426714751,0.00490831015468373));
#25938=CARTESIAN_POINT('',(-0.0046902238877265,0.00414547816651461,0.00607219606185387));
#25939=CARTESIAN_POINT('',(-0.00182049443363357,0.00457890596524882,0.00745356085311647));
#25940=CARTESIAN_POINT('',(-0.000157849955462233,0.00479561986461592,0.00767103973720893));
#25941=CARTESIAN_POINT('',(0.00297062710608921,0.00522904766335012,0.00707425910289169));
#25942=CARTESIAN_POINT('',(0.00443645968946931,0.00544576156271722,0.00625999958448199));
#25943=CARTESIAN_POINT('',(0.00659616431998675,0.00587918936145141,0.00391923224552048));
#25944=CARTESIAN_POINT('',(0.00729003636712409,0.00609590326081851,0.00239272442496866));
#25945=CARTESIAN_POINT('',(0.00763356678947157,0.00652933105955269,-0.000773582057105439));
#25946=CARTESIAN_POINT('',(0.00728322516468172,0.00674604495891977,-0.00241338071862772));
#25947=CARTESIAN_POINT('',(0.00567578698717706,0.00717947275765394,-0.00516286883051849));
#25948=CARTESIAN_POINT('',(0.00441869043446227,0.00739618665702102,-0.00627255828088698));
#25949=CARTESIAN_POINT('',(0.00149100660428099,0.00782961445575517,-0.00752639218982749));
#25950=CARTESIAN_POINT('',(-0.000179580673185502,0.00804632835512224,-0.00767053664839951));
#25951=CARTESIAN_POINT('',(-0.00327882363689482,0.00847975615385636,-0.00693682426351677));
#25952=CARTESIAN_POINT('',(-0.00470747932313764,0.00869647005322342,-0.00605896742006202));
#25953=CARTESIAN_POINT('',(-0.00676205316791046,0.00912989785195752,-0.00362531766556786));
#25954=CARTESIAN_POINT('',(-0.00738797132644047,0.00934661175132457,-0.00206952475452845));
#25955=CARTESIAN_POINT('',(-0.00756094562580771,0.0097133646794052,0.000619311369760928));
#25956=CARTESIAN_POINT('',(-0.00738068052708896,0.0098634037081188,0.00173515302320011));
#25957=CARTESIAN_POINT('',(-0.0069762626742443,0.0100134427368324,0.00276211433842094));
#25958=CARTESIAN_POINT('',(0.00749116155653293,-5.25309875529011E-5,0.000441218836871587));
#25959=CARTESIAN_POINT('',(0.00756200229346425,0.000117510222828747,-0.00080745667076322));
#25960=CARTESIAN_POINT('',(0.00732080995812869,0.000287551433210399,-0.00207465680246657));
#25961=CARTESIAN_POINT('',(0.00610740222916858,0.000674306542959144,-0.00464390302674667));
#25962=CARTESIAN_POINT('',(0.00495270766416033,0.000891020442326238,-0.00586004456971178));
#25963=CARTESIAN_POINT('',(0.00214650740933066,0.00132444824106043,-0.00736648478732597));
#25964=CARTESIAN_POINT('',(0.000495001719509243,0.00154116214042753,-0.00765678346197505));
#25965=CARTESIAN_POINT('',(-0.00265673203217274,0.00197458993916174,-0.00719807619901047));
#25966=CARTESIAN_POINT('',(-0.0041569600940333,0.00219130383852884,-0.00644907026139681));
#25967=CARTESIAN_POINT('',(-0.00641751806412282,0.00262473163726305,-0.00420552241852026));
#25968=CARTESIAN_POINT('',(-0.0071778479723518,0.00284144553663015,-0.00271098051325737));
#25969=CARTESIAN_POINT('',(-0.00766027288391087,0.00327487333536436,0.000437194475124882));
#25970=CARTESIAN_POINT('',(-0.00738236788724097,0.00349158723473147,0.00209082755824425));
#25971=CARTESIAN_POINT('',(-0.00589736618241331,0.00392501503346568,0.00490835786089751));
#25972=CARTESIAN_POINT('',(-0.00469026947425555,0.00414172893283278,0.0060722550804314));
#25973=CARTESIAN_POINT('',(-0.00182051212788961,0.00457515673156699,0.00745363329783904));
#25974=CARTESIAN_POINT('',(-0.000157851489681442,0.00479187063093409,0.00767111429571278));
#25975=CARTESIAN_POINT('',(0.00297065597903474,0.0052252984296683,0.00707432786099915));
#25976=CARTESIAN_POINT('',(0.00443650280954275,0.0054420123290354,0.00626006042841178));
#25977=CARTESIAN_POINT('',(0.00659622843126237,0.00587544012776958,0.00391927033841303));
#25978=CARTESIAN_POINT('',(0.00729010722247398,0.00609215402713668,0.00239274768100166));
#25979=CARTESIAN_POINT('',(0.00763364098375792,0.00652558182587087,-0.000773589575919415));
#25980=CARTESIAN_POINT('',(0.00728329595383027,0.00674229572523794,-0.00241340417542911));
#25981=CARTESIAN_POINT('',(0.00567584215286522,0.00717572352397212,-0.00516291901090978));
#25982=CARTESIAN_POINT('',(0.00441873338182783,0.0073924374233392,-0.00627261924688074));
#25983=CARTESIAN_POINT('',(0.00149102109608724,0.00782586522207334,-0.00752646534243265));
#25984=CARTESIAN_POINT('',(-0.000179582418615949,0.00804257912144041,-0.0076706112020136));
#25985=CARTESIAN_POINT('',(-0.00327885550534983,0.00847600692017453,-0.0069368916858293));
#25986=CARTESIAN_POINT('',(-0.00470752507738052,0.00869272081954159,-0.00605902631006405));
#25987=CARTESIAN_POINT('',(-0.00676211889153913,0.00912614861827569,-0.00362535290176405));
#25988=CARTESIAN_POINT('',(-0.00738804313366706,0.00934286251764274,-0.00206954486922928));
#25989=CARTESIAN_POINT('',(-0.00756101911425425,0.00970961544572337,0.000619317389144314));
#25990=CARTESIAN_POINT('',(-0.00738075226345279,0.00985965447443697,0.00173516988798218));
#25991=CARTESIAN_POINT('',(-0.00697633047987761,0.0100096935031506,0.00276214118473116));
#25992=CARTESIAN_POINT('',(0.00749119806593967,-5.62808667625207E-5,0.000441220987224087));
#25993=CARTESIAN_POINT('',(0.00756203914812496,0.000113760343619128,-0.00080746060603598));
#25994=CARTESIAN_POINT('',(0.00732084563729892,0.000283801554000779,-0.00207466691364739));
#25995=CARTESIAN_POINT('',(0.00610743199459687,0.000670556663749525,-0.00464392565957112));
#25996=CARTESIAN_POINT('',(0.00495273180199492,0.000887270563116618,-0.00586007312960187));
#25997=CARTESIAN_POINT('',(0.00214651787068722,0.00132069836185081,-0.00736652068909999));
#25998=CARTESIAN_POINT('',(0.000495004131981458,0.00153741226121791,-0.00765682077856736));
#25999=CARTESIAN_POINT('',(-0.00265674498019283,0.00197084005995212,-0.00719811128001756));
#26000=CARTESIAN_POINT('',(-0.00415698035366135,0.00218755395931922,-0.00644910169200039));
#26001=CARTESIAN_POINT('',(-0.00641754934095159,0.00262098175805343,-0.00420554291482479));
#26002=CARTESIAN_POINT('',(-0.0071778829547733,0.00283769565742053,-0.00271099372566635));
#26003=CARTESIAN_POINT('',(-0.00766031021750945,0.00327112345615474,0.000437196605863993));
#26004=CARTESIAN_POINT('',(-0.00738240386642389,0.00348783735552185,0.0020908377482359));
#26005=CARTESIAN_POINT('',(-0.00589739492419641,0.00392126515425606,0.00490838178258605));
#26006=CARTESIAN_POINT('',(-0.0046902923330545,0.00413797905362316,0.00607228467456428));
#26007=CARTESIAN_POINT('',(-0.0018205210004546,0.00457140685235737,0.00745366962434564));
#26008=CARTESIAN_POINT('',(-0.000157852258996615,0.00478812075172448,0.00767115168214876));
#26009=CARTESIAN_POINT('',(0.00297067045701477,0.00522154855045868,0.00707436233889838));
#26010=CARTESIAN_POINT('',(0.00443652443156816,0.00543826244982578,0.00626009093784488));
#26011=CARTESIAN_POINT('',(0.00659626057906547,0.00587169024855996,0.00391928943962101));
#26012=CARTESIAN_POINT('',(0.00729014275200938,0.00608840414792706,0.00239275934245064));
#26013=CARTESIAN_POINT('',(0.00763367818756156,0.00652183194666125,-0.000773593346135324));
#26014=CARTESIAN_POINT('',(0.00728333145016984,0.00673854584602832,-0.00241341593755091));
#26015=CARTESIAN_POINT('',(0.00567586981501456,0.0071719736447625,-0.00516294417324391));
#26016=CARTESIAN_POINT('',(0.00441875491725102,0.00738868754412958,-0.00627264981752131));
#26017=CARTESIAN_POINT('',(0.00149102836282355,0.00782211534286372,-0.00752650202389819));
#26018=CARTESIAN_POINT('',(-0.000179583293840374,0.00803882924223079,-0.00767064858599767));
#26019=CARTESIAN_POINT('',(-0.0032788714853909,0.00847225704096491,-0.00693692549391075));
#26020=CARTESIAN_POINT('',(-0.00470754802027749,0.00868897094033197,-0.00605905583972435));
#26021=CARTESIAN_POINT('',(-0.00676215184783665,0.00912239873906607,-0.0036253705705171));
#26022=CARTESIAN_POINT('',(-0.00738807914050922,0.00933911263843312,-0.00206955495549626));
#26023=CARTESIAN_POINT('',(-0.00756105596412327,0.00970586556651375,0.000619320407489371));
#26024=CARTESIAN_POINT('',(-0.00738078823476169,0.00985590459522735,0.00173517834461774));
#26025=CARTESIAN_POINT('',(-0.0069763644801705,0.0100059436239409,0.00276215464648008));
#26026=CARTESIAN_POINT('',(0.00749119806593967,-0.000184931740797058,0.000441220987224088));
#26027=CARTESIAN_POINT('',(0.00756203914812497,-1.48905304154092E-5,-0.000807460606035978));
#26028=CARTESIAN_POINT('',(0.00732084563729892,0.000155150679966243,-0.00207466691364739));
#26029=CARTESIAN_POINT('',(0.00610743199459687,0.000541905789714988,-0.00464392565957112));
#26030=CARTESIAN_POINT('',(0.00495273180199493,0.000758619689082079,-0.00586007312960188));
#26031=CARTESIAN_POINT('',(0.00214651787068723,0.00119204748781627,-0.0073665206891));
#26032=CARTESIAN_POINT('',(0.000495004131981461,0.00140876138718337,-0.00765682077856735));
#26033=CARTESIAN_POINT('',(-0.00265674498019281,0.00184218918591758,-0.00719811128001758));
#26034=CARTESIAN_POINT('',(-0.00415698035366134,0.00205890308528468,-0.00644910169200041));
#26035=CARTESIAN_POINT('',(-0.00641754934095157,0.00249233088401889,-0.0042055429148248));
#26036=CARTESIAN_POINT('',(-0.00717788295477331,0.002709044783386,-0.00271099372566636));
#26037=CARTESIAN_POINT('',(-0.00766031021750946,0.00314247258212021,0.000437196605863996));
#26038=CARTESIAN_POINT('',(-0.00738240386642388,0.00335918648148731,0.00209083774823591));
#26039=CARTESIAN_POINT('',(-0.00589739492419643,0.00379261428022152,0.00490838178258604));
#26040=CARTESIAN_POINT('',(-0.00469029233305451,0.00400932817958862,0.00607228467456427));
#26041=CARTESIAN_POINT('',(-0.00182052100045464,0.00444275597832283,0.00745366962434565));
#26042=CARTESIAN_POINT('',(-0.000157852258996646,0.00465946987768994,0.00767115168214877));
#26043=CARTESIAN_POINT('',(0.00297067045701475,0.00509289767642415,0.00707436233889838));
#26044=CARTESIAN_POINT('',(0.00443652443156816,0.00530961157579124,0.00626009093784489));
#26045=CARTESIAN_POINT('',(0.00659626057906547,0.00574303937452543,0.00391928943962101));
#26046=CARTESIAN_POINT('',(0.00729014275200938,0.00595975327389252,0.00239275934245064));
#26047=CARTESIAN_POINT('',(0.00763367818756156,0.00639318107262671,-0.000773593346135321));
#26048=CARTESIAN_POINT('',(0.00728333145016984,0.00660989497199379,-0.00241341593755092));
#26049=CARTESIAN_POINT('',(0.00567586981501457,0.00704332277072797,-0.00516294417324391));
#26050=CARTESIAN_POINT('',(0.00441875491725102,0.00726003667009504,-0.00627264981752131));
#26051=CARTESIAN_POINT('',(0.00149102836282355,0.00769346446882918,-0.00752650202389819));
#26052=CARTESIAN_POINT('',(-0.000179583293840374,0.00791017836819625,-0.0076706485859977));
#26053=CARTESIAN_POINT('',(-0.0032788714853909,0.00834360616693037,-0.00693692549391075));
#26054=CARTESIAN_POINT('',(-0.00470754802027749,0.00856032006629743,-0.00605905583972436));
#26055=CARTESIAN_POINT('',(-0.00676215184783666,0.00899374786503153,-0.0036253705705171));
#26056=CARTESIAN_POINT('',(-0.00738807914050924,0.00921046176439859,-0.00206955495549626));
#26057=CARTESIAN_POINT('',(-0.00756105596412329,0.00957721469247922,0.000619320407489369));
#26058=CARTESIAN_POINT('',(-0.0073807882347617,0.00972725372119282,0.00173517834461774));
#26059=CARTESIAN_POINT('',(-0.0069763644801705,0.00987729274990641,0.00276215464648008));
#26060=CARTESIAN_POINT('',(0.00745069368358014,-0.000309832735627617,0.000438835336302264));
#26061=CARTESIAN_POINT('',(0.00752115173300428,-0.000139791525245969,-0.000803094723190638));
#26062=CARTESIAN_POINT('',(0.00728126233856912,3.02496851356814E-5,-0.00206344933520408));
#26063=CARTESIAN_POINT('',(0.00607440953829996,0.000417004794884424,-0.00461881627934798));
#26064=CARTESIAN_POINT('',(0.00492595272862557,0.000633718694251518,-0.00582838812533328));
#26065=CARTESIAN_POINT('',(0.00213491179916027,0.00106714649298571,-0.00732669042856967));
#26066=CARTESIAN_POINT('',(0.000492327679369366,0.00128386039235281,-0.00761542088582076));
#26067=CARTESIAN_POINT('',(-0.00264238014648235,0.00171728819108701,-0.00715919159734653));
#26068=CARTESIAN_POINT('',(-0.00413450385254315,0.00193400209045411,-0.00641423185162121));
#26069=CARTESIAN_POINT('',(-0.0063828501019208,0.00236742988918832,-0.00418280383934554));
#26070=CARTESIAN_POINT('',(-0.00713907264523764,0.00258414378855543,-0.0026963355727952));
#26071=CARTESIAN_POINT('',(-0.00761889145761131,0.00301757158728964,0.00043483271448983));
#26072=CARTESIAN_POINT('',(-0.00734248772666813,0.00323428548665675,0.00207953273522452));
#26073=CARTESIAN_POINT('',(-0.00586550812360295,0.00366771328539096,0.00488184250666003));
#26074=CARTESIAN_POINT('',(-0.00466493225148094,0.00388442718475806,0.00603945225736085));
#26075=CARTESIAN_POINT('',(-0.00181067757113305,0.00431785498349227,0.00741336815563682));
#26076=CARTESIAN_POINT('',(-0.000156998762907161,0.00453456888285937,0.00762967430321196));
#26077=CARTESIAN_POINT('',(0.00295460825027614,0.00496799668159358,0.00703611175806975));
#26078=CARTESIAN_POINT('',(0.00441253645523355,0.00518471058096067,0.0062262430653524));
#26079=CARTESIAN_POINT('',(0.0065605950609086,0.00561813837969487,0.00389809811659861));
#26080=CARTESIAN_POINT('',(0.00725072546162622,0.00583485227906196,0.00237982186056218));
#26081=CARTESIAN_POINT('',(0.00759240342518085,0.00626828007779614,-0.000769410581188136));
#26082=CARTESIAN_POINT('',(0.00724395098801784,0.00648499397716323,-0.00240036676690202));
#26083=CARTESIAN_POINT('',(0.00564518078514423,0.0069184217758974,-0.00513502849633172));
#26084=CARTESIAN_POINT('',(0.00439486301943362,0.00713513567526448,-0.00623873404004755));
#26085=CARTESIAN_POINT('',(0.00148296647707642,0.00756856347399862,-0.00748580675551491));
#26086=CARTESIAN_POINT('',(-0.000178612299570156,0.00778527737336569,-0.00762917392726645));
#26087=CARTESIAN_POINT('',(-0.00326114285731525,0.00821870517209982,-0.00689941802446038));
#26088=CARTESIAN_POINT('',(-0.00468209463841377,0.00843541907146688,-0.00602629494990277));
#26089=CARTESIAN_POINT('',(-0.00672558936722847,0.00886884687020098,-0.00360576844619859));
#26090=CARTESIAN_POINT('',(-0.00734813231494467,0.00908556076956803,-0.00205836501705201));
#26091=CARTESIAN_POINT('',(-0.0075201738650095,0.00945231369764866,0.000615971785497641));
#26092=CARTESIAN_POINT('',(-0.00734088083061299,0.00960235272636225,0.00172579635704863));
#26093=CARTESIAN_POINT('',(-0.00693864376688846,0.00975239175507584,0.00274721987009954));
#26094=CARTESIAN_POINT('',(0.00730414745151005,-0.000511926790492136,0.000430203970181813));
#26095=CARTESIAN_POINT('',(0.00737321967538551,-0.000341885580110489,-0.000787298810665295));
#26096=CARTESIAN_POINT('',(0.00713804861837784,-0.00017184436972884,-0.00202286375512473));
#26097=CARTESIAN_POINT('',(0.00595493316902575,0.000214910740019902,-0.00452796968826424));
#26098=CARTESIAN_POINT('',(0.00482906513098801,0.000431624639386996,-0.00571375070295582));
#26099=CARTESIAN_POINT('',(0.00209292063789989,0.000865052438121187,-0.00718258319219017));
#26100=CARTESIAN_POINT('',(0.000482644182849518,0.00108176633748828,-0.00746563466673295));
#26101=CARTESIAN_POINT('',(-0.0025904076898751,0.00151519413622248,-0.00701837886261136));
#26102=CARTESIAN_POINT('',(-0.00405318310754934,0.00173190803558958,-0.00628807158394699));
#26103=CARTESIAN_POINT('',(-0.00625730707572365,0.00216533583432379,-0.00410053309138883));
#26104=CARTESIAN_POINT('',(-0.00699865562622372,0.0023820497336909,-0.00264330187749505));
#26105=CARTESIAN_POINT('',(-0.00746903697652796,0.00281547753242511,0.000426280075152402));
#26106=CARTESIAN_POINT('',(-0.00719806977633214,0.00303219143179222,0.00203863081390608));
#26107=CARTESIAN_POINT('',(-0.00575014059526331,0.00346561923052643,0.0047858225043229));
#26108=CARTESIAN_POINT('',(-0.0045731786143903,0.00368233312989354,0.00592066345598604));
#26109=CARTESIAN_POINT('',(-0.00177506370928174,0.00411576092862775,0.00726755607205175));
#26110=CARTESIAN_POINT('',(-0.000153910785046186,0.00433247482799485,0.00747960773645432));
#26111=CARTESIAN_POINT('',(0.0028964946403615,0.00476590262672905,0.0068977198565423));
#26112=CARTESIAN_POINT('',(0.00432574714153362,0.00498261652609615,0.00610378031222772));
#26113=CARTESIAN_POINT('',(0.00643155600399064,0.00541604432483035,0.00382142718963702));
#26114=CARTESIAN_POINT('',(0.00710811236527552,0.00563275822419744,0.0023330136113609));
#26115=CARTESIAN_POINT('',(0.00744306993200983,0.00606618602293162,-0.000754277195442262));
#26116=CARTESIAN_POINT('',(0.00710147113745925,0.00628289992229871,-0.00235315442396932));
#26117=CARTESIAN_POINT('',(0.00553414683199158,0.00671632772103287,-0.00503402862844448));
#26118=CARTESIAN_POINT('',(0.00430842132107451,0.00693304162039995,-0.00611602560439259));
#26119=CARTESIAN_POINT('',(0.0014537983004299,0.0073664694191341,-0.0073385698913229));
#26120=CARTESIAN_POINT('',(-0.000175099209297627,0.00758318331850117,-0.00747911720230511));
#26121=CARTESIAN_POINT('',(-0.00319700007836367,0.0080166111172353,-0.00676371472515694));
#26122=CARTESIAN_POINT('',(-0.00459000343770219,0.00823332501660236,-0.00590776493702659));
#26123=CARTESIAN_POINT('',(-0.00659330506967508,0.00866675281533646,-0.00353484729416248));
#26124=CARTESIAN_POINT('',(-0.00720360334230944,0.00888346671470351,-0.00201787943942874));
#26125=CARTESIAN_POINT('',(-0.00737226104088444,0.00925021964278414,0.00060385635731609));
#26126=CARTESIAN_POINT('',(-0.00719649448600018,0.00940025867149773,0.00169185200714157));
#26127=CARTESIAN_POINT('',(-0.00680216894415417,0.00955029770021132,0.00269318534154035));
#26128=CARTESIAN_POINT('',(0.00719810560179949,-0.000589119850526096,0.000423958254983186));
#26129=CARTESIAN_POINT('',(0.00726617503288742,-0.000419078640144449,-0.000775868780985295));
#26130=CARTESIAN_POINT('',(0.00703441819691637,-0.000249037429762799,-0.00199349575348868));
#26131=CARTESIAN_POINT('',(0.00586847925604845,0.000137717679985943,-0.00446223247740363));
#26132=CARTESIAN_POINT('',(0.0047589566067198,0.000354431579353036,-0.00563079828484695));
#26133=CARTESIAN_POINT('',(0.00206253554816646,0.000787859378087228,-0.00707830621634101));
#26134=CARTESIAN_POINT('',(0.000475637138941769,0.00100457327745433,-0.00735724834039175));
#26135=CARTESIAN_POINT('',(-0.00255280006697832,0.00143800107618853,-0.00691648581054723));
#26136=CARTESIAN_POINT('',(-0.00399433886367372,0.00165471497555563,-0.00619678115665198));
#26137=CARTESIAN_POINT('',(-0.00616646328855728,0.00208814277428983,-0.00404100141891139));
#26138=CARTESIAN_POINT('',(-0.00689704891674545,0.00230485667365694,-0.00260492633506608));
#26139=CARTESIAN_POINT('',(-0.00736060125534275,0.00273828447239115,0.000420091327189137));
#26140=CARTESIAN_POINT('',(-0.00709356796575188,0.00295499837175826,0.00200903390559903));
#26141=CARTESIAN_POINT('',(-0.00566665986751712,0.00338842617049247,0.00471634177791178));
#26142=CARTESIAN_POINT('',(-0.00450678505887322,0.00360514006985957,0.00583470707181465));
#26143=CARTESIAN_POINT('',(-0.00174929327675202,0.00403856786859379,0.0071620454571755));
#26144=CARTESIAN_POINT('',(-0.000151676303274696,0.00425528176796089,0.00737101854863349));
#26145=CARTESIAN_POINT('',(0.00285444323718545,0.00468870956669509,0.0067975785358435));
#26146=CARTESIAN_POINT('',(0.00426294580416829,0.00490542346606219,0.00601516543159552));
#26147=CARTESIAN_POINT('',(0.00633818246522956,0.00533885126479639,0.00376594758569781));
#26148=CARTESIAN_POINT('',(0.00700491655930799,0.00555556516416348,0.00229914284404808));
#26149=CARTESIAN_POINT('',(0.00733501120121953,0.00598899296289766,-0.000743326574643574));
#26150=CARTESIAN_POINT('',(0.00699837174905264,0.00620570686226475,-0.0023189912516855));
#26151=CARTESIAN_POINT('',(0.00545380190870928,0.00663913466099891,-0.00496094443746942));
#26152=CARTESIAN_POINT('',(0.0042458715205328,0.00685584856036599,-0.00602723294621141));
#26153=CARTESIAN_POINT('',(0.0014326920095305,0.00728927635910014,-0.00723202829551418));
#26154=CARTESIAN_POINT('',(-0.000172557113295315,0.00750599025846721,-0.00737053513607497));
#26155=CARTESIAN_POINT('',(-0.00315058592748773,0.00793941805720134,-0.00666551889530388));
#26156=CARTESIAN_POINT('',(-0.00452336561885433,0.00815613195656839,-0.00582199581397199));
#26157=CARTESIAN_POINT('',(-0.00649758325272985,0.0085895597553025,-0.0034835282664449));
#26158=CARTESIAN_POINT('',(-0.00709902119523878,0.00880627365466954,-0.0019885838002497));
#26159=CARTESIAN_POINT('',(-0.00726523031587315,0.00917302658275018,0.000595089551126265));
#26160=CARTESIAN_POINT('',(-0.00709201554553608,0.00932306561146377,0.00166728964480362));
#26161=CARTESIAN_POINT('',(-0.00670341483470192,0.00947310464017736,0.00265408558936171));
#26162=CARTESIAN_POINT('',(0.00696098881738686,-0.000666312910560056,0.000409992411230955));
#26163=CARTESIAN_POINT('',(0.00702681593563455,-0.000496271700178409,-0.000750310457635969));
#26164=CARTESIAN_POINT('',(0.00680269352999158,-0.000326230489796759,-0.00192782690546716));
#26165=CARTESIAN_POINT('',(0.00567516242971034,6.05246199519836E-5,-0.00431523960526808));
#26166=CARTESIAN_POINT('',(0.0046021891806539,0.000277238519319077,-0.00544531103905756));
#26167=CARTESIAN_POINT('',(0.00199459242202009,0.000710666318053268,-0.00684513580985419));
#26168=CARTESIAN_POINT('',(0.000459968912442717,0.000927380217420367,-0.00711488914686134));
#26169=CARTESIAN_POINT('',(-0.00246870686570896,0.00136080801615457,-0.00668864601969691));
#26170=CARTESIAN_POINT('',(-0.00386275913428326,0.00157752191552167,-0.00599264955552532));
#26171=CARTESIAN_POINT('',(-0.00596333040511978,0.00201094971425588,-0.00390788455243758));
#26172=CARTESIAN_POINT('',(-0.00666984940738199,0.00222766361362299,-0.00251911601352144));
#26173=CARTESIAN_POINT('',(-0.00711813161158341,0.0026610914123572,0.000406252866047666));
#26174=CARTESIAN_POINT('',(-0.00685989481352263,0.0028778053117243,0.00194285320670063));
#26175=CARTESIAN_POINT('',(-0.0054799912854655,0.00331123311045851,0.00456097815053046));
#26176=CARTESIAN_POINT('',(-0.00435832455546914,0.00352794700982562,0.00564250275370733));
#26177=CARTESIAN_POINT('',(-0.00169166883780598,0.00396137480855983,0.00692611654996442));
#26178=CARTESIAN_POINT('',(-0.000146679850139156,0.00417808870792693,0.00712820574304464));
#26179=CARTESIAN_POINT('',(0.00276041344113459,0.00461151650666113,0.00657365573540438));
#26180=CARTESIAN_POINT('',(0.00412251774474152,0.00482823040602823,0.0058170165346839));
#26181=CARTESIAN_POINT('',(0.00612939288526007,0.00526165820476242,0.00364189141992498));
#26182=CARTESIAN_POINT('',(0.00677416372217169,0.00547837210412952,0.00222340550588654));
#26183=CARTESIAN_POINT('',(0.00709338453361007,0.0059117999028637,-0.000718840242141883));
#26184=CARTESIAN_POINT('',(0.00676783450813683,0.00612851380223079,-0.00224260007613187));
#26185=CARTESIAN_POINT('',(0.00527414519860304,0.00656194160096496,-0.00479752321836861));
#26186=CARTESIAN_POINT('',(0.00410600591454249,0.00677865550033204,-0.00582868652661536));
#26187=CARTESIAN_POINT('',(0.00138549690832657,0.00721208329906618,-0.00699379404485457));
#26188=CARTESIAN_POINT('',(-0.000166872813828816,0.00742879719843325,-0.00712773825484702));
#26189=CARTESIAN_POINT('',(-0.0030468007310112,0.00786222499716737,-0.00644594634464542));
#26190=CARTESIAN_POINT('',(-0.0043743589260382,0.00807893889653443,-0.00563021022445137));
#26191=CARTESIAN_POINT('',(-0.00628354276311055,0.00851236669526854,-0.00336877543192919));
#26192=CARTESIAN_POINT('',(-0.00686516840515589,0.00872908059463558,-0.00192307675960106));
#26193=CARTESIAN_POINT('',(-0.00702590233906683,0.00909583352271622,0.000575486376540256));
#26194=CARTESIAN_POINT('',(-0.00685839353244121,0.00924587255142981,0.00161236653292798));
#26195=CARTESIAN_POINT('',(-0.00648259393290923,0.0093959115801434,0.00256665588558687));
#26196=CARTESIAN_POINT('',(0.0068299138826848,-0.000666312910560056,0.000402272282677348));
#26197=CARTESIAN_POINT('',(0.00689450148087976,-0.000496271700178409,-0.000736182163966646));
#26198=CARTESIAN_POINT('',(0.00667459928452825,-0.000326230489796759,-0.00189152605908168));
#26199=CARTESIAN_POINT('',(0.00556829951634954,6.05246199519835E-5,-0.00423398394399313));
#26200=CARTESIAN_POINT('',(0.00451553027885621,0.000277238519319077,-0.00534277621137702));
#26201=CARTESIAN_POINT('',(0.00195703438560715,0.000710666318053268,-0.00671624237921652));
#26202=CARTESIAN_POINT('',(0.000451307729851413,0.000927380217420367,-0.00698091627967214));
#26203=CARTESIAN_POINT('',(-0.00242222128733637,0.00136080801615457,-0.00656269928091072));
#26204=CARTESIAN_POINT('',(-0.00379002364876842,0.00157752191552167,-0.00587980838169368));
#26205=CARTESIAN_POINT('',(-0.00585104130884863,0.00201094971425588,-0.00383429935844122));
#26206=CARTESIAN_POINT('',(-0.00654425660749678,0.00222766361362299,-0.00247168123440579));
#26207=CARTESIAN_POINT('',(-0.00698409768900928,0.0026610914123572,0.000398603152869458));
#26208=CARTESIAN_POINT('',(-0.00673072347187363,0.0028778053117243,0.00190626941610928));
#26209=CARTESIAN_POINT('',(-0.00537680343116006,0.00331123311045851,0.00447509524956026));
#26210=CARTESIAN_POINT('',(-0.00427625760758213,0.00352794700982562,0.00553625481977141));
#26211=CARTESIAN_POINT('',(-0.00165981483138966,0.00396137480855983,0.00679569825762958));
#26212=CARTESIAN_POINT('',(-0.000143917878775103,0.00417808870792693,0.00699398212527661));
#26213=CARTESIAN_POINT('',(0.00270843504825977,0.00461151650666113,0.00644987425566405));
#26214=CARTESIAN_POINT('',(0.00404489102268007,0.00482823040602823,0.00570748251840448));
#26215=CARTESIAN_POINT('',(0.00601397684405166,0.00526165820476243,0.00357331485809136));
#26216=CARTESIAN_POINT('',(0.00664660669100294,0.00547837210412952,0.00218153893503782));
#26217=CARTESIAN_POINT('',(0.00695981659679091,0.0059117999028637,-0.000705304530438881));
#26218=CARTESIAN_POINT('',(0.00664039665562761,0.00612851380223079,-0.00220037207286204));
#26219=CARTESIAN_POINT('',(0.0051748334117791,0.00656194160096496,-0.00470718619024285));
#26220=CARTESIAN_POINT('',(0.0040286901090939,0.00677865550033204,-0.00571893276520051));
#26221=CARTESIAN_POINT('',(0.00135940809802203,0.00721208329906618,-0.00686210139000368));
#26222=CARTESIAN_POINT('',(-0.00016373061036463,0.00742879719843325,-0.00699352343984919));
#26223=CARTESIAN_POINT('',(-0.00298942968541062,0.00786222499716738,-0.00632456962384003));
#26224=CARTESIAN_POINT('',(-0.00429199005206994,0.00807893889653443,-0.00552419375798534));
#26225=CARTESIAN_POINT('',(-0.00616522409043646,0.00851236669526854,-0.00330534162513106));
#26226=CARTESIAN_POINT('',(-0.00673589776214366,0.00872908059463559,-0.00188686535813147));
#26227=CARTESIAN_POINT('',(-0.00689360508727178,0.00909583352271622,0.00056465000814407));
#26228=CARTESIAN_POINT('',(-0.00672925045981043,0.00924587255142981,0.00158200578339029));
#26229=CARTESIAN_POINT('',(-0.00636052714056878,0.0093959115801434,0.00251832593399067));
#26230=CARTESIAN_POINT('',(0.00659279709827217,-0.000589119850526096,0.000388306438925115));
#26231=CARTESIAN_POINT('',(0.00665514238362688,-0.000419078640144449,-0.000710623840617322));
#26232=CARTESIAN_POINT('',(0.00644287461760345,-0.000249037429762799,-0.00182585721106015));
#26233=CARTESIAN_POINT('',(0.00537498269001143,0.000137717679985943,-0.00408699107185757));
#26234=CARTESIAN_POINT('',(0.00435876285279031,0.000354431579353036,-0.00515728896558762));
#26235=CARTESIAN_POINT('',(0.00188909125946077,0.000787859378087228,-0.0064830719727297));
#26236=CARTESIAN_POINT('',(0.000435639503352361,0.00100457327745433,-0.00673855708614173));
#26237=CARTESIAN_POINT('',(-0.00233812808606701,0.00143800107618853,-0.0063348594900604));
#26238=CARTESIAN_POINT('',(-0.00365844391937797,0.00165471497555563,-0.00567567678056703));
#26239=CARTESIAN_POINT('',(-0.00564790842541112,0.00208814277428983,-0.00370118249196741));
#26240=CARTESIAN_POINT('',(-0.00631705709813331,0.00230485667365694,-0.00238587091286116));
#26241=CARTESIAN_POINT('',(-0.00674162804524994,0.00273828447239115,0.000384764691727985));
#26242=CARTESIAN_POINT('',(-0.00649705031964438,0.00295499837175826,0.00184008871721088));
#26243=CARTESIAN_POINT('',(-0.00519013484910844,0.00338842617049247,0.00431973162217894));
#26244=CARTESIAN_POINT('',(-0.00412779710417805,0.00360514006985957,0.0053440505016641));
#26245=CARTESIAN_POINT('',(-0.00160219039244362,0.00403856786859379,0.0065597693504185));
#26246=CARTESIAN_POINT('',(-0.000138921425639559,0.00425528176796089,0.00675116931968775));
#26247=CARTESIAN_POINT('',(0.0026144052522089,0.00468870956669509,0.00622595145522493));
#26248=CARTESIAN_POINT('',(0.00390446296325331,0.00490542346606219,0.00550933362149286));
#26249=CARTESIAN_POINT('',(0.00580518726408218,0.00533885126479638,0.00344925869231854));
#26250=CARTESIAN_POINT('',(0.00641585385386665,0.00555556516416348,0.00210580159687627));
#26251=CARTESIAN_POINT('',(0.00671818992918146,0.00598899296289766,-0.000680818197937192));
#26252=CARTESIAN_POINT('',(0.0064098594147118,0.00620570686226475,-0.0021239808973084));
#26253=CARTESIAN_POINT('',(0.00499517670167286,0.00663913466099892,-0.00454376497114204));
#26254=CARTESIAN_POINT('',(0.00388882450310359,0.00685584856036599,-0.00552038634560447));
#26255=CARTESIAN_POINT('',(0.00131221299681809,0.00728927635910014,-0.00662386713934407));
#26256=CARTESIAN_POINT('',(-0.000158046310898131,0.00750599025846721,-0.00675072655862124));
#26257=CARTESIAN_POINT('',(-0.00288564448893408,0.00793941805720134,-0.00610499707318157));
#26258=CARTESIAN_POINT('',(-0.00414298335925381,0.0081561319565684,-0.00533240816846472));
#26259=CARTESIAN_POINT('',(-0.00595118360081716,0.0085895597553025,-0.00319058879061535));
#26260=CARTESIAN_POINT('',(-0.00650204497206078,0.00880627365466955,-0.00182135831748283));
#26261=CARTESIAN_POINT('',(-0.00665427711046546,0.00917302658275018,0.000545046833558058));
#26262=CARTESIAN_POINT('',(-0.00649562844671556,0.00932306561146377,0.00152708267151465));
#26263=CARTESIAN_POINT('',(-0.00613970623877609,0.00947310464017736,0.00243089623021583));
#26264=CARTESIAN_POINT('',(0.00648675524856161,-0.000511926790492136,0.000382060723726489));
#26265=CARTESIAN_POINT('',(0.0065480977411288,-0.000341885580110489,-0.00069919381093732));
#26266=CARTESIAN_POINT('',(0.00633924419614199,-0.00017184436972884,-0.0017964892094241));
#26267=CARTESIAN_POINT('',(0.00528852877703413,0.000214910740019903,-0.00402125386099697));
#26268=CARTESIAN_POINT('',(0.00428865432852211,0.000431624639386996,-0.00507433654747875));
#26269=CARTESIAN_POINT('',(0.00185870616972735,0.000865052438121187,-0.00637879499688054));
#26270=CARTESIAN_POINT('',(0.000428632459444612,0.00108176633748828,-0.00663017075980053));
#26271=CARTESIAN_POINT('',(-0.00230052046317024,0.00151519413622248,-0.00623296643799627));
#26272=CARTESIAN_POINT('',(-0.00359959967550236,0.00173190803558958,-0.00558438635327201));
#26273=CARTESIAN_POINT('',(-0.00555706463824476,0.00216533583432379,-0.00364165081948996));
#26274=CARTESIAN_POINT('',(-0.00621545038865505,0.0023820497336909,-0.00234749537043218));
#26275=CARTESIAN_POINT('',(-0.00663319232406474,0.00281547753242511,0.000378575943764719));
#26276=CARTESIAN_POINT('',(-0.00639254850906414,0.00303219143179222,0.00181049180890383));
#26277=CARTESIAN_POINT('',(-0.00510665412136226,0.00346561923052643,0.00425025089576781));
#26278=CARTESIAN_POINT('',(-0.00406140354866099,0.00368233312989354,0.00525809411749271));
#26279=CARTESIAN_POINT('',(-0.00157641995991389,0.00411576092862774,0.00645425873554226));
#26280=CARTESIAN_POINT('',(-0.000136686943868066,0.00433247482799485,0.00664258013186692));
#26281=CARTESIAN_POINT('',(0.00257235384903287,0.00476590262672905,0.00612581013452613));
#26282=CARTESIAN_POINT('',(0.00384166162588797,0.00498261652609615,0.00542071874086066));
#26283=CARTESIAN_POINT('',(0.00571181372532109,0.00541604432483035,0.00339377908837933));
#26284=CARTESIAN_POINT('',(0.00631265804789911,0.00563275822419744,0.00207193082956346));
#26285=CARTESIAN_POINT('',(0.00661013119839116,0.00606618602293162,-0.000669867577138504));
#26286=CARTESIAN_POINT('',(0.0063067600263052,0.00628289992229871,-0.00208981772502459));
#26287=CARTESIAN_POINT('',(0.00491483177839056,0.00671632772103287,-0.00447068078016699));
#26288=CARTESIAN_POINT('',(0.00382627470256189,0.00693304162039996,-0.00543159368742329));
#26289=CARTESIAN_POINT('',(0.0012911067059187,0.0073664694191341,-0.00651732554353535));
#26290=CARTESIAN_POINT('',(-0.00015550421489582,0.00758318331850118,-0.00664214449239111));
#26291=CARTESIAN_POINT('',(-0.00283923033805814,0.0080166111172353,-0.0060068012433285));
#26292=CARTESIAN_POINT('',(-0.00407634554040595,0.00823332501660236,-0.00524663904541012));
#26293=CARTESIAN_POINT('',(-0.00585546178387193,0.00866675281533646,-0.00313926976289777));
#26294=CARTESIAN_POINT('',(-0.00639746282499011,0.00888346671470351,-0.00179206267830379));
#26295=CARTESIAN_POINT('',(-0.00654724638545417,0.00925021964278415,0.000536280027368236));
#26296=CARTESIAN_POINT('',(-0.00639114950625147,0.00940025867149774,0.0015025203091767));
#26297=CARTESIAN_POINT('',(-0.00604095212932383,0.00955029770021133,0.00239179647803719));
#26298=CARTESIAN_POINT('',(0.00634020901649153,-0.000309832735627617,0.000373429357606039));
#26299=CARTESIAN_POINT('',(0.00640016568351004,-0.000139791525245969,-0.000683397898411977));
#26300=CARTESIAN_POINT('',(0.00619603047595072,3.0249685135681E-5,-0.00175590362934475));
#26301=CARTESIAN_POINT('',(0.00516905240775992,0.000417004794884424,-0.00393040726991323));
#26302=CARTESIAN_POINT('',(0.00419176673088455,0.000633718694251517,-0.0049596991251013));
#26303=CARTESIAN_POINT('',(0.00181671500846697,0.00106714649298571,-0.00623468776050105));
#26304=CARTESIAN_POINT('',(0.000418948962924764,0.00128386039235281,-0.00648038454071273));
#26305=CARTESIAN_POINT('',(-0.00224854800656299,0.00171728819108701,-0.0060921537032611));
#26306=CARTESIAN_POINT('',(-0.00351827893050854,0.00193400209045412,-0.0054582260855978));
#26307=CARTESIAN_POINT('',(-0.0054315216120476,0.00236742988918832,-0.00355938007153327));
#26308=CARTESIAN_POINT('',(-0.00607503336964112,0.00258414378855543,-0.00229446167513204));
#26309=CARTESIAN_POINT('',(-0.00648333784298138,0.00301757158728964,0.000370023304427295));
#26310=CARTESIAN_POINT('',(-0.00624813055872813,0.00323428548665674,0.00176958988758539));
#26311=CARTESIAN_POINT('',(-0.0049912865930226,0.00366771328539096,0.00415423089343069));
#26312=CARTESIAN_POINT('',(-0.00396964991157034,0.00388442718475806,0.00513930531611789));
#26313=CARTESIAN_POINT('',(-0.00154080609806258,0.00431785498349227,0.00630844665195719));
#26314=CARTESIAN_POINT('',(-0.000133598966007101,0.00453456888285937,0.00649251356510929));
#26315=CARTESIAN_POINT('',(0.00251424023911821,0.00496799668159358,0.00598741823299868));
#26316=CARTESIAN_POINT('',(0.00375487231218804,0.00518471058096067,0.00529825598773598));
#26317=CARTESIAN_POINT('',(0.00558277466840314,0.00561813837969487,0.00331710816141773));
#26318=CARTESIAN_POINT('',(0.00617004495154841,0.00583485227906196,0.00202512258036218));
#26319=CARTESIAN_POINT('',(0.00646079770522014,0.00626828007779614,-0.000654734191392628));
#26320=CARTESIAN_POINT('',(0.0061642801757466,0.00648499397716323,-0.00204260538209188));
#26321=CARTESIAN_POINT('',(0.00480379782523792,0.00691842177589739,-0.00436968091227974));
#26322=CARTESIAN_POINT('',(0.00373983300420278,0.00713513567526448,-0.00530888525176834));
#26323=CARTESIAN_POINT('',(0.00126193852927218,0.00756856347399863,-0.00637008867934335));
#26324=CARTESIAN_POINT('',(-0.00015199112462329,0.00778527737336569,-0.00649208776742977));
#26325=CARTESIAN_POINT('',(-0.00277508755910656,0.00821870517209982,-0.00587109794402506));
#26326=CARTESIAN_POINT('',(-0.00398425433969437,0.00843541907146687,-0.00512810903253394));
#26327=CARTESIAN_POINT('',(-0.00572317748631853,0.00886884687020098,-0.00306834861086167));
#26328=CARTESIAN_POINT('',(-0.00625293385235488,0.00908556076956803,-0.00175157710068052));
#26329=CARTESIAN_POINT('',(-0.00639933356132911,0.00945231369764866,0.000524164599186684));
#26330=CARTESIAN_POINT('',(-0.00624676316163866,0.00960235272636225,0.00146857595926964));
#26331=CARTESIAN_POINT('',(-0.00590447730658955,0.00975239175507584,0.00233776194947801));
#26332=CARTESIAN_POINT('',(0.00629970463413201,-0.000184931740797059,0.000371043706684215));
#26333=CARTESIAN_POINT('',(0.00635927826838935,-1.48905304154102E-5,-0.000679032015566637));
#26334=CARTESIAN_POINT('',(0.00615644717722092,0.000155150679966241,-0.00174468605090144));
#26335=CARTESIAN_POINT('',(0.00513602995146302,0.000541905789714986,-0.00390529788969009));
#26336=CARTESIAN_POINT('',(0.00416498765751519,0.00075861968908208,-0.00492801412083271));
#26337=CARTESIAN_POINT('',(0.00180510893694002,0.00119204748781627,-0.00619485749997073));
#26338=CARTESIAN_POINT('',(0.000416272510312666,0.00140876138718337,-0.00643898464796613));
#26339=CARTESIAN_POINT('',(-0.00223418317285251,0.00184218918591758,-0.00605323402059007));
#26340=CARTESIAN_POINT('',(-0.00349580242939034,0.00205890308528468,-0.00542335624521861));
#26341=CARTESIAN_POINT('',(-0.00539682237301682,0.00249233088401889,-0.00353664099605402));
#26342=CARTESIAN_POINT('',(-0.00603622306010546,0.002709044783386,-0.00227980352226088));
#26343=CARTESIAN_POINT('',(-0.00644191908308324,0.00314247258212021,0.000367659413053137));
#26344=CARTESIAN_POINT('',(-0.00620821441897237,0.00335918648148731,0.00175828487457401));
#26345=CARTESIAN_POINT('',(-0.00495939979242913,0.00379261428022152,0.00412769161750468));
#26346=CARTESIAN_POINT('',(-0.00394428982999677,0.00400932817958863,0.00510647289891446));
#26347=CARTESIAN_POINT('',(-0.00153096266874102,0.00444275597832284,0.00626814518324836));
#26348=CARTESIAN_POINT('',(-0.000132745469917628,0.00465946987768994,0.00645103618617248));
#26349=CARTESIAN_POINT('',(0.00249817803237959,0.00509289767642414,0.00594916765217005));
#26350=CARTESIAN_POINT('',(0.00373088433585343,0.00530961157579123,0.0052644081152435));
#26351=CARTESIAN_POINT('',(0.00554710915024626,0.00574303937452542,0.00329591683839534));
#26352=CARTESIAN_POINT('',(0.00613062766116525,0.00595975327389252,0.00201218509847372));
#26353=CARTESIAN_POINT('',(0.00641952294283942,0.0063931810726267,-0.000650551426445439));
#26354=CARTESIAN_POINT('',(0.0061248997135946,0.00660989497199379,-0.00202955621144299));
#26355=CARTESIAN_POINT('',(0.00477310879536758,0.00704332277072796,-0.00434176523536755));
#26356=CARTESIAN_POINT('',(0.00371594110638537,0.00726003667009504,-0.00527496947429457));
#26357=CARTESIAN_POINT('',(0.00125387664352505,0.00769346446882918,-0.00632939341096007));
#26358=CARTESIAN_POINT('',(-0.00015102013035307,0.00791017836819625,-0.00645061310869855));
#26359=CARTESIAN_POINT('',(-0.00275735893103092,0.00834360616693037,-0.0058335904745747));
#26360=CARTESIAN_POINT('',(-0.00395880095783066,0.00856032006629742,-0.00509534814271236));
#26361=CARTESIAN_POINT('',(-0.00568661500571035,0.00899374786503153,-0.00304874648654315));
#26362=CARTESIAN_POINT('',(-0.00621298702679032,0.00921046176439858,-0.00174038716223627));
#26363=CARTESIAN_POINT('',(-0.00635845146221533,0.00957721469247922,0.000520815977194954));
#26364=CARTESIAN_POINT('',(-0.00620685575748995,0.0097272537211928,0.00145919397170054));
#26365=CARTESIAN_POINT('',(-0.00586675659330751,0.00987729274990639,0.00232282717309746));
#26366=CARTESIAN_POINT('',(0.00629970463413201,-5.62808667607383E-5,0.000371043706684215));
#26367=CARTESIAN_POINT('',(0.00635927826838935,0.00011376034362091,-0.000679032015566637));
#26368=CARTESIAN_POINT('',(0.00615644717722091,0.000283801554002562,-0.00174468605090144));
#26369=CARTESIAN_POINT('',(0.00513602995146302,0.000670556663751307,-0.00390529788969009));
#26370=CARTESIAN_POINT('',(0.00416498765751519,0.000887270563118401,-0.00492801412083271));
#26371=CARTESIAN_POINT('',(0.00180510893694002,0.00132069836185259,-0.00619485749997072));
#26372=CARTESIAN_POINT('',(0.000416272510312665,0.00153741226121969,-0.00643898464796613));
#26373=CARTESIAN_POINT('',(-0.00223418317285251,0.0019708400599539,-0.00605323402059007));
#26374=CARTESIAN_POINT('',(-0.00349580242939034,0.002187553959321,-0.00542335624521861));
#26375=CARTESIAN_POINT('',(-0.00539682237301682,0.00262098175805521,-0.00353664099605401));
#26376=CARTESIAN_POINT('',(-0.00603622306010547,0.00283769565742231,-0.00227980352226088));
#26377=CARTESIAN_POINT('',(-0.00644191908308324,0.00327112345615653,0.000367659413053137));
#26378=CARTESIAN_POINT('',(-0.00620821441897237,0.00348783735552363,0.00175828487457401));
#26379=CARTESIAN_POINT('',(-0.00495939979242914,0.00392126515425784,0.00412769161750468));
#26380=CARTESIAN_POINT('',(-0.00394428982999677,0.00413797905362495,0.00510647289891447));
#26381=CARTESIAN_POINT('',(-0.00153096266874101,0.00457140685235916,0.00626814518324837));
#26382=CARTESIAN_POINT('',(-0.000132745469917627,0.00478812075172626,0.00645103618617248));
#26383=CARTESIAN_POINT('',(0.00249817803237959,0.00522154855046046,0.00594916765217005));
#26384=CARTESIAN_POINT('',(0.00373088433585343,0.00543826244982756,0.0052644081152435));
#26385=CARTESIAN_POINT('',(0.00554710915024626,0.00587169024856175,0.00329591683839534));
#26386=CARTESIAN_POINT('',(0.00613062766116525,0.00608840414792885,0.00201218509847372));
#26387=CARTESIAN_POINT('',(0.00641952294283942,0.00652183194666303,-0.000650551426445441));
#26388=CARTESIAN_POINT('',(0.0061248997135946,0.00673854584603012,-0.00202955621144299));
#26389=CARTESIAN_POINT('',(0.00477310879536758,0.00717197364476428,-0.00434176523536755));
#26390=CARTESIAN_POINT('',(0.00371594110638537,0.00738868754413136,-0.00527496947429457));
#26391=CARTESIAN_POINT('',(0.00125387664352505,0.00782211534286551,-0.00632939341096007));
#26392=CARTESIAN_POINT('',(-0.000151020130353072,0.00803882924223258,-0.00645061310869855));
#26393=CARTESIAN_POINT('',(-0.00275735893103092,0.0084722570409667,-0.0058335904745747));
#26394=CARTESIAN_POINT('',(-0.00395880095783065,0.00868897094033375,-0.00509534814271236));
#26395=CARTESIAN_POINT('',(-0.00568661500571035,0.00912239873906786,-0.00304874648654315));
#26396=CARTESIAN_POINT('',(-0.00621298702679033,0.00933911263843491,-0.00174038716223628));
#26397=CARTESIAN_POINT('',(-0.00635845146221534,0.00970586556651554,0.000520815977194954));
#26398=CARTESIAN_POINT('',(-0.00620685575748996,0.00985590459522913,0.00145919397170054));
#26399=CARTESIAN_POINT('',(-0.00586675659330751,0.0100059436239427,0.00232282717309746));
#26400=CARTESIAN_POINT('',(0.00629974114353878,-5.25309875491508E-5,0.000371045857036716));
#26401=CARTESIAN_POINT('',(0.0063593151230501,0.000117510222832498,-0.000679035950839401));
#26402=CARTESIAN_POINT('',(0.00615648285639118,0.000287551433214149,-0.00174469616208227));
#26403=CARTESIAN_POINT('',(0.00513605971689134,0.000674306542962894,-0.00390532052251457));
#26404=CARTESIAN_POINT('',(0.00416501179534981,0.000891020442329988,-0.00492804268072283));
#26405=CARTESIAN_POINT('',(0.00180511939829658,0.00132444824106418,-0.00619489340174477));
#26406=CARTESIAN_POINT('',(0.000416274922784883,0.00154116214043128,-0.00643902196455848));
#26407=CARTESIAN_POINT('',(-0.00223419612087262,0.00197458993916549,-0.0060532691015972));
#26408=CARTESIAN_POINT('',(-0.00349582268901842,0.00219130383853259,-0.00542338767582222));
#26409=CARTESIAN_POINT('',(-0.00539685364984562,0.0026247316372668,-0.00353666149235856));
#26410=CARTESIAN_POINT('',(-0.00603625804252701,0.0028414455366339,-0.00227981673466987));
#26411=CARTESIAN_POINT('',(-0.00644195641668186,0.00327487333536811,0.000367661543792251));
#26412=CARTESIAN_POINT('',(-0.00620825039815532,0.00349158723473522,0.00175829506456568));
#26413=CARTESIAN_POINT('',(-0.00495942853421227,0.00392501503346943,0.00412771553919324));
#26414=CARTESIAN_POINT('',(-0.00394431268879574,0.00414172893283653,0.00510650249304738));
#26415=CARTESIAN_POINT('',(-0.00153097154130601,0.00457515673157075,0.00626818150975501));
#26416=CARTESIAN_POINT('',(-0.0001327462392328,0.00479187063093785,0.0064510735726085));
#26417=CARTESIAN_POINT('',(0.00249819251035964,0.00522529842967205,0.00594920213006932));
#26418=CARTESIAN_POINT('',(0.00373090595787887,0.00544201232903915,0.00526443862467663));
#26419=CARTESIAN_POINT('',(0.0055471412980494,0.00587544012777333,0.00329593593960333));
#26420=CARTESIAN_POINT('',(0.00613066319070069,0.00609215402714043,0.00201219675992271));
#26421=CARTESIAN_POINT('',(0.00641956014664309,0.00652558182587462,-0.000650555196661354));
#26422=CARTESIAN_POINT('',(0.00612493520993421,0.0067422957252417,-0.0020295679735648));
#26423=CARTESIAN_POINT('',(0.00477313645751695,0.00717572352397587,-0.00434179039770171));
#26424=CARTESIAN_POINT('',(0.00371596264180859,0.00739243742334294,-0.00527500004493517));
#26425=CARTESIAN_POINT('',(0.00125388391026136,0.0078258652220771,-0.00632943009242565));
#26426=CARTESIAN_POINT('',(-0.000151021005577498,0.00804257912144416,-0.00645065049268266));
#26427=CARTESIAN_POINT('',(-0.002757374911072,0.00847600692017828,-0.00583362428265618));
#26428=CARTESIAN_POINT('',(-0.00395882390072764,0.00869272081954534,-0.00509537767237269));
#26429=CARTESIAN_POINT('',(-0.0056866479620079,0.00912614861827944,-0.00304876415529623));
#26430=CARTESIAN_POINT('',(-0.00621302303363253,0.00934286251764649,-0.00174039724850326));
#26431=CARTESIAN_POINT('',(-0.0063584883120844,0.00970961544572712,0.000520818995540014));
#26432=CARTESIAN_POINT('',(-0.0062068917287989,0.00985965447444072,0.0014592024283361));
#26433=CARTESIAN_POINT('',(-0.00586679059360044,0.0100096935031543,0.0023228406348464));
#26434=CARTESIAN_POINT('',(0.00629981395301298,-4.87817538653648E-5,0.000371050145411927));
#26435=CARTESIAN_POINT('',(0.0063593886210526,0.000121259456516284,-0.000679043798820677));
#26436=CARTESIAN_POINT('',(0.00615655401015281,0.000291300666897935,-0.00174471632646797));
#26437=CARTESIAN_POINT('',(0.00513611907707756,0.00067805577664668,-0.00390536565839037));
#26438=CARTESIAN_POINT('',(0.00416505993261639,0.000894769676013774,-0.00492809963674502));
#26439=CARTESIAN_POINT('',(0.0018051402610259,0.00132819747474797,-0.0061949649994376));
#26440=CARTESIAN_POINT('',(0.000416279733896571,0.00154491137411507,-0.00643909638377553));
#26441=CARTESIAN_POINT('',(-0.00223422194267086,0.00197833917284927,-0.00605333906246232));
#26442=CARTESIAN_POINT('',(-0.00349586309210897,0.00219505307221637,-0.00542345035681118));
#26443=CARTESIAN_POINT('',(-0.00539691602416666,0.00262848087095058,-0.00353670236744498));
#26444=CARTESIAN_POINT('',(-0.00603632780678623,0.00284519477031769,-0.00227984308372992));
#26445=CARTESIAN_POINT('',(-0.00644203086981395,0.0032786225690519,0.000367665793053145));
#26446=CARTESIAN_POINT('',(-0.00620832215022209,0.00349533646841901,0.00175831538612116));
#26447=CARTESIAN_POINT('',(-0.00495948585297754,0.00392876426715322,0.00412776324540707));
#26448=CARTESIAN_POINT('',(-0.00394435827532484,0.00414547816652032,0.00510656151162497));
#26449=CARTESIAN_POINT('',(-0.00153098923556207,0.00457890596525453,0.00626825395447765));
#26450=CARTESIAN_POINT('',(-0.00013274777345201,0.00479561986462163,0.00645114813111243));
#26451=CARTESIAN_POINT('',(0.00249822138330521,0.00522904766335583,0.00594927088817685));
#26452=CARTESIAN_POINT('',(0.00373094907795236,0.00544576156272293,0.00526449946860648));
#26453=CARTESIAN_POINT('',(0.00554720540932508,0.00587918936145712,0.00329597403249593));
#26454=CARTESIAN_POINT('',(0.00613073404605065,0.00609590326082422,0.00201222001595574));
#26455=CARTESIAN_POINT('',(0.00641963434092953,0.0065293310595584,-0.000650562715475337));
#26456=CARTESIAN_POINT('',(0.00612500599908283,0.00674604495892549,-0.00202959143036622));
#26457=CARTESIAN_POINT('',(0.00477319162320516,0.00717947275765965,-0.00434184057809305));
#26458=CARTESIAN_POINT('',(0.00371600558917419,0.00739618665702673,-0.00527506101092899));
#26459=CARTESIAN_POINT('',(0.00125389840206763,0.00782961445576088,-0.00632950324503089));
#26460=CARTESIAN_POINT('',(-0.000151022751007946,0.00804632835512795,-0.00645072504629683));
#26461=CARTESIAN_POINT('',(-0.00275740677952704,0.00847975615386207,-0.00583369170496878));
#26462=CARTESIAN_POINT('',(-0.00395886965497057,0.00869647005322912,-0.00509543656237478));
#26463=CARTESIAN_POINT('',(-0.00568671368563664,0.00912989785196323,-0.00304879939149245));
#26464=CARTESIAN_POINT('',(-0.00621309484085919,0.00934661175133028,-0.00174041736320412));
#26465=CARTESIAN_POINT('',(-0.00635856180053102,0.00971336467941091,0.000520825014923407));
#26466=CARTESIAN_POINT('',(-0.0062069634651628,0.00986340370812451,0.00145921929311818));
#26467=CARTESIAN_POINT('',(-0.00586685839923381,0.0100134427368381,0.00232286748115665));
#26468=CARTESIAN_POINT('',(-0.00697636803347297,0.0100021874430334,0.00276214562330082));
#26469=CARTESIAN_POINT('',(-0.00753804382756523,0.00979380836024526,0.00133584489681522));
#26470=CARTESIAN_POINT('',(-0.00776779845912848,0.00937705019466896,-0.00186177246719335));
#26471=CARTESIAN_POINT('',(-0.00528323152104243,0.00875191294630448,-0.00599199413777197));
#26472=CARTESIAN_POINT('',(-0.00087751154538944,0.00812677569793997,-0.0079400821121839));
#26473=CARTESIAN_POINT('',(0.0038480746341964,0.00750163844957543,-0.00700128379985256));
#26474=CARTESIAN_POINT('',(0.0071744693740918,0.00687650120121086,-0.00351543059877151));
#26475=CARTESIAN_POINT('',(0.0078914902835435,0.00625136395284629,0.00124942414839732));
#26476=CARTESIAN_POINT('',(0.00573800816630541,0.00562622670448166,0.005560182342935));
#26477=CARTESIAN_POINT('',(0.0014971987061511,0.00500108945611705,0.00784857616645092));
#26478=CARTESIAN_POINT('',(-0.00328822052470963,0.00437595220775241,0.00728203066161055));
#26479=CARTESIAN_POINT('',(-0.00687737560563289,0.00375081495938778,0.00406674111468162));
#26480=CARTESIAN_POINT('',(-0.00796476957421187,0.00312567771102313,-0.000627461007861309));
#26481=CARTESIAN_POINT('',(-0.00615519713512889,0.00250054046265849,-0.00509305407738273));
#26482=CARTESIAN_POINT('',(-0.00210705476033651,0.00187540321429386,-0.00770553365716223));
#26483=CARTESIAN_POINT('',(0.00270641916035431,0.00125026596592923,-0.00751610423345641));
#26484=CARTESIAN_POINT('',(0.00653694894897428,0.000625128717564618,-0.00459055394770496));
#26485=CARTESIAN_POINT('',(0.0075004521700649,0.000208370551988218,-0.00153290696293537));
#26486=CARTESIAN_POINT('',(0.00750327649637306,-8.53079997731299E-9,5.83687127765024E-10));
#26487=CARTESIAN_POINT('',(0.00630986196639554,-9.03189203241712E-9,3.59078576052906E-9));
#26488=CARTESIAN_POINT('',(0.00630748748308214,0.000208370074868084,-0.00128909129339307));
#26489=CARTESIAN_POINT('',(0.00549723302828212,0.000625128288388326,-0.0038604125171732));
#26490=CARTESIAN_POINT('',(0.00227595940277768,0.0012502656086687,-0.00632064842559635));
#26491=CARTESIAN_POINT('',(-0.00177191976628907,0.00187540292894909,-0.00647995041664462));
#26492=CARTESIAN_POINT('',(-0.00517619621271276,0.00250054024922949,-0.00428299345973494));
#26493=CARTESIAN_POINT('',(-0.00669795326198427,0.0031256775695099,-0.000527664383287013));
#26494=CARTESIAN_POINT('',(-0.0057835134182492,0.0037508148897903,0.00341991386813026));
#26495=CARTESIAN_POINT('',(-0.00276522310213338,0.0043759522100707,0.00612380489522609));
#26496=CARTESIAN_POINT('',(0.00125906345149119,0.0050010895303511,0.00660024130588146));
#26497=CARTESIAN_POINT('',(0.00482536249576932,0.00562622685063147,0.00467582317649158));
#26498=CARTESIAN_POINT('',(0.00663632912242476,0.00625136417091186,0.00105070204310645));
#26499=CARTESIAN_POINT('',(0.00603335321048816,0.00687650149119221,-0.00295629117688575));
#26500=CARTESIAN_POINT('',(0.0032360303450091,0.00750163881147252,-0.00588771168090631));
#26501=CARTESIAN_POINT('',(-0.000737939723699143,0.00812677613175284,-0.00667719275794199));
#26502=CARTESIAN_POINT('',(-0.00444291960613415,0.00875191345203308,-0.00503895366700153));
#26503=CARTESIAN_POINT('',(-0.00653231080331541,0.00937705077231335,-0.00156565414967004));
#26504=CARTESIAN_POINT('',(-0.00633909965413823,0.00979380898583348,0.00112337445858087));
#26505=CARTESIAN_POINT('',(-0.00586675994202744,0.0100021880925935,0.00232281866952534));
#26506=CARTESIAN_POINT('',(0.00629981376813919,-7.12754161583918E-5,0.000371050098800527));
#26507=CARTESIAN_POINT('',(0.00635938760157998,9.87634366672949E-5,-0.000679029292887613));
#26508=CARTESIAN_POINT('',(0.0061565597919047,0.000268802289492985,-0.00174468683320115));
#26509=CARTESIAN_POINT('',(0.00513614563794227,0.000655555202048129,-0.00390533092155032));
#26510=CARTESIAN_POINT('',(0.00416509255857977,0.000872269261777583,-0.00492807221758922));
#26511=CARTESIAN_POINT('',(0.00180517935721193,0.0013056973812365,-0.00619495373145521));
#26512=CARTESIAN_POINT('',(0.00041631923520657,0.00152241144096596,-0.00643909394928229));
#26513=CARTESIAN_POINT('',(-0.00223418666799694,0.00195583956042489,-0.00605335220863278));
#26514=CARTESIAN_POINT('',(-0.0034958324491951,0.00217255362015435,-0.00542347025015618));
#26515=CARTESIAN_POINT('',(-0.00539689715743606,0.00260598173961328,-0.00353673137452573));
#26516=CARTESIAN_POINT('',(-0.00603631608447885,0.00282269579934275,-0.00227987445737188));
#26517=CARTESIAN_POINT('',(-0.00644203278688762,0.00325612391880168,0.000367634290427892));
#26518=CARTESIAN_POINT('',(-0.0062083305622536,0.00347283797853115,0.00175828612107382));
#26519=CARTESIAN_POINT('',(-0.00495950418817836,0.00390626609799008,0.00412774140168303));
#26520=CARTESIAN_POINT('',(-0.00394438003873714,0.00412298015771955,0.00510654485164633));
#26521=CARTESIAN_POINT('',(-0.00153101401290164,0.00455640827717848,0.00626824802518821));
#26522=CARTESIAN_POINT('',(-0.000132772136507351,0.00477312233690794,0.00645114774876679));
#26523=CARTESIAN_POINT('',(0.00249820074447072,0.00520655045636687,0.00594927968387582));
#26524=CARTESIAN_POINT('',(0.0037309317490545,0.00542326451609633,0.00526451189540625));
#26525=CARTESIAN_POINT('',(0.0055471956057837,0.00585669263555524,0.00329599076501096));
#26526=CARTESIAN_POINT('',(0.00613072845792912,0.0060734066952847,0.00201223742308522));
#26527=CARTESIAN_POINT('',(0.00641963610782257,0.0065068348147436,-0.000650546460226448));
#26528=CARTESIAN_POINT('',(0.00612501090557062,0.00672354887447305,-0.00202957700161239));
#26529=CARTESIAN_POINT('',(0.0047732006664181,0.00715697699393194,-0.00434183081328834));
#26530=CARTESIAN_POINT('',(0.00371601562951754,0.00737369105366138,-0.00527505408357836));
#26531=CARTESIAN_POINT('',(0.00125390849600593,0.00780711917312025,-0.00632950136668111));
#26532=CARTESIAN_POINT('',(-0.000151013600605117,0.00802383323284968,-0.00645072537949384));
#26533=CARTESIAN_POINT('',(-0.00275740029882653,0.00845726135230853,-0.00583369489991698));
#26534=CARTESIAN_POINT('',(-0.00395886490043688,0.00867397541203794,-0.00509544040752736));
#26535=CARTESIAN_POINT('',(-0.00568671181406075,0.00910740353149676,-0.00304880313354801));
#26536=CARTESIAN_POINT('',(-0.00621309412607427,0.00932411759122617,-0.00174042035195825));
#26537=CARTESIAN_POINT('',(-0.0063664962444253,0.00971087477110569,0.000644159634078352));
#26538=CARTESIAN_POINT('',(-0.00616278732211593,0.00988091789125582,0.0017096785410187));
#26539=CARTESIAN_POINT('',(-0.0057208257156327,0.0100509610114059,0.00266411091696313));
#26540=CARTESIAN_POINT('',(0.00629974101447218,-6.75276211545794E-5,0.000371045813712693));
#26541=CARTESIAN_POINT('',(0.00635931415992202,0.000102511231671107,-0.000679021451088969));
#26542=CARTESIAN_POINT('',(0.00615648869261233,0.000272550084496797,-0.00174466668461112));
#26543=CARTESIAN_POINT('',(0.00513608632294611,0.000659302997051941,-0.00390528582067021));
#26544=CARTESIAN_POINT('',(0.00416504445783136,0.000876017056781396,-0.0049280153055378));
#26545=CARTESIAN_POINT('',(0.00180515851002141,0.00130944517624031,-0.00619488218876878));
#26546=CARTESIAN_POINT('',(0.00041631442732619,0.00152615923596978,-0.00643901958713219));
#26547=CARTESIAN_POINT('',(-0.00223416086639727,0.0019595873554287,-0.00605328230123756));
#26548=CARTESIAN_POINT('',(-0.00349579207742551,0.00217630141515817,-0.00542340761697953));
#26549=CARTESIAN_POINT('',(-0.0053968348311399,0.0026097295346171,-0.00353669053043316));
#26550=CARTESIAN_POINT('',(-0.00603624637382603,0.00282644359434656,-0.00227984812814483));
#26551=CARTESIAN_POINT('',(-0.00644195839079822,0.0032598717138055,0.000367630044787666));
#26552=CARTESIAN_POINT('',(-0.00620825886508428,0.00347658577353496,0.00175826581543183));
#26553=CARTESIAN_POINT('',(-0.00495944691313349,0.0039100138929939,0.00412769373228605));
#26554=CARTESIAN_POINT('',(-0.00394433448689665,0.00412672795272337,0.0051064858784961));
#26555=CARTESIAN_POINT('',(-0.00153099633192125,0.0045601560721823,0.00626817563605952));
#26556=CARTESIAN_POINT('',(-0.00013277060318269,0.00477687013191176,0.00645107324741287));
#26557=CARTESIAN_POINT('',(0.00249817189389326,0.00521029825137068,0.00594921097836658));
#26558=CARTESIAN_POINT('',(0.00373088866223065,0.00542701231110014,0.00526445109796691));
#26559=CARTESIAN_POINT('',(0.00554713154375952,0.00586044043055906,0.00329595270112154));
#26560=CARTESIAN_POINT('',(0.00613065765695099,0.00607715449028852,0.00201221418467583));
#26561=CARTESIAN_POINT('',(0.00641956197038218,0.00651058260974742,-0.000650538947363007));
#26562=CARTESIAN_POINT('',(0.00612494017062189,0.00672729666947687,-0.00202955356295614));
#26563=CARTESIAN_POINT('',(0.00477314554290736,0.00716072478893575,-0.00434178067147069));
#26564=CARTESIAN_POINT('',(0.00371597271495313,0.0073774388486652,-0.00527499316439211));
#26565=CARTESIAN_POINT('',(0.00125389401519038,0.00781086696812407,-0.0063294282701656));
#26566=CARTESIAN_POINT('',(-0.000151011856618133,0.0080275810278535,-0.00645065088301767));
#26567=CARTESIAN_POINT('',(-0.002757368454872,0.00846100914731235,-0.00583362752924352));
#26568=CARTESIAN_POINT('',(-0.00395881918131735,0.00867772320704176,-0.00509538156261729));
#26569=CARTESIAN_POINT('',(-0.00568664614082771,0.00911115132650058,-0.00304876792431546));
#26570=CARTESIAN_POINT('',(-0.00621302237389273,0.00932786538622998,-0.00174040025263986));
#26571=CARTESIAN_POINT('',(-0.00636642272067288,0.00971462256610951,0.000644152194973444));
#26572=CARTESIAN_POINT('',(-0.00616271615090465,0.00988466568625963,0.00170965879672342));
#26573=CARTESIAN_POINT('',(-0.00572075964843382,0.0100547088064097,0.00266408015036499));
#26574=CARTESIAN_POINT('',(0.00629970453308949,-6.37791813663305E-5,0.000371043665010978));
#26575=CARTESIAN_POINT('',(0.00635927733355519,0.000106259671459356,-0.000679017518920748));
#26576=CARTESIAN_POINT('',(0.00615645304079433,0.000276298524285046,-0.00174465658136197));
#26577=CARTESIAN_POINT('',(0.00513605658021061,0.00066305143684019,-0.00390526320541885));
#26578=CARTESIAN_POINT('',(0.00416502033833495,0.000879765496569645,-0.00492798676772777));
#26579=CARTESIAN_POINT('',(0.00180514805646811,0.00131319361602856,-0.0061948463146166));
#26580=CARTESIAN_POINT('',(0.000416312016476933,0.00152990767575802,-0.00643898229919651));
#26581=CARTESIAN_POINT('',(-0.00223414792851976,0.00196333579521695,-0.00605324724708094));
#26582=CARTESIAN_POINT('',(-0.00349577183352528,0.00218004985494641,-0.00542337621038546));
#26583=CARTESIAN_POINT('',(-0.00539680357842707,0.00261347797440534,-0.0035366700496927));
#26584=CARTESIAN_POINT('',(-0.00603621141832334,0.00283019203413481,-0.00227983492569542));
#26585=CARTESIAN_POINT('',(-0.00644192108584413,0.00326362015359374,0.000367627915866442));
#26586=CARTESIAN_POINT('',(-0.00620822291346865,0.00348033421332321,0.00175825563343103));
#26587=CARTESIAN_POINT('',(-0.00495941819330511,0.00391376233278214,0.00412766982908521));
#26588=CARTESIAN_POINT('',(-0.00394431164551705,0.00413047639251162,0.00510645630717482));
#26589=CARTESIAN_POINT('',(-0.00153098746602296,0.00456390451197054,0.00626813933746984));
#26590=CARTESIAN_POINT('',(-0.000132769834316927,0.0047806185717,0.00645103588967525));
#26591=CARTESIAN_POINT('',(0.00249815742714539,0.00521404669115893,0.00594917652688009));
#26592=CARTESIAN_POINT('',(0.00373086705690167,0.00543076075088839,0.00526442061187951));
#26593=CARTESIAN_POINT('',(0.00554709942068839,0.0058641888703473,0.00329593361447789));
#26594=CARTESIAN_POINT('',(0.00613062215471882,0.00608090293007676,0.00201220253207685));
#26595=CARTESIAN_POINT('',(0.00641952479512427,0.00651433104953567,-0.000650535180135078));
#26596=CARTESIAN_POINT('',(0.0061249047014993,0.00673104510926511,-0.00202954180994597));
#26597=CARTESIAN_POINT('',(0.00477311790193787,0.007164473228724,-0.00434175552850657));
#26598=CARTESIAN_POINT('',(0.00371595119600142,0.00738118728845344,-0.0052749626172563));
#26599=CARTESIAN_POINT('',(0.00125388675397324,0.00781461540791232,-0.00632939161686598));
#26600=CARTESIAN_POINT('',(-0.00015101098211848,0.00803132946764175,-0.00645061352772593));
#26601=CARTESIAN_POINT('',(-0.00275735248713402,0.0084647575871006,-0.00583359374709313));
#26602=CARTESIAN_POINT('',(-0.00395879625605784,0.00868147164683,-0.00509535205560036));
#26603=CARTESIAN_POINT('',(-0.0056866132098368,0.00911489976628883,-0.00304875026910247));
#26604=CARTESIAN_POINT('',(-0.00621298639469194,0.00933161382601823,-0.00174039017409734));
#26605=CARTESIAN_POINT('',(-0.00636638585314085,0.00971837100589775,0.000644148464730775));
#26606=CARTESIAN_POINT('',(-0.00616268046302387,0.00988841412604788,0.00170964889620264));
#26607=CARTESIAN_POINT('',(-0.00572072651989384,0.010058457246198,0.00266406472285341));
#26608=CARTESIAN_POINT('',(0.00629970453308949,6.4870253252478E-5,0.00037104366501098));
#26609=CARTESIAN_POINT('',(0.0063592773335552,0.000234909106078165,-0.000679017518920747));
#26610=CARTESIAN_POINT('',(0.00615645304079433,0.000404947958903854,-0.00174465658136197));
#26611=CARTESIAN_POINT('',(0.00513605658021061,0.000791700871458999,-0.00390526320541886));
#26612=CARTESIAN_POINT('',(0.00416502033833495,0.00100841493118845,-0.00492798676772778));
#26613=CARTESIAN_POINT('',(0.00180514805646811,0.00144184305064737,-0.00619484631461661));
#26614=CARTESIAN_POINT('',(0.000416312016476927,0.00165855711037684,-0.00643898229919652));
#26615=CARTESIAN_POINT('',(-0.00223414792851977,0.00209198522983576,-0.00605324724708094));
#26616=CARTESIAN_POINT('',(-0.00349577183352529,0.00230869928956523,-0.00542337621038546));
#26617=CARTESIAN_POINT('',(-0.00539680357842707,0.00274212740902415,-0.0035366700496927));
#26618=CARTESIAN_POINT('',(-0.00603621141832334,0.00295884146875362,-0.00227983492569542));
#26619=CARTESIAN_POINT('',(-0.00644192108584413,0.00339226958821256,0.000367627915866445));
#26620=CARTESIAN_POINT('',(-0.00620822291346865,0.00360898364794202,0.00175825563343103));
#26621=CARTESIAN_POINT('',(-0.00495941819330511,0.00404241176740095,0.00412766982908522));
#26622=CARTESIAN_POINT('',(-0.00394431164551705,0.00425912582713043,0.00510645630717482));
#26623=CARTESIAN_POINT('',(-0.00153098746602296,0.00469255394658935,0.00626813933746984));
#26624=CARTESIAN_POINT('',(-0.000132769834316927,0.0049092680063188,0.00645103588967525));
#26625=CARTESIAN_POINT('',(0.00249815742714539,0.00534269612577773,0.0059491765268801));
#26626=CARTESIAN_POINT('',(0.00373086705690168,0.0055594101855072,0.00526442061187951));
#26627=CARTESIAN_POINT('',(0.00554709942068839,0.00599283830496611,0.00329593361447789));
#26628=CARTESIAN_POINT('',(0.00613062215471881,0.00620955236469557,0.00201220253207685));
#26629=CARTESIAN_POINT('',(0.00641952479512428,0.00664298048415448,-0.000650535180135079));
#26630=CARTESIAN_POINT('',(0.00612490470149931,0.00685969454388393,-0.00202954180994598));
#26631=CARTESIAN_POINT('',(0.00477311790193787,0.00729312266334281,-0.00434175552850658));
#26632=CARTESIAN_POINT('',(0.0037159511960014,0.00750983672307226,-0.0052749626172563));
#26633=CARTESIAN_POINT('',(0.00125388675397322,0.00794326484253113,-0.00632939161686598));
#26634=CARTESIAN_POINT('',(-0.000151010982118486,0.00815997890226056,-0.00645061352772594));
#26635=CARTESIAN_POINT('',(-0.00275735248713402,0.0085934070217194,-0.00583359374709313));
#26636=CARTESIAN_POINT('',(-0.00395879625605785,0.00881012108144881,-0.00509535205560036));
#26637=CARTESIAN_POINT('',(-0.0056866132098368,0.00924354920090765,-0.00304875026910247));
#26638=CARTESIAN_POINT('',(-0.00621298639469194,0.00946026326063705,-0.00174039017409734));
#26639=CARTESIAN_POINT('',(-0.00636638585314084,0.00984702044051656,0.000644148464730776));
#26640=CARTESIAN_POINT('',(-0.00616268046302386,0.0100170635606667,0.00170964889620264));
#26641=CARTESIAN_POINT('',(-0.00572072651989384,0.0101871066808168,0.00266406472285341));
#26642=CARTESIAN_POINT('',(0.00634020891479936,0.000189771248083037,0.00037342931566486));
#26643=CARTESIAN_POINT('',(0.0064001647426653,0.000359810100908722,-0.000683383308558913));
#26644=CARTESIAN_POINT('',(0.00619603637722438,0.000529848953734411,-0.00175587397032886));
#26645=CARTESIAN_POINT('',(0.00516907920771887,0.000916601866289553,-0.00393037236263709));
#26646=CARTESIAN_POINT('',(0.00419179962182787,0.00113331592601901,-0.0049596715961277));
#26647=CARTESIAN_POINT('',(0.00181675437951675,0.00156674404547792,-0.00623467650322993));
#26648=CARTESIAN_POINT('',(0.000418988723096619,0.00178345810520739,-0.00648038217684154));
#26649=CARTESIAN_POINT('',(-0.00224851253562439,0.00221688622466631,-0.00609216701479261));
#26650=CARTESIAN_POINT('',(-0.00351824813792527,0.00243360028439577,-0.00545824617913206));
#26651=CARTESIAN_POINT('',(-0.00543150269661675,0.0028670284038547,-0.00355940931197431));
#26652=CARTESIAN_POINT('',(-0.00607502165300737,0.00308374246358417,-0.00229449328047711));
#26653=CARTESIAN_POINT('',(-0.00648333985861916,0.0035171705830431,0.000369991604727282));
#26654=CARTESIAN_POINT('',(-0.00624813910784035,0.00373388464277257,0.00176956045843447));
#26655=CARTESIAN_POINT('',(-0.00499130511220827,0.0041673127622315,0.00415420896492109));
#26656=CARTESIAN_POINT('',(-0.003969671867355,0.00438402682196097,0.00513928861770052));
#26657=CARTESIAN_POINT('',(-0.00154083105478036,0.0048174549414199,0.00630844076859283));
#26658=CARTESIAN_POINT('',(-0.00013362348705897,0.00503416900114937,0.00649251326670571));
#26659=CARTESIAN_POINT('',(0.00251421950140125,0.00546759712060829,0.00598742716476928));
#26660=CARTESIAN_POINT('',(0.00375485492214007,0.00568431118033775,0.00529826856471998));
#26661=CARTESIAN_POINT('',(0.0055827648762884,0.00611773929979667,0.00331712504536326));
#26662=CARTESIAN_POINT('',(0.0061700394096979,0.00633445335952612,0.00202514012605585));
#26663=CARTESIAN_POINT('',(0.00646079956941439,0.00676788147898503,-0.000654717840625502));
#26664=CARTESIAN_POINT('',(0.00616428519572137,0.00698459553871448,-0.00204259088799945));
#26665=CARTESIAN_POINT('',(0.00480380699035953,0.00741802365817337,-0.00436967114300784));
#26666=CARTESIAN_POINT('',(0.00373984315869069,0.00763473771790281,-0.00530887835064227));
#26667=CARTESIAN_POINT('',(0.00126194870472618,0.00806816583736168,-0.00637008687371401));
#26668=CARTESIAN_POINT('',(-0.000151981917569498,0.00828487989709111,-0.00649208818915132));
#26669=CARTESIAN_POINT('',(-0.00277508107377819,0.00871830801654996,-0.00587110123758437));
#26670=CARTESIAN_POINT('',(-0.00398424960769119,0.00893502207627938,-0.00512811297058012));
#26671=CARTESIAN_POINT('',(-0.00572317567889829,0.0093684501957382,-0.00306835241774121));
#26672=CARTESIAN_POINT('',(-0.00625293321619238,0.00958516425546761,-0.00175158013190655));
#26673=CARTESIAN_POINT('',(-0.00640731896696443,0.00997192143534712,0.000648290061397133));
#26674=CARTESIAN_POINT('',(-0.00620230383909161,0.0101419645554972,0.0017206412008604));
#26675=CARTESIAN_POINT('',(-0.00575750832281848,0.0103120076756474,0.00268119350942863));
#26676=CARTESIAN_POINT('',(0.00648675514451895,0.000391865302947556,0.00038206068081589));
#26677=CARTESIAN_POINT('',(0.00654809677853758,0.00056190415577324,-0.000699178883857519));
#26678=CARTESIAN_POINT('',(0.00633925023381643,0.000731943008598929,-0.00179645886487608));
#26679=CARTESIAN_POINT('',(0.00528855619644159,0.00111869592115407,-0.00402121814688153));
#26680=CARTESIAN_POINT('',(0.00428868797969965,0.00133540998088352,-0.00507430838220636));
#26681=CARTESIAN_POINT('',(0.00185874645079114,0.00176883810034244,-0.00637878347941126));
#26682=CARTESIAN_POINT('',(0.000428673138624558,0.0019855521600719,-0.00663016834129133));
#26683=CARTESIAN_POINT('',(-0.00230048417236396,0.00241898027953082,-0.00623298005720765));
#26684=CARTESIAN_POINT('',(-0.00359956817118591,0.00263569433926028,-0.00558440691124391));
#26685=CARTESIAN_POINT('',(-0.00555704528560669,0.00306912245871922,-0.0036416807357883));
#26686=CARTESIAN_POINT('',(-0.00621543840120553,0.00328583651844868,-0.00234752770629642));
#26687=CARTESIAN_POINT('',(-0.00663319438629153,0.00371926463790762,0.000378543511364632));
#26688=CARTESIAN_POINT('',(-0.0063925572557787,0.00393597869763708,0.00181046169953381));
#26689=CARTESIAN_POINT('',(-0.00510667306859641,0.00436940681709602,0.00425022846040734));
#26690=CARTESIAN_POINT('',(-0.00406142601192695,0.00458612087682549,0.00525807703311169));
#26691=CARTESIAN_POINT('',(-0.00157644549347588,0.00501954899628442,0.00645425271619107));
#26692=CARTESIAN_POINT('',(-0.000136712031694268,0.00523626305601388,0.0066425798265661));
#26693=CARTESIAN_POINT('',(0.00257233263198876,0.00566969117547281,0.00612581927274375));
#26694=CARTESIAN_POINT('',(0.00384164383389017,0.00588640523520227,0.00542073160854637));
#26695=CARTESIAN_POINT('',(0.00571180370687351,0.00631983335466118,0.00339379636257676));
#26696=CARTESIAN_POINT('',(0.00631265237795545,0.00653654741439063,0.00207194878080453));
#26697=CARTESIAN_POINT('',(0.00661013310567399,0.00696997553384954,-0.00066985084844325));
#26698=CARTESIAN_POINT('',(0.00630676516231059,0.00718668959357899,-0.00208980289591881));
#26699=CARTESIAN_POINT('',(0.00491484115535283,0.00762011771303788,-0.00447067078509022));
#26700=CARTESIAN_POINT('',(0.00382628509175847,0.00783683177276732,-0.00543158662678607));
#26701=CARTESIAN_POINT('',(0.00129111711656598,0.00827025989222619,-0.00651732369617108));
#26702=CARTESIAN_POINT('',(-0.000155494795032157,0.00848697395195563,-0.00664214492386024));
#26703=CARTESIAN_POINT('',(-0.00283922370282928,0.00892040207141447,-0.00600680461301443));
#26704=CARTESIAN_POINT('',(-0.00407634069902827,0.00913711613114389,-0.00524664307447946));
#26705=CARTESIAN_POINT('',(-0.00585545993467536,0.00957054425060272,-0.00313927365776871));
#26706=CARTESIAN_POINT('',(-0.00639746217412347,0.00978725831033213,-0.00179206577959293));
#26707=CARTESIAN_POINT('',(-0.00655541636404353,0.0101740154902116,0.000663274498903706));
#26708=CARTESIAN_POINT('',(-0.00634566256045371,0.0103440586103618,0.0017604117327269));
#26709=CARTESIAN_POINT('',(-0.00589058613596731,0.0105141017305119,0.00274316604144382));
#26710=CARTESIAN_POINT('',(0.00659279699252868,0.000469058362981516,0.000388306395313039));
#26711=CARTESIAN_POINT('',(0.00665514140529975,0.000639097215807201,-0.000710608669517962));
#26712=CARTESIAN_POINT('',(0.00644288075397842,0.00080913606863289,-0.00182582637045641));
#26713=CARTESIAN_POINT('',(0.00537501055765604,0.00119588898118803,-0.00408695477390774));
#26714=CARTESIAN_POINT('',(0.0043587970540785,0.00141260304091748,-0.00515726033988509));
#26715=CARTESIAN_POINT('',(0.00188913219901688,0.0018460311603764,-0.00648306026697927));
#26716=CARTESIAN_POINT('',(0.000435680847532806,0.00206274522010586,-0.0067385546280961));
#26717=CARTESIAN_POINT('',(-0.00233809120199892,0.00249617333956478,-0.00633487333191104));
#26718=CARTESIAN_POINT('',(-0.00365841190004657,0.00271288739929425,-0.00567569767460917));
#26719=CARTESIAN_POINT('',(-0.00564788875640694,0.00314631551875317,-0.00370121289732066));
#26720=CARTESIAN_POINT('',(-0.00631704491471967,0.00336302957848265,-0.00238590377733404));
#26721=CARTESIAN_POINT('',(-0.00674163014118887,0.00379645769794157,0.000384731729141146));
#26722=CARTESIAN_POINT('',(-0.00649705920934535,0.00401317175767105,0.00184005811562972));
#26723=CARTESIAN_POINT('',(-0.00519015410608139,0.00444659987712998,0.00431970882005773));
#26724=CARTESIAN_POINT('',(-0.00412781993466094,0.00466331393685945,0.00534403313799717));
#26725=CARTESIAN_POINT('',(-0.00160221634341401,0.00509674205631838,0.00655976323266633));
#26726=CARTESIAN_POINT('',(-0.000138946923587524,0.00531345611604784,0.00675116900939604));
#26727=CARTESIAN_POINT('',(0.00261438368832041,0.00574688423550677,0.00622596074282903));
#26728=CARTESIAN_POINT('',(0.00390444488040186,0.00596359829523623,0.0055093466995323));
#26729=CARTESIAN_POINT('',(0.00580517708185861,0.00639702641469514,0.00344927624890489));
#26730=CARTESIAN_POINT('',(0.00641584809123392,0.0066137404744246,0.00210581984157422));
#26731=CARTESIAN_POINT('',(0.00671819186764348,0.0070471685938835,-0.000680801195770578));
#26732=CARTESIAN_POINT('',(0.00640986463467774,0.00726388265361295,-0.00212396582578469));
#26733=CARTESIAN_POINT('',(0.00499518623192447,0.00769731077307184,-0.00454375481267135));
#26734=CARTESIAN_POINT('',(0.00388883506213696,0.00791402483280128,-0.0055203791695439));
#26735=CARTESIAN_POINT('',(0.00131222357765282,0.00834745295226015,-0.00662386526178012));
#26736=CARTESIAN_POINT('',(-0.000158036737043802,0.00856416701198959,-0.00675072699714379));
#26737=CARTESIAN_POINT('',(-0.00288563774523621,0.00899759513144844,-0.00610500049795324));
#26738=CARTESIAN_POINT('',(-0.00414297843873199,0.00921430919117785,-0.00533241226339903));
#26739=CARTESIAN_POINT('',(-0.00595118172139095,0.00964773731063668,-0.00319059274915747));
#26740=CARTESIAN_POINT('',(-0.00650204431055414,0.00986445137036608,-0.00182136146947011));
#26741=CARTESIAN_POINT('',(-0.00666258064729905,0.0102512085502456,0.000674117339743923));
#26742=CARTESIAN_POINT('',(-0.00644939790574807,0.0104212516703957,0.00178918995993563));
#26743=CARTESIAN_POINT('',(-0.00598688214619151,0.0105912947905458,0.00278800978688379));
#26744=CARTESIAN_POINT('',(0.00682991377313814,0.000546251423015476,0.000402272237496718));
#26745=CARTESIAN_POINT('',(0.00689450046736609,0.000716290275841162,-0.000736166447222965));
#26746=CARTESIAN_POINT('',(0.00667460564160431,0.000886329128666851,-0.00189149410926364));
#26747=CARTESIAN_POINT('',(0.00556832838628288,0.00127308204122199,-0.00423394634054989));
#26748=CARTESIAN_POINT('',(0.0045155657102292,0.00148979610095144,-0.00534274655612142));
#26749=CARTESIAN_POINT('',(0.00195707679759685,0.00192322422041036,-0.00671623025245665));
#26750=CARTESIAN_POINT('',(0.000451350561018182,0.00213993828013982,-0.00698091373322034));
#26751=CARTESIAN_POINT('',(-0.00242218307669453,0.00257336639959874,-0.00656271362059788));
#26752=CARTESIAN_POINT('',(-0.00378999047782856,0.00279008045932821,-0.00587983002721171));
#26753=CARTESIAN_POINT('',(-0.00585102093242832,0.00322350857878714,-0.00383433085735453));
#26754=CARTESIAN_POINT('',(-0.00654424398589403,0.0034402226385166,-0.00247171528088352));
#26755=CARTESIAN_POINT('',(-0.00698409986033083,0.00387365075797554,0.000398569004749002));
#26756=CARTESIAN_POINT('',(-0.00673073268130192,0.00409036481770501,0.00190623771391051));
#26757=CARTESIAN_POINT('',(-0.00537682338073001,0.00452379293716394,0.00447507162733712));
#26758=CARTESIAN_POINT('',(-0.00427628125918701,0.00474050699689341,0.00553623683160219));
#26759=CARTESIAN_POINT('',(-0.00165984171571361,0.00517393511635234,0.00679569191984611));
#26760=CARTESIAN_POINT('',(-0.000143944293783209,0.0053906491760818,0.00699398180382494));
#26761=CARTESIAN_POINT('',(0.00270841270880366,0.00582407729554073,0.00644988387730647));
#26762=CARTESIAN_POINT('',(0.00404487228946013,0.00604079135527019,0.00570749606680917));
#26763=CARTESIAN_POINT('',(0.00601396629561387,0.0064742194747291,0.00357333304611855));
#26764=CARTESIAN_POINT('',(0.00664660072111115,0.00669093353445856,0.00218155783592524));
#26765=CARTESIAN_POINT('',(0.00695981860497174,0.00712436165391747,-0.000705286916771713));
#26766=CARTESIAN_POINT('',(0.00664040206333504,0.00734107571364691,-0.00220035645927534));
#26767=CARTESIAN_POINT('',(0.00517484328479609,0.0077745038331058,-0.00470717566641223));
#26768=CARTESIAN_POINT('',(0.00402870104789384,0.00799121789283525,-0.00571892533104548));
#26769=CARTESIAN_POINT('',(0.00135941905940744,0.00842464601229412,-0.0068620994449112));
#26770=CARTESIAN_POINT('',(-0.000163720692176703,0.00864136007202355,-0.00699352389414366));
#26771=CARTESIAN_POINT('',(-0.00298942269916865,0.0090747881914824,-0.00632457317178717));
#26772=CARTESIAN_POINT('',(-0.00429198495457645,0.00929150225121182,-0.00552419800019821));
#26773=CARTESIAN_POINT('',(-0.00616522214341475,0.00972493037067064,-0.00330534572604625));
#26774=CARTESIAN_POINT('',(-0.00673589707684525,0.00994164443040004,-0.00188686862348324));
#26775=CARTESIAN_POINT('',(-0.00690220726941841,0.0103284016102796,0.000698362668931858));
#26776=CARTESIAN_POINT('',(-0.00668135718949568,0.0104984447304297,0.00185354003224629));
#26777=CARTESIAN_POINT('',(-0.00620220657101483,0.0106684878505798,0.00288828345005326));
#26778=CARTESIAN_POINT('',(0.00696098870573786,0.000546251423015476,0.000409992365183249));
#26779=CARTESIAN_POINT('',(0.00702681490267023,0.000716290275841162,-0.000750294439267526));
#26780=CARTESIAN_POINT('',(0.0068027000090682,0.00088632912866685,-0.00192779434249054));
#26781=CARTESIAN_POINT('',(0.00567519185369527,0.00127308204122199,-0.00431520128016583));
#26782=CARTESIAN_POINT('',(0.00460222529200104,0.00148979610095144,-0.00544528081467901));
#26783=CARTESIAN_POINT('',(0.00199463564795106,0.00192322422041036,-0.00684512345036601));
#26784=CARTESIAN_POINT('',(0.000460012565595309,0.00213993828013982,-0.00711488655153982));
#26785=CARTESIAN_POINT('',(-0.00246866792175518,0.00257336639959874,-0.00668866063458132));
#26786=CARTESIAN_POINT('',(-0.0038627253267499,0.00279008045932821,-0.00599267161644901));
#26787=CARTESIAN_POINT('',(-0.00596330963764944,0.00322350857878714,-0.00390791665585604));
#26788=CARTESIAN_POINT('',(-0.00666983654355425,0.0034402226385166,-0.00251915071339539));
#26789=CARTESIAN_POINT('',(-0.00711813382457544,0.00387365075797554,0.000406218062580345));
#26790=CARTESIAN_POINT('',(-0.00685990419969183,0.00409036481770501,0.00194282089609541));
#26791=CARTESIAN_POINT('',(-0.00548001161789365,0.00452379293716394,0.00456095407496612));
#26792=CARTESIAN_POINT('',(-0.00435834866097909,0.00474050699689341,0.00564248442032174));
#26793=CARTESIAN_POINT('',(-0.00169169623807508,0.00517393511635234,0.00692611009055063));
#26794=CARTESIAN_POINT('',(-0.000146706772085636,0.0053906491760818,0.00712820541542389));
#26795=CARTESIAN_POINT('',(0.00276039067295526,0.00582407729554073,0.00657366554169863));
#26796=CARTESIAN_POINT('',(0.0041224986520067,0.00604079135527019,0.00581703034310011));
#26797=CARTESIAN_POINT('',(0.00612938213438403,0.0064742194747291,0.00364190995700408));
#26798=CARTESIAN_POINT('',(0.00677415763770992,0.00669093353445856,0.00222342476950659));
#26799=CARTESIAN_POINT('',(0.0070933865803305,0.00712436165391747,-0.000718822290445522));
#26800=CARTESIAN_POINT('',(0.0067678400196252,0.00734107571364692,-0.00224258416290012));
#26801=CARTESIAN_POINT('',(0.00527415526109607,0.0077745038331058,-0.00479751249257198));
#26802=CARTESIAN_POINT('',(0.00410601706327225,0.00799121789283524,-0.00582867894978923));
#26803=CARTESIAN_POINT('',(0.00138550808007523,0.00842464601229412,-0.00699379206243323));
#26804=CARTESIAN_POINT('',(-0.000166862705297958,0.00864136007202355,-0.00712773871785999));
#26805=CARTESIAN_POINT('',(-0.00304679361069417,0.0090747881914824,-0.00644594996068229));
#26806=CARTESIAN_POINT('',(-0.00437435373071718,0.00929150225121181,-0.00563021454807782));
#26807=CARTESIAN_POINT('',(-0.00628354077872295,0.00972493037067064,-0.00336877961154627));
#26808=CARTESIAN_POINT('',(-0.00686516770670571,0.00994164443040004,-0.00192308008761919));
#26809=CARTESIAN_POINT('',(-0.00703466960828227,0.0103284016102796,0.000711765157279578));
#26810=CARTESIAN_POINT('',(-0.00680958112794892,0.0104984447304297,0.00188911187734821));
#26811=CARTESIAN_POINT('',(-0.00632123498561395,0.0106684878505798,0.00294371336778276));
#26812=CARTESIAN_POINT('',(0.00719810548634731,0.000469058362981516,0.000423958207366928));
#26813=CARTESIAN_POINT('',(0.00726617396473655,0.000639097215807201,-0.000775852216972529));
#26814=CARTESIAN_POINT('',(0.00703442489669408,0.00080913606863289,-0.00199346208129777));
#26815=CARTESIAN_POINT('',(0.00586850968232211,0.00119588898118803,-0.00446219284680798));
#26816=CARTESIAN_POINT('',(0.00475899394815174,0.00141260304091748,-0.00563076703091534));
#26817=CARTESIAN_POINT('',(0.00206258024653102,0.0018460311603764,-0.00707829343584338));
#26818=CARTESIAN_POINT('',(0.000475682279080687,0.00206274522010586,-0.00735724565666407));
#26819=CARTESIAN_POINT('',(-0.00255275979645077,0.00249617333956479,-0.00691650092326816));
#26820=CARTESIAN_POINT('',(-0.0039943039045319,0.00271288739929425,-0.00619680396905156));
#26821=CARTESIAN_POINT('',(-0.00616644181367082,0.00314631551875318,-0.00404103461588991));
#26822=CARTESIAN_POINT('',(-0.00689703561472861,0.00336302957848265,-0.00260496221694487));
#26823=CARTESIAN_POINT('',(-0.0073606035437174,0.00379645769794158,0.000420055338188199));
#26824=CARTESIAN_POINT('',(-0.00709357767164839,0.00401317175767105,0.00200900049437622));
#26825=CARTESIAN_POINT('',(-0.00566668089254228,0.00444659987712998,0.0047163168822455));
#26826=CARTESIAN_POINT('',(-0.00450680998550517,0.00466331393685945,0.00583468811392677));
#26827=CARTESIAN_POINT('',(-0.00174932161037469,0.00509674205631838,0.00716203877773041));
#26828=CARTESIAN_POINT('',(-0.000151704142281321,0.00531345611604784,0.00737101820985279));
#26829=CARTESIAN_POINT('',(0.00285441969343851,0.00574688423550677,0.00679758867617607));
#26830=CARTESIAN_POINT('',(0.00426292606106497,0.00596359829523623,0.00601517971037698));
#26831=CARTESIAN_POINT('',(0.00633817134813929,0.00639702641469514,0.00376596675421775));
#26832=CARTESIAN_POINT('',(0.00700491026758715,0.0066137404744246,0.00229916276385761));
#26833=CARTESIAN_POINT('',(0.00733501331765875,0.0070471685938835,-0.000743308011446658));
#26834=CARTESIAN_POINT('',(0.0069983774482825,0.00726388265361295,-0.00231897479639079));
#26835=CARTESIAN_POINT('',(0.00545381231396769,0.00769731077307185,-0.00496093334631286));
#26836=CARTESIAN_POINT('',(0.00424588304902913,0.00791402483280129,-0.00602722511129081));
#26837=CARTESIAN_POINT('',(0.00143270356182986,0.00834745295226016,-0.00723202624556431));
#26838=CARTESIAN_POINT('',(-0.000172546660430858,0.00856416701198959,-0.00737053561485987));
#26839=CARTESIAN_POINT('',(-0.00315057856462661,0.00899759513144844,-0.00666552263451621));
#26840=CARTESIAN_POINT('',(-0.00452336024656164,0.00921430919117786,-0.00582200028487701));
#26841=CARTESIAN_POINT('',(-0.00649758120074675,0.00964773731063668,-0.00348353258843506));
#26842=CARTESIAN_POINT('',(-0.00709902047299683,0.00986445137036609,-0.00198858724163231));
#26843=CARTESIAN_POINT('',(-0.00727429623040165,0.0102512085502456,0.000736010486467512));
#26844=CARTESIAN_POINT('',(-0.00704154041169653,0.0104212516703957,0.00195346194965887));
#26845=CARTESIAN_POINT('',(-0.00653655941043727,0.0105912947905458,0.00304398703095224));
#26846=CARTESIAN_POINT('',(0.00730414733435704,0.000391865302947556,0.000430203921864076));
#26847=CARTESIAN_POINT('',(0.00737321859149873,0.000561904155773241,-0.000787282002632974));
#26848=CARTESIAN_POINT('',(0.00713805541685607,0.000731943008598929,-0.00202282958687811));
#26849=CARTESIAN_POINT('',(0.00595496404353656,0.00111869592115407,-0.00452792947383419));
#26850=CARTESIAN_POINT('',(0.00482910302253058,0.00133540998088352,-0.00571371898859407));
#26851=CARTESIAN_POINT('',(0.00209296599475677,0.00176883810034244,-0.0071825702234114));
#26852=CARTESIAN_POINT('',(0.000482689987988938,0.0019855521600719,-0.00746563194346884));
#26853=CARTESIAN_POINT('',(-0.00259036682608572,0.00241898027953082,-0.00701839419797155));
#26854=CARTESIAN_POINT('',(-0.00405314763339256,0.00263569433926028,-0.00628809473241681));
#26855=CARTESIAN_POINT('',(-0.00625728528447107,0.00306912245871922,-0.00410056677742228));
#26856=CARTESIAN_POINT('',(-0.00699864212824275,0.00328583651844868,-0.00264333828798249));
#26857=CARTESIAN_POINT('',(-0.00746903929861474,0.00371926463790762,0.000426243555964711));
#26858=CARTESIAN_POINT('',(-0.00719807962521505,0.00393597869763709,0.00203859691047211));
#26859=CARTESIAN_POINT('',(-0.00575016193002726,0.00436940681709602,0.00478579724189588));
#26860=CARTESIAN_POINT('',(-0.00457320390823917,0.00458612087682549,0.00592064421881225));
#26861=CARTESIAN_POINT('',(-0.00177509246031282,0.00501954899628442,0.00726754929420567));
#26862=CARTESIAN_POINT('',(-0.000153939034174578,0.00523626305601388,0.00747960739268273));
#26863=CARTESIAN_POINT('',(0.00289647074977017,0.00566969117547281,0.00689773014626135));
#26864=CARTESIAN_POINT('',(0.00432572710757667,0.00588640523520227,0.00610379480136291));
#26865=CARTESIAN_POINT('',(0.00643154472312439,0.00631983335466118,0.00382144664054589));
#26866=CARTESIAN_POINT('',(0.00710810598086562,0.00653654741439064,0.00233303382462729));
#26867=CARTESIAN_POINT('',(0.00744307207962825,0.00696997553384954,-0.000754258358773985));
#26868=CARTESIAN_POINT('',(0.00710147692064965,0.00718668959357899,-0.00235313772625666));
#26869=CARTESIAN_POINT('',(0.00553415739053934,0.00762011771303789,-0.00503401737389399));
#26870=CARTESIAN_POINT('',(0.00430843301940762,0.00783683177276733,-0.00611601765404865));
#26871=CARTESIAN_POINT('',(0.0014538100229167,0.0082702598922262,-0.00733856781117336));
#26872=CARTESIAN_POINT('',(-0.000175088602442502,0.00848697395195563,-0.00747911768814341));
#26873=CARTESIAN_POINT('',(-0.00319699260703353,0.00892040207141448,-0.00676371851945502));
#26874=CARTESIAN_POINT('',(-0.00458999798626536,0.0091371161311439,-0.00590776947379658));
#26875=CARTESIAN_POINT('',(-0.00659330298746234,0.00957054425060272,-0.00353485167982381));
#26876=CARTESIAN_POINT('',(-0.0072036026094275,0.00978725831033213,-0.00201788293150949));
#26877=CARTESIAN_POINT('',(-0.00738146051365716,0.0101740154902116,0.000746853327307728));
#26878=CARTESIAN_POINT('',(-0.00714527575699089,0.0103440586103618,0.0019822401768676));
#26879=CARTESIAN_POINT('',(-0.00663285542066147,0.0105141017305119,0.00308883077639221));
#26880=CARTESIAN_POINT('',(0.00745069356407664,0.000189771248083037,0.000438835287015107));
#26881=CARTESIAN_POINT('',(0.00752115062737102,0.000359810100908722,-0.00080307757793158));
#26882=CARTESIAN_POINT('',(0.00728126927344812,0.000529848953734411,-0.00206341448142532));
#26883=CARTESIAN_POINT('',(0.00607444103225929,0.000916601866289553,-0.00461877525807863));
#26884=CARTESIAN_POINT('',(0.00492599138040236,0.00113331592601901,-0.00582835577467273));
#26885=CARTESIAN_POINT('',(0.00213495806603116,0.00156674404547792,-0.00732667719959273));
#26886=CARTESIAN_POINT('',(0.000492374403516869,0.00178345810520739,-0.00761541810791863));
#26887=CARTESIAN_POINT('',(-0.00264233846282531,0.00221688622466631,-0.0071592072403866));
#26888=CARTESIAN_POINT('',(-0.00413446766665321,0.00243360028439577,-0.00641425546452866));
#26889=CARTESIAN_POINT('',(-0.00638282787346101,0.00286702840385471,-0.00418283820123627));
#26890=CARTESIAN_POINT('',(-0.00713905887644092,0.00308374246358417,-0.0026963727138018));
#26891=CARTESIAN_POINT('',(-0.00761889382628711,0.0035171705830431,0.000434795462602067));
#26892=CARTESIAN_POINT('',(-0.0073424977731534,0.00373388464277257,0.00207949815157147));
#26893=CARTESIAN_POINT('',(-0.00586552988641539,0.0041673127622315,0.00488181673738215));
#26894=CARTESIAN_POINT('',(-0.0046649580528111,0.00438402682196097,0.00603943263422343));
#26895=CARTESIAN_POINT('',(-0.00181070689900835,0.0048174549414199,0.00741336124180392));
#26896=CARTESIAN_POINT('',(-0.000157027578809877,0.00503416900114937,0.00762967395254313));
#26897=CARTESIAN_POINT('',(0.00295458388035767,0.00546759712060829,0.00703612225423582));
#26898=CARTESIAN_POINT('',(0.00441251601932677,0.00568431118033775,0.0062262578451893));
#26899=CARTESIAN_POINT('',(0.00656058355370951,0.00611773929979667,0.00389811795775938));
#26900=CARTESIAN_POINT('',(0.00725071894912317,0.00633445335952612,0.00237984247937596));
#26901=CARTESIAN_POINT('',(0.00759240561588785,0.00676788147898503,-0.000769391366591733));
#26902=CARTESIAN_POINT('',(0.00724395688723887,0.00698459553871448,-0.00240034973417602));
#26903=CARTESIAN_POINT('',(0.00564519155553264,0.00741802365817337,-0.00513501701597638));
#26904=CARTESIAN_POINT('',(0.00439487495247539,0.00763473771790281,-0.00623872593019245));
#26905=CARTESIAN_POINT('',(0.00148297843475648,0.00806816583736168,-0.00748580463363043));
#26906=CARTESIAN_POINT('',(-0.000178601479905164,0.00828487989709111,-0.00762917442285234));
#26907=CARTESIAN_POINT('',(-0.00326113523608462,0.00871830801654996,-0.00689942189488508));
#26908=CARTESIAN_POINT('',(-0.00468208907760243,0.00893502207627938,-0.00602629957769591));
#26909=CARTESIAN_POINT('',(-0.00672558724323942,0.0093684501957382,-0.00360577291985132));
#26910=CARTESIAN_POINT('',(-0.00734813156735859,0.0095851642554676,-0.00205836857919588));
#26911=CARTESIAN_POINT('',(-0.00752955791073626,0.00997192143534712,0.000761837764814304));
#26912=CARTESIAN_POINT('',(-0.007288634478353,0.0101419645554972,0.0020220107087341));
#26913=CARTESIAN_POINT('',(-0.0067659332338103,0.0103120076756474,0.0031508033084074));
#26914=CARTESIAN_POINT('',(0.0074911979457865,6.48702532524772E-5,0.000441220937668989));
#26915=CARTESIAN_POINT('',(0.00756203803648113,0.000234909106078164,-0.000807443367569745));
#26916=CARTESIAN_POINT('',(0.00732085260987818,0.000404947958903854,-0.00207463187039221));
#26917=CARTESIAN_POINT('',(0.00610746365976755,0.000791700871458998,-0.00464388441529687));
#26918=CARTESIAN_POINT('',(0.00495277066389529,0.00100841493118845,-0.00586004060307266));
#26919=CARTESIAN_POINT('',(0.00214656438907979,0.00144184305064737,-0.00736650738820606));
#26920=CARTESIAN_POINT('',(0.000495051110136548,0.00165855711037683,-0.00765681798556365));
#26921=CARTESIAN_POINT('',(-0.00265670306992994,0.00209198522983576,-0.00719812700809825));
#26922=CARTESIAN_POINT('',(-0.0041569439710532,0.00230869928956522,-0.00644912543327526));
#26923=CARTESIAN_POINT('',(-0.0064175269916507,0.00274212740902416,-0.00420557746351788));
#26924=CARTESIAN_POINT('',(-0.00717786911112494,0.00295884146875362,-0.00271103106858349));
#26925=CARTESIAN_POINT('',(-0.00766031259906214,0.00339226958821256,0.000437159151462911));
#26926=CARTESIAN_POINT('',(-0.00738241396752509,0.00360898364794202,0.00209080297657492));
#26927=CARTESIAN_POINT('',(-0.00589741680531854,0.00404241176740095,0.00490835587321803));
#26928=CARTESIAN_POINT('',(-0.00469031827464905,0.00425912582713042,0.00607226494474913));
#26929=CARTESIAN_POINT('',(-0.00182055048776573,0.00469255394658935,0.00745366267292691));
#26930=CARTESIAN_POINT('',(-0.000157881231551919,0.00490926800631881,0.00767115132957359));
#26931=CARTESIAN_POINT('',(0.00297064595461353,0.00534269612577774,0.00707437289212501));
#26932=CARTESIAN_POINT('',(0.00443650388456516,0.0055594101855072,0.00626010579802976));
#26933=CARTESIAN_POINT('',(0.00659624900930952,0.00599283830496612,0.00391930938864474));
#26934=CARTESIAN_POINT('',(0.00729013620410225,0.00620955236469557,0.00239278007335497));
#26935=CARTESIAN_POINT('',(0.00763368039017796,0.00664298048415448,-0.000773574027082155));
#26936=CARTESIAN_POINT('',(0.00728333738146094,0.00685969454388392,-0.00241339881222951));
#26937=CARTESIAN_POINT('',(0.00567588064395429,0.00729312266334281,-0.00516293263047764));
#26938=CARTESIAN_POINT('',(0.00441876691516466,0.00750983672307225,-0.00627264166357842));
#26939=CARTESIAN_POINT('',(0.00149104038550943,0.00794326484253112,-0.00752649989047846));
#26940=CARTESIAN_POINT('',(-0.00017957241535618,0.00815997890226055,-0.00767064908427772));
#26941=CARTESIAN_POINT('',(-0.00327886382272879,0.0085934070217194,-0.00693692938537633));
#26942=CARTESIAN_POINT('',(-0.00470754242923579,0.00881012108144882,-0.00605906049267568));
#26943=CARTESIAN_POINT('',(-0.00676214971230091,0.00924354920090764,-0.00362537506849006));
#26944=CARTESIAN_POINT('',(-0.00738807838885903,0.00946026326063704,-0.00206955853700509));
#26945=CARTESIAN_POINT('',(-0.00757049102455984,0.00984702044051656,0.000765979361480664));
#26946=CARTESIAN_POINT('',(-0.00732825785442074,0.0100170635606667,0.00203300301339187));
#26947=CARTESIAN_POINT('',(-0.00680271503673494,0.0101871066808168,0.00316793209498263));
#26948=CARTESIAN_POINT('',(0.0074911979457865,-6.37794509163898E-5,0.00044122093766899));
#26949=CARTESIAN_POINT('',(0.00756203803648112,0.000106259401909297,-0.000807443367569744));
#26950=CARTESIAN_POINT('',(0.00732085260987817,0.000276298254734986,-0.00207463187039221));
#26951=CARTESIAN_POINT('',(0.00610746365976754,0.00066305116729013,-0.00464388441529687));
#26952=CARTESIAN_POINT('',(0.00495277066389528,0.000879765227019586,-0.00586004060307266));
#26953=CARTESIAN_POINT('',(0.00214656438907979,0.0013131933464785,-0.00736650738820606));
#26954=CARTESIAN_POINT('',(0.000495051110136555,0.00152990740620797,-0.00765681798556366));
#26955=CARTESIAN_POINT('',(-0.00265670306992994,0.00196333552566689,-0.00719812700809826));
#26956=CARTESIAN_POINT('',(-0.0041569439710532,0.00218004958539635,-0.00644912543327526));
#26957=CARTESIAN_POINT('',(-0.0064175269916507,0.00261347770485529,-0.00420557746351788));
#26958=CARTESIAN_POINT('',(-0.00717786911112494,0.00283019176458475,-0.00271103106858349));
#26959=CARTESIAN_POINT('',(-0.00766031259906214,0.00326361988404369,0.000437159151462912));
#26960=CARTESIAN_POINT('',(-0.00738241396752509,0.00348033394377315,0.00209080297657492));
#26961=CARTESIAN_POINT('',(-0.00589741680531855,0.00391376206323209,0.00490835587321803));
#26962=CARTESIAN_POINT('',(-0.00469031827464905,0.00413047612296156,0.00607226494474913));
#26963=CARTESIAN_POINT('',(-0.00182055048776573,0.00456390424242049,0.00745366267292691));
#26964=CARTESIAN_POINT('',(-0.000157881231551919,0.00478061830214995,0.00767115132957359));
#26965=CARTESIAN_POINT('',(0.00297064595461353,0.00521404642160888,0.00707437289212501));
#26966=CARTESIAN_POINT('',(0.00443650388456517,0.00543076048133834,0.00626010579802976));
#26967=CARTESIAN_POINT('',(0.00659624900930953,0.00586418860079725,0.00391930938864474));
#26968=CARTESIAN_POINT('',(0.00729013620410225,0.00608090266052671,0.00239278007335497));
#26969=CARTESIAN_POINT('',(0.00763368039017796,0.00651433077998561,-0.000773574027082154));
#26970=CARTESIAN_POINT('',(0.00728333738146094,0.00673104483971505,-0.00241339881222951));
#26971=CARTESIAN_POINT('',(0.00567588064395429,0.00716447295917395,-0.00516293263047764));
#26972=CARTESIAN_POINT('',(0.00441876691516466,0.00738118701890338,-0.00627264166357842));
#26973=CARTESIAN_POINT('',(0.00149104038550943,0.00781461513836225,-0.00752649989047846));
#26974=CARTESIAN_POINT('',(-0.00017957241535618,0.00803132919809169,-0.00767064908427772));
#26975=CARTESIAN_POINT('',(-0.00327886382272879,0.00846475731755054,-0.00693692938537633));
#26976=CARTESIAN_POINT('',(-0.00470754242923578,0.00868147137727995,-0.00605906049267568));
#26977=CARTESIAN_POINT('',(-0.0067621497123009,0.00911489949673877,-0.00362537506849006));
#26978=CARTESIAN_POINT('',(-0.00738807838885903,0.00933161355646818,-0.00206955853700509));
#26979=CARTESIAN_POINT('',(-0.00757049102455984,0.0097183707363477,0.000765979361480661));
#26980=CARTESIAN_POINT('',(-0.00732825785442074,0.00988841385649782,0.00203300301339187));
#26981=CARTESIAN_POINT('',(-0.00680271503673493,0.0100584569766479,0.00316793209498262));
#26982=CARTESIAN_POINT('',(0.00749116145915708,-6.75281602410481E-5,0.000441218788658249));
#26983=CARTESIAN_POINT('',(0.00756200120481795,0.000102510692584639,-0.000807439434836002));
#26984=CARTESIAN_POINT('',(0.00732081695293276,0.000272549545410328,-0.00207462176569003));
#26985=CARTESIAN_POINT('',(0.00610743391275447,0.000659302457965472,-0.004643861796793));
#26986=CARTESIAN_POINT('',(0.00495274654093002,0.000876016517694927,-0.00586001206115835));
#26987=CARTESIAN_POINT('',(0.00214655393402308,0.00130944463715384,-0.00736647150889449));
#26988=CARTESIAN_POINT('',(0.000495048698940571,0.00152615869688331,-0.00765678069226526));
#26989=CARTESIAN_POINT('',(-0.00265669013019172,0.00195958681634223,-0.00719809194890018));
#26990=CARTESIAN_POINT('',(-0.0041569237242415,0.0021763008760717,-0.00644909402216432));
#26991=CARTESIAN_POINT('',(-0.00641749573444313,0.00260972899553063,-0.00420555697983189));
#26992=CARTESIAN_POINT('',(-0.00717783415059498,0.00282644305526009,-0.00271101786423531));
#26993=CARTESIAN_POINT('',(-0.00766027528874288,0.00325987117471903,0.000437157022235508));
#26994=CARTESIAN_POINT('',(-0.00738237801073893,0.00347658523444849,0.00209079279310975));
#26995=CARTESIAN_POINT('',(-0.00589738808135971,0.00391001335390743,0.00490833196657945));
#26996=CARTESIAN_POINT('',(-0.00469029542998442,0.0041267274136369,0.00607223536917492));
#26997=CARTESIAN_POINT('',(-0.00182054162059236,0.00456015553309583,0.0074536263691168));
#26998=CARTESIAN_POINT('',(-0.000157880462575577,0.00477686959282529,0.00767111396646321));
#26999=CARTESIAN_POINT('',(0.00297063148578507,0.00521029771228422,0.00707433843568374));
#27000=CARTESIAN_POINT('',(0.00443648227612893,0.00542701177201368,0.00626007530755787));
#27001=CARTESIAN_POINT('',(0.00659621688161849,0.00586043989147259,0.00391929029925606));
#27002=CARTESIAN_POINT('',(0.00729010069676417,0.00607715395120205,0.00239276841908012));
#27003=CARTESIAN_POINT('',(0.00763364320957354,0.00651058207066095,-0.000773570259312425));
#27004=CARTESIAN_POINT('',(0.00728330190723721,0.0067272961303904,-0.00241338705752903));
#27005=CARTESIAN_POINT('',(0.0056758529990095,0.00716072424984929,-0.00516290748389749));
#27006=CARTESIAN_POINT('',(0.00441874539311811,0.00737743830957873,-0.00627261111204935));
#27007=CARTESIAN_POINT('',(0.00149103312324799,0.0078108664290376,-0.00752646323190739));
#27008=CARTESIAN_POINT('',(-0.000179571540730757,0.00802758048876703,-0.00767061172361357));
#27009=CARTESIAN_POINT('',(-0.00327884785269434,0.00846100860822588,-0.00693689559836742));
#27010=CARTESIAN_POINT('',(-0.00470751950067918,0.00867772266795529,-0.00605903098141508));
#27011=CARTESIAN_POINT('',(-0.00676211677657388,0.00911115078741411,-0.00362535741073791));
#27012=CARTESIAN_POINT('',(-0.00738804240448374,0.00932786484714353,-0.00206954845701308));
#27013=CARTESIAN_POINT('',(-0.00757045415172555,0.00971462202702305,0.000765975630701511));
#27014=CARTESIAN_POINT('',(-0.00732822216140734,0.00988466514717316,0.0020329931114472));
#27015=CARTESIAN_POINT('',(-0.00680268190343044,0.0100547082673233,0.00316791666525226));
#27016=CARTESIAN_POINT('',(0.00749108869504174,-7.12762246428155E-5,0.000441214502955024));
#27017=CARTESIAN_POINT('',(0.00756192775261285,9.87626281828712E-5,-0.000807431591911178));
#27018=CARTESIAN_POINT('',(0.00732074584342964,0.000268801481008561,-0.0020746016142064));
#27019=CARTESIAN_POINT('',(0.00610737458923994,0.000655554393563705,-0.00464381668943585));
#27020=CARTESIAN_POINT('',(0.00495269843327375,0.00087226845329316,-0.00585995514093365));
#27021=CARTESIAN_POINT('',(0.00214653308383864,0.00130569657275208,-0.00736639995593364));
#27022=CARTESIAN_POINT('',(0.000495043890369721,0.00152241063248154,-0.00765670631943583));
#27023=CARTESIAN_POINT('',(-0.00265666432488661,0.00195583875194046,-0.00719802203146539));
#27024=CARTESIAN_POINT('',(-0.00415688334667402,0.00217255281166993,-0.00644903137999276));
#27025=CARTESIAN_POINT('',(-0.00641743339919614,0.00260598093112886,-0.00420551612987359));
#27026=CARTESIAN_POINT('',(-0.00717776442993084,0.00282269499085832,-0.00271099153122705));
#27027=CARTESIAN_POINT('',(-0.00766020088196928,0.00325612311031726,0.000437152775985556));
#27028=CARTESIAN_POINT('',(-0.007382306303273,0.00347283717004673,0.00209077248455162));
#27029=CARTESIAN_POINT('',(-0.00589733079808942,0.00390626528950566,0.00490828429033655));
#27030=CARTESIAN_POINT('',(-0.00469024987160212,0.00412297934923513,0.00607217638755542));
#27031=CARTESIAN_POINT('',(-0.00182052393707276,0.00455640746869406,0.00745355396959213));
#27032=CARTESIAN_POINT('',(-0.000157878929030712,0.00477312152842352,0.00767103945440996));
#27033=CARTESIAN_POINT('',(0.0029706026310643,0.00520654964788245,0.00707426972030753));
#27034=CARTESIAN_POINT('',(0.00443643918311728,0.00542326370761191,0.00626001450138726));
#27035=CARTESIAN_POINT('',(0.0065961528103942,0.00585669182707082,0.0039192522299002));
#27036=CARTESIAN_POINT('',(0.00729002988561815,0.00607340588680028,0.0023927451773334));
#27037=CARTESIAN_POINT('',(0.00763356906148608,0.00650683400625918,-0.000773562745370043));
#27038=CARTESIAN_POINT('',(0.00728323116213006,0.00672354806598863,-0.0024133636155067));
#27039=CARTESIAN_POINT('',(0.00567579786758234,0.00715697618544752,-0.00516285733487884));
#27040=CARTESIAN_POINT('',(0.00441870247239064,0.00737369024517696,-0.00627255018411434));
#27041=CARTESIAN_POINT('',(0.00149101864035281,0.00780711836463583,-0.00752639012489431));
#27042=CARTESIAN_POINT('',(-0.000179569796493315,0.00802383242436526,-0.00767053721643878));
#27043=CARTESIAN_POINT('',(-0.00327881600416663,0.00845726054382411,-0.00693682821801869));
#27044=CARTESIAN_POINT('',(-0.00470747377499381,0.00867397460355352,-0.00605897212805414));
#27045=CARTESIAN_POINT('',(-0.00676205109390934,0.00910740272301235,-0.00362532219644888));
#27046=CARTESIAN_POINT('',(-0.00738797064199769,0.00932411678274176,-0.00206952835480817));
#27047=CARTESIAN_POINT('',(-0.0075703806174142,0.00971087396262128,0.000765968190528255));
#27048=CARTESIAN_POINT('',(-0.00732815097997499,0.0098809170827714,0.00203297336431639));
#27049=CARTESIAN_POINT('',(-0.00680261582674348,0.0100509602029215,0.00316788589423566));
#45463=MECHANICAL_DESIGN_GEOMETRIC_PRESENTATION_REPRESENTATION('',(#13531),#45464);
#45464=(
GEOMETRIC_REPRESENTATION_CONTEXT(3)
GLOBAL_UNCERTAINTY_ASSIGNED_CONTEXT((#45492))
GLOBAL_UNIT_ASSIGNED_CONTEXT((#45522,#45521,#45520))
REPRESENTATION_CONTEXT('MAS-690','TOP_LEVEL_ASSEMBLY_PART')
);
#45467=(
GEOMETRIC_REPRESENTATION_CONTEXT(3)
GLOBAL_UNCERTAINTY_ASSIGNED_CONTEXT((#45495))
GLOBAL_UNIT_ASSIGNED_CONTEXT((#45522,#45521,#45520))
REPRESENTATION_CONTEXT('75632s_.prt','COMPONENT_PART')
);
#45492=UNCERTAINTY_MEASURE_WITH_UNIT(LENGTH_MEASURE(1.E-8),#45522,
'DISTANCE_ACCURACY_VALUE','Maximum Tolerance applied to model');
#45495=UNCERTAINTY_MEASURE_WITH_UNIT(LENGTH_MEASURE(2.E-5),#45522,
'DISTANCE_ACCURACY_VALUE','Maximum Tolerance applied to model');
#45520=(
NAMED_UNIT(*)
SI_UNIT($,.STERADIAN.)
SOLID_ANGLE_UNIT()
);
#45521=(
NAMED_UNIT(*)
PLANE_ANGLE_UNIT()
SI_UNIT($,.RADIAN.)
);
#45522=(
LENGTH_UNIT()
NAMED_UNIT(*)
SI_UNIT($,.METRE.)
);
#45528=PRODUCT_DEFINITION_SHAPE('','',#45588);
#45588=PRODUCT_DEFINITION('','',#45644,#45616);
#45616=PRODUCT_DEFINITION_CONTEXT('',#45782,'design');
#45644=PRODUCT_DEFINITION_FORMATION_WITH_SPECIFIED_SOURCE('','',#45700,
 .NOT_KNOWN.);
#45700=PRODUCT('75632s_.prt','75632s_.prt','75632s_.prt',(#45756));
#45756=PRODUCT_CONTEXT('',#45782,'mechanical');
#45782=APPLICATION_CONTEXT('managed model based 3d engineering');
ENDSEC;
END-ISO-10303-21;
